ISO-10303-21;
HEADER;
/* Generated by software containing ST-Developer
 * from STEP Tools, Inc. (www.steptools.com) 
 */

FILE_DESCRIPTION(
/* description */ (''),
/* implementation_level */ '2;1');

FILE_NAME(
/* name */ 'Socket head cap screw M3x16.step',
/* time_stamp */ '2026-11-10T05:20:16-08:00',
/* author */ (''),
/* organization */ (''),
/* preprocessor_version */ 'ST-DEVELOPER v20.2',
/* originating_system */ 'Autodesk Translation Framework v15.17.0.0',
/* authorisation */ '');

FILE_SCHEMA (('AUTOMOTIVE_DESIGN { 1 0 10303 214 3 1 1 }'));
ENDSEC;

DATA;
#10=MECHANICAL_DESIGN_GEOMETRIC_PRESENTATION_REPRESENTATION('',(#118),#24809);
#75=CONICAL_SURFACE('',#10550,0.1,0.785398163397448);
#98=SHAPE_REPRESENTATION_RELATIONSHIP('SRR','None',#24862,#108);
#108=ADVANCED_BREP_SHAPE_REPRESENTATION('',(#128),#24805);
#118=STYLED_ITEM('',(#24921),#128);
#128=MANIFOLD_SOLID_BREP('Body1',#9895);
#181=FACE_BOUND('',#2400,.T.);
#182=FACE_BOUND('',#2403,.T.);
#269=B_SPLINE_SURFACE_WITH_KNOTS('',3,3,((#21470,#21471,#21472,#21473,#21474,
#21475,#21476,#21477,#21478,#21479,#21480,#21481,#21482,#21483,#21484,#21485,
#21486,#21487,#21488,#21489,#21490,#21491,#21492,#21493,#21494,#21495,#21496,
#21497,#21498,#21499,#21500,#21501,#21502,#21503,#21504,#21505,#21506,#21507,
#21508,#21509,#21510,#21511,#21512,#21513,#21514,#21515,#21516,#21517,#21518,
#21519,#21520,#21521,#21522,#21523,#21524,#21525,#21526,#21527,#21528,#21529,
#21530,#21531,#21532,#21533,#21534,#21535,#21536,#21537,#21538,#21539,#21540,
#21541,#21542,#21543,#21544,#21545,#21546,#21547,#21548,#21549,#21550,#21551,
#21552,#21553,#21554,#21555,#21556,#21557,#21558,#21559,#21560,#21561,#21562,
#21563,#21564,#21565,#21566,#21567,#21568,#21569,#21570,#21571,#21572,#21573,
#21574,#21575,#21576,#21577,#21578,#21579,#21580,#21581,#21582,#21583,#21584,
#21585,#21586,#21587,#21588,#21589,#21590,#21591,#21592,#21593,#21594,#21595,
#21596,#21597,#21598,#21599,#21600,#21601,#21602,#21603,#21604,#21605,#21606,
#21607,#21608,#21609,#21610,#21611,#21612,#21613,#21614,#21615,#21616,#21617,
#21618,#21619,#21620,#21621,#21622,#21623,#21624,#21625,#21626,#21627,#21628,
#21629,#21630,#21631,#21632,#21633,#21634,#21635,#21636,#21637,#21638,#21639,
#21640,#21641,#21642,#21643,#21644,#21645,#21646,#21647,#21648,#21649,#21650,
#21651,#21652,#21653,#21654,#21655,#21656,#21657,#21658,#21659,#21660,#21661,
#21662,#21663,#21664,#21665),(#21666,#21667,#21668,#21669,#21670,#21671,
#21672,#21673,#21674,#21675,#21676,#21677,#21678,#21679,#21680,#21681,#21682,
#21683,#21684,#21685,#21686,#21687,#21688,#21689,#21690,#21691,#21692,#21693,
#21694,#21695,#21696,#21697,#21698,#21699,#21700,#21701,#21702,#21703,#21704,
#21705,#21706,#21707,#21708,#21709,#21710,#21711,#21712,#21713,#21714,#21715,
#21716,#21717,#21718,#21719,#21720,#21721,#21722,#21723,#21724,#21725,#21726,
#21727,#21728,#21729,#21730,#21731,#21732,#21733,#21734,#21735,#21736,#21737,
#21738,#21739,#21740,#21741,#21742,#21743,#21744,#21745,#21746,#21747,#21748,
#21749,#21750,#21751,#21752,#21753,#21754,#21755,#21756,#21757,#21758,#21759,
#21760,#21761,#21762,#21763,#21764,#21765,#21766,#21767,#21768,#21769,#21770,
#21771,#21772,#21773,#21774,#21775,#21776,#21777,#21778,#21779,#21780,#21781,
#21782,#21783,#21784,#21785,#21786,#21787,#21788,#21789,#21790,#21791,#21792,
#21793,#21794,#21795,#21796,#21797,#21798,#21799,#21800,#21801,#21802,#21803,
#21804,#21805,#21806,#21807,#21808,#21809,#21810,#21811,#21812,#21813,#21814,
#21815,#21816,#21817,#21818,#21819,#21820,#21821,#21822,#21823,#21824,#21825,
#21826,#21827,#21828,#21829,#21830,#21831,#21832,#21833,#21834,#21835,#21836,
#21837,#21838,#21839,#21840,#21841,#21842,#21843,#21844,#21845,#21846,#21847,
#21848,#21849,#21850,#21851,#21852,#21853,#21854,#21855,#21856,#21857,#21858,
#21859,#21860,#21861),(#21862,#21863,#21864,#21865,#21866,#21867,#21868,
#21869,#21870,#21871,#21872,#21873,#21874,#21875,#21876,#21877,#21878,#21879,
#21880,#21881,#21882,#21883,#21884,#21885,#21886,#21887,#21888,#21889,#21890,
#21891,#21892,#21893,#21894,#21895,#21896,#21897,#21898,#21899,#21900,#21901,
#21902,#21903,#21904,#21905,#21906,#21907,#21908,#21909,#21910,#21911,#21912,
#21913,#21914,#21915,#21916,#21917,#21918,#21919,#21920,#21921,#21922,#21923,
#21924,#21925,#21926,#21927,#21928,#21929,#21930,#21931,#21932,#21933,#21934,
#21935,#21936,#21937,#21938,#21939,#21940,#21941,#21942,#21943,#21944,#21945,
#21946,#21947,#21948,#21949,#21950,#21951,#21952,#21953,#21954,#21955,#21956,
#21957,#21958,#21959,#21960,#21961,#21962,#21963,#21964,#21965,#21966,#21967,
#21968,#21969,#21970,#21971,#21972,#21973,#21974,#21975,#21976,#21977,#21978,
#21979,#21980,#21981,#21982,#21983,#21984,#21985,#21986,#21987,#21988,#21989,
#21990,#21991,#21992,#21993,#21994,#21995,#21996,#21997,#21998,#21999,#22000,
#22001,#22002,#22003,#22004,#22005,#22006,#22007,#22008,#22009,#22010,#22011,
#22012,#22013,#22014,#22015,#22016,#22017,#22018,#22019,#22020,#22021,#22022,
#22023,#22024,#22025,#22026,#22027,#22028,#22029,#22030,#22031,#22032,#22033,
#22034,#22035,#22036,#22037,#22038,#22039,#22040,#22041,#22042,#22043,#22044,
#22045,#22046,#22047,#22048,#22049,#22050,#22051,#22052,#22053,#22054,#22055,
#22056,#22057),(#22058,#22059,#22060,#22061,#22062,#22063,#22064,#22065,
#22066,#22067,#22068,#22069,#22070,#22071,#22072,#22073,#22074,#22075,#22076,
#22077,#22078,#22079,#22080,#22081,#22082,#22083,#22084,#22085,#22086,#22087,
#22088,#22089,#22090,#22091,#22092,#22093,#22094,#22095,#22096,#22097,#22098,
#22099,#22100,#22101,#22102,#22103,#22104,#22105,#22106,#22107,#22108,#22109,
#22110,#22111,#22112,#22113,#22114,#22115,#22116,#22117,#22118,#22119,#22120,
#22121,#22122,#22123,#22124,#22125,#22126,#22127,#22128,#22129,#22130,#22131,
#22132,#22133,#22134,#22135,#22136,#22137,#22138,#22139,#22140,#22141,#22142,
#22143,#22144,#22145,#22146,#22147,#22148,#22149,#22150,#22151,#22152,#22153,
#22154,#22155,#22156,#22157,#22158,#22159,#22160,#22161,#22162,#22163,#22164,
#22165,#22166,#22167,#22168,#22169,#22170,#22171,#22172,#22173,#22174,#22175,
#22176,#22177,#22178,#22179,#22180,#22181,#22182,#22183,#22184,#22185,#22186,
#22187,#22188,#22189,#22190,#22191,#22192,#22193,#22194,#22195,#22196,#22197,
#22198,#22199,#22200,#22201,#22202,#22203,#22204,#22205,#22206,#22207,#22208,
#22209,#22210,#22211,#22212,#22213,#22214,#22215,#22216,#22217,#22218,#22219,
#22220,#22221,#22222,#22223,#22224,#22225,#22226,#22227,#22228,#22229,#22230,
#22231,#22232,#22233,#22234,#22235,#22236,#22237,#22238,#22239,#22240,#22241,
#22242,#22243,#22244,#22245,#22246,#22247,#22248,#22249,#22250,#22251,#22252,
#22253)),.UNSPECIFIED.,.F.,.F.,.F.,(4,4),(4,1,1,1,1,1,1,1,1,1,1,1,1,1,1,
1,1,1,1,1,1,1,1,1,1,1,1,1,1,1,1,1,1,1,1,1,1,1,1,1,1,1,1,1,1,1,1,1,1,1,1,
1,1,1,1,1,1,1,1,1,1,1,1,1,1,1,1,1,1,1,1,1,1,1,1,1,1,1,1,1,1,1,1,1,1,1,1,
1,1,1,1,1,1,1,1,1,1,1,1,1,1,1,1,1,1,1,1,1,1,1,1,1,1,1,1,1,1,1,1,1,1,1,1,
1,1,1,1,1,1,1,1,1,1,1,1,1,1,1,1,1,1,1,1,1,1,1,1,1,1,1,1,1,1,1,1,1,1,1,1,
1,1,1,1,1,1,1,1,1,1,1,1,1,1,1,1,1,1,1,1,1,1,1,1,1,1,1,1,1,1,1,1,1,1,4),
(0.,0.0329955678841871),(11.6159397475006,12.61358260836,13.6112254692194,
14.6088683300789,15.6065111909383,16.6041540517977,17.6017969126571,18.5994397735165,
19.5970826343759,20.5947254952353,21.5923683560947,22.5900112169541,23.5876540778135,
24.5852969386729,25.5829397995323,26.5805826603917,27.5782255212511,28.5758683821105,
29.5735112429699,30.5711541038294,31.5687969646888,32.5664398255482,33.5640826864076,
34.561725547267,35.5593684081264,36.5570112689858,37.5546541298452,38.5522969907046,
39.549939851564,40.5475827124234,41.5452255732828,42.5428684341422,43.5405112950016,
44.538154155861,45.5357970167204,46.5334398775799,47.5310827384393,48.5287255992987,
49.5263684601581,50.5240113210175,51.5216541818769,52.5192970427363,53.5169399035957,
54.5145827644551,55.5122256253145,56.5098684861739,57.5075113470333,58.5051542078927,
59.5027970687521,60.5004399296115,61.4980827904709,62.4957256513303,63.4933685121897,
64.4910113730492,65.4886542339086,66.486297094768,67.4839399556274,68.4815828164868,
69.4792256773462,70.4768685382056,71.474511399065,72.4721542599244,73.4697971207838,
74.4674399816432,75.4650828425026,76.462725703362,77.4603685642214,78.4580114250808,
79.4556542859402,80.4532971467996,81.4509400076591,82.4485828685185,83.4462257293779,
84.4438685902373,85.4415114510967,86.4391543119561,87.4367971728155,88.4344400336749,
89.4320828945343,90.4297257553937,91.4273686162531,92.4250114771125,93.4226543379719,
94.4202971988313,95.4179400596907,96.4155829205502,97.4132257814096,98.410868642269,
99.4085115031284,100.406154363988,101.403797224847,102.401440085707,103.399082946566,
104.396725807425,105.394368668285,106.392011529144,107.389654390004,108.387297250863,
109.384940111722,110.382582972582,111.380225833441,112.377868694301,113.37551155516,
114.373154416019,115.370797276879,116.368440137738,117.366082998598,118.363725859457,
119.361368720316,120.359011581176,121.356654442035,122.354297302895,123.351940163754,
124.349583024614,125.347225885473,126.344868746332,127.342511607192,128.340154468051,
129.337797328911,130.33544018977,131.333083050629,132.330725911489,133.328368772348,
134.326011633208,135.323654494067,136.321297354926,137.318940215786,138.316583076645,
139.314225937505,140.311868798364,141.309511659223,142.307154520083,143.304797380942,
144.302440241802,145.300083102661,146.29772596352,147.29536882438,148.293011685239,
149.290654546099,150.288297406958,151.285940267817,152.283583128677,153.281225989536,
154.278868850396,155.276511711255,156.274154572115,157.271797432974,158.269440293833,
159.267083154693,160.264726015552,161.262368876412,162.260011737271,163.25765459813,
164.25529745899,165.252940319849,166.250583180709,167.248226041568,168.245868902427,
169.243511763287,170.241154624146,171.238797485006,172.236440345865,173.234083206724,
174.231726067584,175.229368928443,176.227011789303,177.224654650162,178.222297511021,
179.219940371881,180.21758323274,181.2152260936,182.212868954459,183.210511815318,
184.208154676178,185.205797537037,186.203440397897,187.201083258756,188.198726119616,
189.196368980475,190.194011841334,191.191654702194,192.189297563053,193.186940423913,
194.184583284772,195.182226145631,196.179869006491,197.17751186735,198.17515472821,
199.172797589069,200.170440449928,201.168083310788,202.165726171647,203.163369032507,
204.161011893366),.UNSPECIFIED.);
#270=B_SPLINE_SURFACE_WITH_KNOTS('',3,3,((#22343,#22344,#22345,#22346,#22347,
#22348,#22349,#22350,#22351,#22352,#22353,#22354,#22355,#22356,#22357,#22358,
#22359,#22360,#22361,#22362,#22363,#22364,#22365,#22366,#22367,#22368,#22369,
#22370,#22371,#22372,#22373,#22374,#22375,#22376,#22377,#22378,#22379,#22380,
#22381,#22382,#22383,#22384,#22385,#22386,#22387,#22388,#22389,#22390,#22391,
#22392,#22393,#22394,#22395,#22396,#22397,#22398,#22399,#22400,#22401,#22402,
#22403,#22404,#22405,#22406,#22407,#22408,#22409,#22410,#22411,#22412,#22413,
#22414,#22415,#22416,#22417,#22418,#22419,#22420,#22421,#22422,#22423,#22424,
#22425,#22426,#22427,#22428,#22429,#22430,#22431,#22432,#22433,#22434,#22435,
#22436,#22437,#22438,#22439,#22440,#22441,#22442,#22443,#22444,#22445,#22446,
#22447,#22448,#22449,#22450,#22451,#22452,#22453,#22454,#22455,#22456,#22457,
#22458,#22459,#22460,#22461,#22462,#22463,#22464,#22465,#22466,#22467,#22468,
#22469,#22470,#22471,#22472,#22473,#22474,#22475,#22476,#22477,#22478,#22479,
#22480,#22481,#22482,#22483,#22484,#22485,#22486,#22487,#22488,#22489,#22490,
#22491,#22492,#22493,#22494,#22495,#22496,#22497,#22498,#22499,#22500,#22501,
#22502,#22503,#22504,#22505,#22506,#22507,#22508,#22509,#22510,#22511,#22512,
#22513,#22514,#22515,#22516,#22517,#22518,#22519,#22520,#22521,#22522,#22523,
#22524,#22525,#22526,#22527,#22528,#22529,#22530,#22531,#22532,#22533,#22534,
#22535,#22536,#22537,#22538,#22539,#22540),(#22541,#22542,#22543,#22544,
#22545,#22546,#22547,#22548,#22549,#22550,#22551,#22552,#22553,#22554,#22555,
#22556,#22557,#22558,#22559,#22560,#22561,#22562,#22563,#22564,#22565,#22566,
#22567,#22568,#22569,#22570,#22571,#22572,#22573,#22574,#22575,#22576,#22577,
#22578,#22579,#22580,#22581,#22582,#22583,#22584,#22585,#22586,#22587,#22588,
#22589,#22590,#22591,#22592,#22593,#22594,#22595,#22596,#22597,#22598,#22599,
#22600,#22601,#22602,#22603,#22604,#22605,#22606,#22607,#22608,#22609,#22610,
#22611,#22612,#22613,#22614,#22615,#22616,#22617,#22618,#22619,#22620,#22621,
#22622,#22623,#22624,#22625,#22626,#22627,#22628,#22629,#22630,#22631,#22632,
#22633,#22634,#22635,#22636,#22637,#22638,#22639,#22640,#22641,#22642,#22643,
#22644,#22645,#22646,#22647,#22648,#22649,#22650,#22651,#22652,#22653,#22654,
#22655,#22656,#22657,#22658,#22659,#22660,#22661,#22662,#22663,#22664,#22665,
#22666,#22667,#22668,#22669,#22670,#22671,#22672,#22673,#22674,#22675,#22676,
#22677,#22678,#22679,#22680,#22681,#22682,#22683,#22684,#22685,#22686,#22687,
#22688,#22689,#22690,#22691,#22692,#22693,#22694,#22695,#22696,#22697,#22698,
#22699,#22700,#22701,#22702,#22703,#22704,#22705,#22706,#22707,#22708,#22709,
#22710,#22711,#22712,#22713,#22714,#22715,#22716,#22717,#22718,#22719,#22720,
#22721,#22722,#22723,#22724,#22725,#22726,#22727,#22728,#22729,#22730,#22731,
#22732,#22733,#22734,#22735,#22736,#22737,#22738),(#22739,#22740,#22741,
#22742,#22743,#22744,#22745,#22746,#22747,#22748,#22749,#22750,#22751,#22752,
#22753,#22754,#22755,#22756,#22757,#22758,#22759,#22760,#22761,#22762,#22763,
#22764,#22765,#22766,#22767,#22768,#22769,#22770,#22771,#22772,#22773,#22774,
#22775,#22776,#22777,#22778,#22779,#22780,#22781,#22782,#22783,#22784,#22785,
#22786,#22787,#22788,#22789,#22790,#22791,#22792,#22793,#22794,#22795,#22796,
#22797,#22798,#22799,#22800,#22801,#22802,#22803,#22804,#22805,#22806,#22807,
#22808,#22809,#22810,#22811,#22812,#22813,#22814,#22815,#22816,#22817,#22818,
#22819,#22820,#22821,#22822,#22823,#22824,#22825,#22826,#22827,#22828,#22829,
#22830,#22831,#22832,#22833,#22834,#22835,#22836,#22837,#22838,#22839,#22840,
#22841,#22842,#22843,#22844,#22845,#22846,#22847,#22848,#22849,#22850,#22851,
#22852,#22853,#22854,#22855,#22856,#22857,#22858,#22859,#22860,#22861,#22862,
#22863,#22864,#22865,#22866,#22867,#22868,#22869,#22870,#22871,#22872,#22873,
#22874,#22875,#22876,#22877,#22878,#22879,#22880,#22881,#22882,#22883,#22884,
#22885,#22886,#22887,#22888,#22889,#22890,#22891,#22892,#22893,#22894,#22895,
#22896,#22897,#22898,#22899,#22900,#22901,#22902,#22903,#22904,#22905,#22906,
#22907,#22908,#22909,#22910,#22911,#22912,#22913,#22914,#22915,#22916,#22917,
#22918,#22919,#22920,#22921,#22922,#22923,#22924,#22925,#22926,#22927,#22928,
#22929,#22930,#22931,#22932,#22933,#22934,#22935,#22936),(#22937,#22938,
#22939,#22940,#22941,#22942,#22943,#22944,#22945,#22946,#22947,#22948,#22949,
#22950,#22951,#22952,#22953,#22954,#22955,#22956,#22957,#22958,#22959,#22960,
#22961,#22962,#22963,#22964,#22965,#22966,#22967,#22968,#22969,#22970,#22971,
#22972,#22973,#22974,#22975,#22976,#22977,#22978,#22979,#22980,#22981,#22982,
#22983,#22984,#22985,#22986,#22987,#22988,#22989,#22990,#22991,#22992,#22993,
#22994,#22995,#22996,#22997,#22998,#22999,#23000,#23001,#23002,#23003,#23004,
#23005,#23006,#23007,#23008,#23009,#23010,#23011,#23012,#23013,#23014,#23015,
#23016,#23017,#23018,#23019,#23020,#23021,#23022,#23023,#23024,#23025,#23026,
#23027,#23028,#23029,#23030,#23031,#23032,#23033,#23034,#23035,#23036,#23037,
#23038,#23039,#23040,#23041,#23042,#23043,#23044,#23045,#23046,#23047,#23048,
#23049,#23050,#23051,#23052,#23053,#23054,#23055,#23056,#23057,#23058,#23059,
#23060,#23061,#23062,#23063,#23064,#23065,#23066,#23067,#23068,#23069,#23070,
#23071,#23072,#23073,#23074,#23075,#23076,#23077,#23078,#23079,#23080,#23081,
#23082,#23083,#23084,#23085,#23086,#23087,#23088,#23089,#23090,#23091,#23092,
#23093,#23094,#23095,#23096,#23097,#23098,#23099,#23100,#23101,#23102,#23103,
#23104,#23105,#23106,#23107,#23108,#23109,#23110,#23111,#23112,#23113,#23114,
#23115,#23116,#23117,#23118,#23119,#23120,#23121,#23122,#23123,#23124,#23125,
#23126,#23127,#23128,#23129,#23130,#23131,#23132,#23133,#23134)),
 .UNSPECIFIED.,.F.,.F.,.F.,(4,4),(4,1,1,1,1,1,1,1,1,1,1,1,1,1,1,1,1,1,1,
1,1,1,1,1,1,1,1,1,1,1,1,1,1,1,1,1,1,1,1,1,1,1,1,1,1,1,1,1,1,1,1,1,1,1,1,
1,1,1,1,1,1,1,1,1,1,1,1,1,1,1,1,1,1,1,1,1,1,1,1,1,1,1,1,1,1,1,1,1,1,1,1,
1,1,1,1,1,1,1,1,1,1,1,1,1,1,1,1,1,1,1,1,1,1,1,1,1,1,1,1,1,1,1,1,1,1,1,1,
1,1,1,1,1,1,1,1,1,1,1,1,1,1,1,1,1,1,1,1,1,1,1,1,1,1,1,1,1,1,1,1,1,1,1,1,
1,1,1,1,1,1,1,1,1,1,1,1,1,1,1,1,1,1,1,1,1,1,1,1,1,1,1,1,1,1,1,1,4),(0.,
0.0329955678841871),(8.30203615430855,9.30007843543257,10.2981207165566,
11.2961629976806,12.2942052788047,13.2922475599287,14.2902898410527,15.2883321221767,
16.2863744033008,17.2844166844248,18.2824589655488,19.2805012466728,20.2785435277969,
21.2765858089209,22.2746280900449,23.272670371169,24.270712652293,25.268754933417,
26.266797214541,27.2648394956651,28.2628817767891,29.2609240579131,30.2589663390371,
31.2570086201612,32.2550509012852,33.2530931824092,34.2511354635333,35.2491777446573,
36.2472200257813,37.2452623069053,38.2433045880294,39.2413468691534,40.2393891502774,
41.2374314314014,42.2354737125255,43.2335159936495,44.2315582747735,45.2296005558975,
46.2276428370216,47.2256851181456,48.2237273992696,49.2217696803937,50.2198119615177,
51.2178542426417,52.2158965237657,53.2139388048898,54.2119810860138,55.2100233671378,
56.2080656482619,57.2061079293859,58.2041502105099,59.2021924916339,60.200234772758,
61.198277053882,62.196319335006,63.19436161613,64.1924038972541,65.1904461783781,
66.1884884595021,67.1865307406262,68.1845730217502,69.1826153028742,70.1806575839982,
71.1786998651223,72.1767421462463,73.1747844273703,74.1728267084943,75.1708689896184,
76.1689112707424,77.1669535518664,78.1649958329905,79.1630381141145,80.1610803952385,
81.1591226763625,82.1571649574865,83.1552072386106,84.1532495197346,85.1512918008586,
86.1493340819827,87.1473763631067,88.1454186442307,89.1434609253548,90.1415032064788,
91.1395454876028,92.1375877687268,93.1356300498508,94.1336723309749,95.1317146120989,
96.1297568932229,97.127799174347,98.125841455471,99.123883736595,100.121926017719,
101.119968298843,102.118010579967,103.116052861091,104.114095142215,105.112137423339,
106.110179704463,107.108221985587,108.106264266711,109.104306547835,110.102348828959,
111.100391110083,112.098433391207,113.096475672331,114.094517953455,115.092560234579,
116.090602515703,117.088644796828,118.086687077952,119.084729359076,120.0827716402,
121.080813921324,122.078856202448,123.076898483572,124.074940764696,125.07298304582,
126.071025326944,127.069067608068,128.067109889192,129.065152170316,130.06319445144,
131.061236732564,132.059279013688,133.057321294812,134.055363575936,135.05340585706,
136.051448138184,137.049490419308,138.047532700432,139.045574981556,140.04361726268,
141.041659543804,142.039701824928,143.037744106052,144.035786387176,145.0338286683,
146.031870949424,147.029913230548,148.027955511672,149.025997792796,150.02404007392,
151.022082355044,152.020124636168,153.018166917292,154.016209198417,155.014251479541,
156.012293760665,157.010336041789,158.008378322913,159.006420604037,160.004462885161,
161.002505166285,162.000547447409,162.998589728533,163.996632009657,164.994674290781,
165.992716571905,166.990758853029,167.988801134153,168.986843415277,169.984885696401,
170.982927977525,171.980970258649,172.979012539773,173.977054820897,174.975097102021,
175.973139383145,176.971181664269,177.969223945393,178.967266226517,179.965308507641,
180.963350788765,181.961393069889,182.959435351013,183.957477632137,184.955519913261,
185.953562194385,186.951604475509,187.949646756633,188.947689037757,189.945731318881,
190.943773600006,191.94181588113,192.939858162254,193.937900443378,194.935942724502,
195.933985005626,196.93202728675,197.930069567874,198.928111848998,199.926154130122,
200.924196411246,201.92223869237,202.920280973494),.UNSPECIFIED.);
#817=B_SPLINE_CURVE_WITH_KNOTS('',3,(#19094,#19095,#19096,#19097,#19098,
#19099,#19100,#19101,#19102,#19103),.UNSPECIFIED.,.F.,.F.,(4,3,3,4),(-4.09202352044852,
-3.99057144343763,-2.99292858257822,-2.07317267331971),.UNSPECIFIED.);
#818=B_SPLINE_CURVE_WITH_KNOTS('',3,(#19106,#19107,#19108,#19109,#19110,
#19111,#19112),.UNSPECIFIED.,.F.,.F.,(4,3,4),(0.,0.998042281124014,1.12274180646116),
 .UNSPECIFIED.);
#819=B_SPLINE_CURVE_WITH_KNOTS('',3,(#19117,#19118,#19119,#19120,#19121,
#19122,#19123,#19124,#19125,#19126,#19127,#19128,#19129,#19130,#19131,#19132,
#19133,#19134,#19135,#19136,#19137,#19138),.UNSPECIFIED.,.F.,.F.,(4,3,3,
3,3,3,3,4),(-10.3752088276281,-9.97642860859406,-8.97878574773466,-7.98114288687525,
-6.98350002601584,-5.98585716515644,-4.98821430429703,-4.09202352044852),
 .UNSPECIFIED.);
#820=B_SPLINE_CURVE_WITH_KNOTS('',3,(#19139,#19140,#19141,#19142,#19143,
#19144,#19145,#19146,#19147,#19148,#19149,#19150,#19151,#19152,#19153,#19154,
#19155,#19156,#19157,#19158,#19159,#19160),.UNSPECIFIED.,.F.,.F.,(4,3,3,
3,3,3,3,4),(1.12274180646116,1.99608456224804,2.99412684337208,3.99216912449611,
4.99021140562014,5.98825368674417,6.98629596786821,7.40592711364074),
 .UNSPECIFIED.);
#821=B_SPLINE_CURVE_WITH_KNOTS('',3,(#19165,#19166,#19167,#19168,#19169,
#19170,#19171,#19172,#19173,#19174,#19175,#19176,#19177,#19178,#19179,#19180,
#19181,#19182,#19183,#19184,#19185,#19186),.UNSPECIFIED.,.F.,.F.,(4,3,3,
3,3,3,3,4),(-16.6583941348077,-15.9622857737505,-14.9646429128911,-13.9670000520317,
-12.9693571911723,-11.9717143303129,-10.9740714694535,-10.3752088276281),
 .UNSPECIFIED.);
#822=B_SPLINE_CURVE_WITH_KNOTS('',3,(#19187,#19188,#19189,#19190,#19191,
#19192,#19193,#19194,#19195,#19196,#19197,#19198,#19199,#19200,#19201,#19202,
#19203,#19204,#19205,#19206,#19207,#19208),.UNSPECIFIED.,.F.,.F.,(4,3,3,
3,3,3,3,4),(7.40592711364074,7.98433824899223,8.98238053011626,9.98042281124028,
10.9784650923643,11.9765073734883,12.9745496546124,13.6891124208203),
 .UNSPECIFIED.);
#823=B_SPLINE_CURVE_WITH_KNOTS('',3,(#19213,#19214,#19215,#19216,#19217,
#19218,#19219,#19220,#19221,#19222,#19223,#19224,#19225,#19226,#19227,#19228,
#19229,#19230,#19231,#19232,#19233,#19234),.UNSPECIFIED.,.F.,.F.,(4,3,3,
3,3,3,3,4),(-22.9415794419873,-21.9481429389069,-20.9505000780475,-19.9528572171881,
-18.9552143563287,-17.9575714954693,-16.9599286346099,-16.6583941348077),
 .UNSPECIFIED.);
#824=B_SPLINE_CURVE_WITH_KNOTS('',3,(#19235,#19236,#19237,#19238,#19239,
#19240,#19241,#19242,#19243,#19244,#19245,#19246,#19247,#19248,#19249,#19250,
#19251,#19252,#19253,#19254,#19255,#19256,#19257,#19258,#19259),
 .UNSPECIFIED.,.F.,.F.,(4,3,3,3,3,3,3,3,4),(13.6891124208203,13.9725919357364,
14.9706342168604,15.9686764979844,16.9667187791085,17.9647610602325,18.9628033413565,
19.9608456224805,19.9722977279999),.UNSPECIFIED.);
#825=B_SPLINE_CURVE_WITH_KNOTS('',3,(#19264,#19265,#19266,#19267,#19268,
#19269,#19270,#19271,#19272,#19273,#19274,#19275,#19276,#19277,#19278,#19279,
#19280,#19281,#19282,#19283,#19284,#19285),.UNSPECIFIED.,.F.,.F.,(4,3,3,
3,3,3,3,4),(-29.2247647491669,-28.9316429649228,-27.9340001040634,-26.936357243204,
-25.9387143823446,-24.9410715214852,-23.9434286606257,-22.9415794419873),
 .UNSPECIFIED.);
#826=B_SPLINE_CURVE_WITH_KNOTS('',3,(#19286,#19287,#19288,#19289,#19290,
#19291,#19292,#19293,#19294,#19295,#19296,#19297,#19298,#19299,#19300,#19301,
#19302,#19303,#19304,#19305,#19306,#19307),.UNSPECIFIED.,.F.,.F.,(4,3,3,
3,3,3,3,4),(19.9722977279999,20.9588879036046,21.9569301847286,22.9549724658526,
23.9530147469767,24.9510570281007,25.9490993092247,26.2554830351795),
 .UNSPECIFIED.);
#827=B_SPLINE_CURVE_WITH_KNOTS('',3,(#19312,#19313,#19314,#19315,#19316,
#19317,#19318,#19319,#19320,#19321,#19322,#19323,#19324,#19325,#19326,#19327,
#19328,#19329,#19330,#19331,#19332,#19333),.UNSPECIFIED.,.F.,.F.,(4,3,3,
3,3,3,3,4),(-35.5079500563465,-34.9175001300792,-33.9198572692198,-32.9222144083604,
-31.924571547501,-30.9269286866416,-29.9292858257822,-29.2247647491669),
 .UNSPECIFIED.);
#828=B_SPLINE_CURVE_WITH_KNOTS('',3,(#19334,#19335,#19336,#19337,#19338,
#19339,#19340,#19341,#19342,#19343,#19344,#19345,#19346,#19347,#19348,#19349,
#19350,#19351,#19352,#19353,#19354,#19355),.UNSPECIFIED.,.F.,.F.,(4,3,3,
3,3,3,3,4),(26.2554830351795,26.9471415903487,27.9451838714728,28.9432261525968,
29.9412684337208,30.9393107148448,31.9373529959689,32.5386683423591),
 .UNSPECIFIED.);
#829=B_SPLINE_CURVE_WITH_KNOTS('',3,(#19360,#19361,#19362,#19363,#19364,
#19365,#19366,#19367,#19368,#19369,#19370,#19371,#19372,#19373,#19374,#19375,
#19376,#19377,#19378,#19379,#19380,#19381),.UNSPECIFIED.,.F.,.F.,(4,3,3,
3,3,3,3,4),(-41.791135363526,-40.9033572952357,-39.9057144343762,-38.9080715735168,
-37.9104287126574,-36.912785851798,-35.9151429909386,-35.5079500563465),
 .UNSPECIFIED.);
#830=B_SPLINE_CURVE_WITH_KNOTS('',3,(#19382,#19383,#19384,#19385,#19386,
#19387,#19388,#19389,#19390,#19391,#19392,#19393,#19394,#19395,#19396,#19397,
#19398,#19399,#19400,#19401,#19402,#19403),.UNSPECIFIED.,.F.,.F.,(4,3,3,
3,3,3,3,4),(32.5386683423591,32.9353952770929,33.9334375582169,34.931479839341,
35.929522120465,36.927564401589,37.9256066827131,38.8218536495387),
 .UNSPECIFIED.);
#831=B_SPLINE_CURVE_WITH_KNOTS('',3,(#19408,#19409,#19410,#19411,#19412,
#19413,#19414,#19415,#19416,#19417,#19418,#19419,#19420,#19421,#19422,#19423,
#19424,#19425,#19426,#19427,#19428,#19429,#19430,#19431,#19432),
 .UNSPECIFIED.,.F.,.F.,(4,3,3,3,3,3,3,3,4),(-48.0743206707056,-47.8868573212515,
-46.8892144603921,-45.8915715995327,-44.8939287386733,-43.8962858778139,
-42.8986430169545,-41.9010001560951,-41.791135363526),.UNSPECIFIED.);
#832=B_SPLINE_CURVE_WITH_KNOTS('',3,(#19433,#19434,#19435,#19436,#19437,
#19438,#19439,#19440,#19441,#19442,#19443,#19444,#19445,#19446,#19447,#19448,
#19449,#19450,#19451,#19452,#19453,#19454,#19455,#19456,#19457),
 .UNSPECIFIED.,.F.,.F.,(4,3,3,3,3,3,3,3,4),(38.8218536495387,38.9236489638371,
39.9216912449611,40.9197335260851,41.9177758072091,42.9158180883332,43.9138603694572,
44.9119026505812,45.1050389567183),.UNSPECIFIED.);
#833=B_SPLINE_CURVE_WITH_KNOTS('',3,(#19462,#19463,#19464,#19465,#19466,
#19467,#19468,#19469,#19470,#19471,#19472,#19473,#19474,#19475,#19476,#19477,
#19478,#19479,#19480,#19481,#19482,#19483),.UNSPECIFIED.,.F.,.F.,(4,3,3,
3,3,3,3,4),(-54.3575059778852,-53.8727144864079,-52.8750716255485,-51.8774287646891,
-50.8797859038297,-49.8821430429703,-48.8845001821109,-48.0743206707056),
 .UNSPECIFIED.);
#834=B_SPLINE_CURVE_WITH_KNOTS('',3,(#19484,#19485,#19486,#19487,#19488,
#19489,#19490,#19491,#19492,#19493,#19494,#19495,#19496,#19497,#19498,#19499,
#19500,#19501,#19502,#19503,#19504,#19505),.UNSPECIFIED.,.F.,.F.,(4,3,3,
3,3,3,3,4),(45.1050389567183,45.9099449317052,46.9079872128293,47.9060294939533,
48.9040717750773,49.9021140562014,50.9001563373254,51.3882242638979),
 .UNSPECIFIED.);
#835=B_SPLINE_CURVE_WITH_KNOTS('',3,(#19510,#19511,#19512,#19513,#19514,
#19515,#19516,#19517,#19518,#19519,#19520,#19521,#19522,#19523,#19524,#19525,
#19526,#19527,#19528,#19529,#19530,#19531),.UNSPECIFIED.,.F.,.F.,(4,3,3,
3,3,3,3,4),(-60.6406912850648,-59.8585716515644,-58.860928790705,-57.8632859298455,
-56.8656430689861,-55.8680002081267,-54.8703573472673,-54.3575059778852),
 .UNSPECIFIED.);
#836=B_SPLINE_CURVE_WITH_KNOTS('',3,(#19532,#19533,#19534,#19535,#19536,
#19537,#19538,#19539,#19540,#19541,#19542,#19543,#19544,#19545,#19546,#19547,
#19548,#19549,#19550,#19551,#19552,#19553),.UNSPECIFIED.,.F.,.F.,(4,3,3,
3,3,3,3,4),(51.3882242638979,51.8981986184494,52.8962408995734,53.8942831806975,
54.8923254618215,55.8903677429455,56.8884100240695,57.6714095710775),
 .UNSPECIFIED.);
#837=B_SPLINE_CURVE_WITH_KNOTS('',3,(#19558,#19559,#19560,#19561,#19562,
#19563,#19564,#19565,#19566,#19567,#19568,#19569,#19570,#19571,#19572,#19573,
#19574,#19575,#19576,#19577,#19578,#19579,#19580,#19581,#19582),
 .UNSPECIFIED.,.F.,.F.,(4,3,3,3,3,3,3,3,4),(-66.9238765922444,-66.8420716775802,
-65.8444288167208,-64.8467859558614,-63.849143095002,-62.8515002341426,
-61.8538573732832,-60.8562145124238,-60.6406912850648),.UNSPECIFIED.);
#838=B_SPLINE_CURVE_WITH_KNOTS('',3,(#19583,#19584,#19585,#19586,#19587,
#19588,#19589,#19590,#19591,#19592,#19593,#19594,#19595,#19596,#19597,#19598,
#19599,#19600,#19601,#19602,#19603,#19604,#19605,#19606,#19607),
 .UNSPECIFIED.,.F.,.F.,(4,3,3,3,3,3,3,3,4),(57.6714095710775,57.8864523051936,
58.8844945863176,59.8825368674416,60.8805791485657,61.8786214296897,62.8766637108137,
63.8747059919378,63.9545948782571),.UNSPECIFIED.);
#839=B_SPLINE_CURVE_WITH_KNOTS('',3,(#19612,#19613,#19614,#19615,#19616,
#19617,#19618,#19619,#19620,#19621,#19622,#19623,#19624,#19625,#19626,#19627,
#19628,#19629,#19630,#19631,#19632,#19633),.UNSPECIFIED.,.F.,.F.,(4,3,3,
3,3,3,3,4),(-73.207061899424,-72.8279288427366,-71.8302859818773,-70.8326431210178,
-69.8350002601584,-68.837357399299,-67.8397145384396,-66.9238765922444),
 .UNSPECIFIED.);
#840=B_SPLINE_CURVE_WITH_KNOTS('',3,(#19634,#19635,#19636,#19637,#19638,
#19639,#19640,#19641,#19642,#19643,#19644,#19645,#19646,#19647,#19648,#19649,
#19650,#19651,#19652,#19653,#19654,#19655),.UNSPECIFIED.,.F.,.F.,(4,3,3,
3,3,3,3,4),(63.9545948782571,64.8727482730618,65.8707905541858,66.8688328353098,
67.8668751164338,68.8649173975579,69.8629596786819,70.2377801854366),
 .UNSPECIFIED.);
#841=B_SPLINE_CURVE_WITH_KNOTS('',3,(#19660,#19661,#19662,#19663,#19664,
#19665,#19666,#19667,#19668,#19669,#19670,#19671,#19672,#19673,#19674,#19675,
#19676,#19677,#19678,#19679,#19680,#19681),.UNSPECIFIED.,.F.,.F.,(4,3,3,
3,3,3,3,4),(-79.4902472066036,-78.8137860078931,-77.8161431470337,-76.8185002861743,
-75.8208574253149,-74.8232145644555,-73.825571703596,-73.207061899424),
 .UNSPECIFIED.);
#842=B_SPLINE_CURVE_WITH_KNOTS('',3,(#19682,#19683,#19684,#19685,#19686,
#19687,#19688,#19689,#19690,#19691,#19692,#19693,#19694,#19695,#19696,#19697,
#19698,#19699,#19700,#19701,#19702,#19703),.UNSPECIFIED.,.F.,.F.,(4,3,3,
3,3,3,3,4),(70.2377801854366,70.8610019598059,71.85904424093,72.857086522054,
73.855128803178,74.853171084302,75.8512133654261,76.5209654926162),
 .UNSPECIFIED.);
#843=B_SPLINE_CURVE_WITH_KNOTS('',3,(#19708,#19709,#19710,#19711,#19712,
#19713,#19714,#19715,#19716,#19717,#19718,#19719,#19720,#19721,#19722,#19723,
#19724,#19725,#19726,#19727,#19728,#19729),.UNSPECIFIED.,.F.,.F.,(4,3,3,
3,3,3,3,4),(-85.7734325137832,-84.7996431730495,-83.8020003121901,-82.8043574513307,
-81.8067145904713,-80.8090717296119,-79.8114288687525,-79.4902472066036),
 .UNSPECIFIED.);
#844=B_SPLINE_CURVE_WITH_KNOTS('',3,(#19730,#19731,#19732,#19733,#19734,
#19735,#19736,#19737,#19738,#19739,#19740,#19741,#19742,#19743,#19744,#19745,
#19746,#19747,#19748,#19749,#19750,#19751),.UNSPECIFIED.,.F.,.F.,(4,3,3,
3,3,3,3,4),(76.5209654926162,76.8492556465501,77.8472979276741,78.8453402087982,
79.8433824899222,80.8414247710462,81.8394670521702,82.8041507997958),
 .UNSPECIFIED.);
#845=B_SPLINE_CURVE_WITH_KNOTS('',3,(#19756,#19757,#19758,#19759,#19760,
#19761,#19762,#19763,#19764,#19765,#19766,#19767,#19768,#19769,#19770,#19771,
#19772,#19773,#19774,#19775,#19776,#19777,#19778,#19779,#19780),
 .UNSPECIFIED.,.F.,.F.,(4,3,3,3,3,3,3,3,4),(-92.0566178209628,-91.7831431990654,
-90.7855003382059,-89.7878574773465,-88.7902146164871,-87.7925717556277,
-86.7949288947683,-85.7972860339089,-85.7734325137832),.UNSPECIFIED.);
#846=B_SPLINE_CURVE_WITH_KNOTS('',3,(#19781,#19782,#19783,#19784,#19785,
#19786,#19787,#19788,#19789,#19790,#19791,#19792,#19793,#19794,#19795,#19796,
#19797,#19798,#19799,#19800,#19801,#19802,#19803,#19804,#19805),
 .UNSPECIFIED.,.F.,.F.,(4,3,3,3,3,3,3,3,4),(82.8041507997958,82.8375093332942,
83.8355516144183,84.8335938955423,85.8316361766664,86.8296784577904,87.8277207389144,
88.8257630200384,89.0873361069754),.UNSPECIFIED.);
#847=B_SPLINE_CURVE_WITH_KNOTS('',3,(#19810,#19811,#19812,#19813,#19814,
#19815,#19816,#19817,#19818,#19819,#19820,#19821,#19822,#19823,#19824,#19825,
#19826,#19827,#19828,#19829,#19830,#19831),.UNSPECIFIED.,.F.,.F.,(4,3,3,
3,3,3,3,4),(-98.3398031281424,-97.7690003642218,-96.7713575033624,-95.773714642503,
-94.7760717816436,-93.7784289207842,-92.7807860599248,-92.0566178209628),
 .UNSPECIFIED.);
#848=B_SPLINE_CURVE_WITH_KNOTS('',3,(#19832,#19833,#19834,#19835,#19836,
#19837,#19838,#19839,#19840,#19841,#19842,#19843,#19844,#19845,#19846,#19847,
#19848,#19849,#19850,#19851,#19852,#19853),.UNSPECIFIED.,.F.,.F.,(4,3,3,
3,3,3,3,4),(89.0873361069754,89.8238053011624,90.8218475822865,91.8198898634105,
92.8179321445345,93.8159744256585,94.8140167067826,95.370521414155),
 .UNSPECIFIED.);
#849=B_SPLINE_CURVE_WITH_KNOTS('',3,(#19858,#19859,#19860,#19861,#19862,
#19863,#19864,#19865,#19866,#19867,#19868,#19869,#19870,#19871,#19872,#19873,
#19874,#19875,#19876,#19877,#19878,#19879),.UNSPECIFIED.,.F.,.F.,(4,3,3,
3,3,3,3,4),(-104.622988435322,-103.754857529378,-102.757214668519,-101.759571807659,
-100.7619289468,-99.7642860859406,-98.7666432250812,-98.3398031281424),
 .UNSPECIFIED.);
#850=B_SPLINE_CURVE_WITH_KNOTS('',3,(#19880,#19881,#19882,#19883,#19884,
#19885,#19886,#19887,#19888,#19889,#19890,#19891,#19892,#19893,#19894,#19895,
#19896,#19897,#19898,#19899,#19900,#19901),.UNSPECIFIED.,.F.,.F.,(4,3,3,
3,3,3,3,4),(95.370521414155,95.8120589879066,96.8101012690306,97.8081435501546,
98.8061858312787,99.8042281124027,100.802270393527,101.653706721335),
 .UNSPECIFIED.);
#851=B_SPLINE_CURVE_WITH_KNOTS('',3,(#19906,#19907,#19908,#19909,#19910,
#19911,#19912,#19913,#19914,#19915,#19916,#19917,#19918,#19919,#19920,#19921,
#19922,#19923,#19924,#19925,#19926,#19927,#19928,#19929,#19930),
 .UNSPECIFIED.,.F.,.F.,(4,3,3,3,3,3,3,3,4),(-110.906173742502,-110.738357555394,
-109.740714694535,-108.743071833675,-107.745428972816,-106.747786111956,
-105.750143251097,-104.752500390238,-104.622988435322),.UNSPECIFIED.);
#852=B_SPLINE_CURVE_WITH_KNOTS('',3,(#19931,#19932,#19933,#19934,#19935,
#19936,#19937,#19938,#19939,#19940,#19941,#19942,#19943,#19944,#19945,#19946,
#19947,#19948,#19949,#19950,#19951,#19952,#19953,#19954,#19955),
 .UNSPECIFIED.,.F.,.F.,(4,3,3,3,3,3,3,3,4),(101.653706721335,101.800312674651,
102.798354955775,103.796397236899,104.794439518023,105.792481799147,106.790524080271,
107.788566361395,107.936892028514),.UNSPECIFIED.);
#853=B_SPLINE_CURVE_WITH_KNOTS('',3,(#19960,#19961,#19962,#19963,#19964,
#19965,#19966,#19967,#19968,#19969,#19970,#19971,#19972,#19973,#19974,#19975,
#19976,#19977,#19978,#19979,#19980,#19981),.UNSPECIFIED.,.F.,.F.,(4,3,3,
3,3,3,3,4),(-117.189359049681,-116.724214720551,-115.726571859691,-114.728928998832,
-113.731286137972,-112.733643277113,-111.736000416253,-110.906173742502),
 .UNSPECIFIED.);
#854=B_SPLINE_CURVE_WITH_KNOTS('',3,(#19982,#19983,#19984,#19985,#19986,
#19987,#19988,#19989,#19990,#19991,#19992,#19993,#19994,#19995,#19996,#19997,
#19998,#19999,#20000,#20001,#20002,#20003),.UNSPECIFIED.,.F.,.F.,(4,3,3,
3,3,3,3,4),(107.936892028514,108.786608642519,109.784650923643,110.782693204767,
111.780735485891,112.778777767015,113.776820048139,114.220077335694),
 .UNSPECIFIED.);
#855=B_SPLINE_CURVE_WITH_KNOTS('',3,(#20008,#20009,#20010,#20011,#20012,
#20013,#20014,#20015,#20016,#20017,#20018,#20019,#20020,#20021,#20022,#20023,
#20024,#20025,#20026,#20027,#20028,#20029),.UNSPECIFIED.,.F.,.F.,(4,3,3,
3,3,3,3,4),(-123.472544356861,-122.710071885707,-121.712429024848,-120.714786163988,
-119.717143303129,-118.719500442269,-117.72185758141,-117.189359049681),
 .UNSPECIFIED.);
#856=B_SPLINE_CURVE_WITH_KNOTS('',3,(#20030,#20031,#20032,#20033,#20034,
#20035,#20036,#20037,#20038,#20039,#20040,#20041,#20042,#20043,#20044,#20045,
#20046,#20047,#20048,#20049,#20050,#20051),.UNSPECIFIED.,.F.,.F.,(4,3,3,
3,3,3,3,4),(114.220077335694,114.774862329263,115.772904610387,116.770946891511,
117.768989172635,118.767031453759,119.765073734883,120.503262642873),
 .UNSPECIFIED.);
#857=B_SPLINE_CURVE_WITH_KNOTS('',3,(#20056,#20057,#20058,#20059,#20060,
#20061,#20062,#20063,#20064,#20065,#20066,#20067,#20068,#20069,#20070,#20071,
#20072,#20073,#20074,#20075,#20076,#20077,#20078,#20079,#20080),
 .UNSPECIFIED.,.F.,.F.,(4,3,3,3,3,3,3,3,4),(-129.75572966404,-129.693571911723,
-128.695929050863,-127.698286190004,-126.700643329145,-125.703000468285,
-124.705357607426,-123.707714746566,-123.472544356861),.UNSPECIFIED.);
#858=B_SPLINE_CURVE_WITH_KNOTS('',3,(#20081,#20082,#20083,#20084,#20085,
#20086,#20087,#20088,#20089,#20090,#20091,#20092,#20093,#20094,#20095,#20096,
#20097,#20098,#20099,#20100,#20101,#20102,#20103,#20104,#20105),
 .UNSPECIFIED.,.F.,.F.,(4,3,3,3,3,3,3,3,4),(120.503262642873,120.763116016007,
121.761158297131,122.759200578255,123.757242859379,124.755285140503,125.753327421627,
126.751369702751,126.786447950053),.UNSPECIFIED.);
#859=B_SPLINE_CURVE_WITH_KNOTS('',3,(#20110,#20111,#20112,#20113,#20114,
#20115,#20116,#20117,#20118,#20119,#20120,#20121,#20122,#20123,#20124,#20125,
#20126,#20127,#20128,#20129,#20130,#20131),.UNSPECIFIED.,.F.,.F.,(4,3,3,
3,3,3,3,4),(-136.03891497122,-135.679429076879,-134.68178621602,-133.68414335516,
-132.686500494301,-131.688857633442,-130.691214772582,-129.75572966404),
 .UNSPECIFIED.);
#860=B_SPLINE_CURVE_WITH_KNOTS('',3,(#20132,#20133,#20134,#20135,#20136,
#20137,#20138,#20139,#20140,#20141,#20142,#20143,#20144,#20145,#20146,#20147,
#20148,#20149,#20150,#20151,#20152,#20153),.UNSPECIFIED.,.F.,.F.,(4,3,3,
3,3,3,3,4),(126.786447950053,127.749411983875,128.747454265,129.745496546124,
130.743538827248,131.741581108372,132.739623389496,133.069633257233),
 .UNSPECIFIED.);
#861=B_SPLINE_CURVE_WITH_KNOTS('',3,(#20158,#20159,#20160,#20161,#20162,
#20163,#20164,#20165,#20166,#20167,#20168,#20169,#20170,#20171,#20172,#20173,
#20174,#20175,#20176,#20177,#20178,#20179),.UNSPECIFIED.,.F.,.F.,(4,3,3,
3,3,3,3,4),(-142.322100278399,-141.665286242036,-140.667643381176,-139.670000520317,
-138.672357659457,-137.674714798598,-136.677071937739,-136.03891497122),
 .UNSPECIFIED.);
#862=B_SPLINE_CURVE_WITH_KNOTS('',3,(#20180,#20181,#20182,#20183,#20184,
#20185,#20186,#20187,#20188,#20189,#20190,#20191,#20192,#20193,#20194,#20195,
#20196,#20197,#20198,#20199,#20200,#20201),.UNSPECIFIED.,.F.,.F.,(4,3,3,
3,3,3,3,4),(133.069633257233,133.73766567062,134.735707951744,135.733750232868,
136.731792513992,137.729834795116,138.72787707624,139.352818564412),
 .UNSPECIFIED.);
#863=B_SPLINE_CURVE_WITH_KNOTS('',3,(#20206,#20207,#20208,#20209,#20210,
#20211,#20212,#20213,#20214,#20215,#20216,#20217,#20218,#20219,#20220,#20221,
#20222,#20223,#20224,#20225,#20226,#20227),.UNSPECIFIED.,.F.,.F.,(4,3,3,
3,3,3,3,4),(-148.605285585579,-147.651143407192,-146.653500546333,-145.655857685473,
-144.658214824614,-143.660571963754,-142.662929102895,-142.322100278399),
 .UNSPECIFIED.);
#864=B_SPLINE_CURVE_WITH_KNOTS('',3,(#20228,#20229,#20230,#20231,#20232,
#20233,#20234,#20235,#20236,#20237,#20238,#20239,#20240,#20241,#20242,#20243,
#20244,#20245,#20246,#20247,#20248,#20249),.UNSPECIFIED.,.F.,.F.,(4,3,3,
3,3,3,3,4),(139.352818564412,139.725919357364,140.723961638488,141.722003919612,
142.720046200736,143.71808848186,144.716130762984,145.636003871592),
 .UNSPECIFIED.);
#865=B_SPLINE_CURVE_WITH_KNOTS('',3,(#20254,#20255,#20256,#20257,#20258,
#20259,#20260,#20261,#20262,#20263,#20264,#20265,#20266,#20267,#20268,#20269,
#20270,#20271,#20272,#20273,#20274,#20275,#20276,#20277,#20278),
 .UNSPECIFIED.,.F.,.F.,(4,3,3,3,3,3,3,3,4),(-154.888470892759,-154.634643433208,
-153.637000572349,-152.639357711489,-151.64171485063,-150.64407198977,-149.646429128911,
-148.648786268052,-148.605285585579),.UNSPECIFIED.);
#866=B_SPLINE_CURVE_WITH_KNOTS('',3,(#20279,#20280,#20281,#20282,#20283,
#20284,#20285,#20286,#20287,#20288,#20289,#20290,#20291,#20292,#20293,#20294,
#20295,#20296,#20297,#20298,#20299,#20300,#20301,#20302,#20303),
 .UNSPECIFIED.,.F.,.F.,(4,3,3,3,3,3,3,3,4),(145.636003871592,145.714173044108,
146.712215325232,147.710257606356,148.70829988748,149.706342168604,150.704384449728,
151.702426730852,151.919189178771),.UNSPECIFIED.);
#867=B_SPLINE_CURVE_WITH_KNOTS('',3,(#20308,#20309,#20310,#20311,#20312,
#20313,#20314,#20315,#20316,#20317,#20318,#20319,#20320,#20321,#20322,#20323,
#20324,#20325,#20326,#20327,#20328,#20329),.UNSPECIFIED.,.F.,.F.,(4,3,3,
3,3,3,3,4),(-161.171656199938,-160.620500598364,-159.622857737505,-158.625214876646,
-157.627572015786,-156.629929154927,-155.632286294067,-154.888470892759),
 .UNSPECIFIED.);
#868=B_SPLINE_CURVE_WITH_KNOTS('',3,(#20330,#20331,#20332,#20333,#20334,
#20335,#20336,#20337,#20338,#20339,#20340,#20341,#20342,#20343,#20344,#20345,
#20346,#20347,#20348,#20349,#20350,#20351),.UNSPECIFIED.,.F.,.F.,(4,3,3,
3,3,3,3,4),(151.919189178771,152.700469011976,153.6985112931,154.696553574224,
155.694595855348,156.692638136472,157.690680417596,158.202374485951),
 .UNSPECIFIED.);
#869=B_SPLINE_CURVE_WITH_KNOTS('',3,(#20356,#20357,#20358,#20359,#20360,
#20361,#20362,#20363,#20364,#20365,#20366,#20367,#20368,#20369,#20370,#20371,
#20372,#20373,#20374,#20375,#20376,#20377),.UNSPECIFIED.,.F.,.F.,(4,3,3,
3,3,3,3,4),(-167.454841507118,-166.606357763521,-165.608714902661,-164.611072041802,
-163.613429180943,-162.615786320083,-161.618143459224,-161.171656199938),
 .UNSPECIFIED.);
#870=B_SPLINE_CURVE_WITH_KNOTS('',3,(#20378,#20379,#20380,#20381,#20382,
#20383,#20384,#20385,#20386,#20387,#20388,#20389,#20390,#20391,#20392,#20393,
#20394,#20395,#20396,#20397,#20398,#20399),.UNSPECIFIED.,.F.,.F.,(4,3,3,
3,3,3,3,4),(158.202374485951,158.68872269872,159.686764979844,160.684807260968,
161.682849542092,162.680891823216,163.67893410434,164.48555979313),
 .UNSPECIFIED.);
#871=B_SPLINE_CURVE_WITH_KNOTS('',3,(#20404,#20405,#20406,#20407,#20408,
#20409,#20410,#20411,#20412,#20413,#20414,#20415,#20416,#20417,#20418,#20419,
#20420,#20421,#20422,#20423,#20424,#20425,#20426,#20427,#20428),
 .UNSPECIFIED.,.F.,.F.,(4,3,3,3,3,3,3,3,4),(-173.738026814297,-173.589857789537,
-172.592214928677,-171.594572067818,-170.596929206958,-169.599286346099,
-168.60164348524,-167.60400062438,-167.454841507118),.UNSPECIFIED.);
#872=B_SPLINE_CURVE_WITH_KNOTS('',3,(#20429,#20430,#20431,#20432,#20433,
#20434,#20435,#20436,#20437,#20438,#20439,#20440,#20441,#20442,#20443,#20444,
#20445,#20446,#20447,#20448,#20449,#20450,#20451,#20452,#20453),
 .UNSPECIFIED.,.F.,.F.,(4,3,3,3,3,3,3,3,4),(164.48555979313,164.676976385465,
165.675018666588,166.673060947713,167.671103228837,168.669145509961,169.667187791085,
170.665230072209,170.76874510031),.UNSPECIFIED.);
#873=B_SPLINE_CURVE_WITH_KNOTS('',3,(#20458,#20459,#20460,#20461,#20462,
#20463,#20464,#20465,#20466,#20467,#20468,#20469,#20470,#20471,#20472,#20473,
#20474,#20475,#20476,#20477,#20478,#20479),.UNSPECIFIED.,.F.,.F.,(4,3,3,
3,3,3,3,4),(-180.021212121477,-179.575714954693,-178.578072093834,-177.580429232974,
-176.582786372115,-175.585143511255,-174.587500650396,-173.738026814297),
 .UNSPECIFIED.);
#874=B_SPLINE_CURVE_WITH_KNOTS('',3,(#20480,#20481,#20482,#20483,#20484,
#20485,#20486,#20487,#20488,#20489,#20490,#20491,#20492,#20493,#20494,#20495,
#20496,#20497,#20498,#20499,#20500,#20501),.UNSPECIFIED.,.F.,.F.,(4,3,3,
3,3,3,3,4),(170.76874510031,171.663272353333,172.661314634457,173.659356915581,
174.657399196705,175.655441477829,176.653483758953,177.051930407489),
 .UNSPECIFIED.);
#875=B_SPLINE_CURVE_WITH_KNOTS('',3,(#20506,#20507,#20508,#20509,#20510,
#20511,#20512,#20513,#20514,#20515,#20516,#20517,#20518,#20519,#20520,#20521,
#20522,#20523,#20524,#20525,#20526,#20527),.UNSPECIFIED.,.F.,.F.,(4,3,3,
3,3,3,3,4),(-186.304397428656,-185.56157211985,-184.56392925899,-183.566286398131,
-182.568643537271,-181.571000676412,-180.573357815553,-180.021212121477),
 .UNSPECIFIED.);
#876=B_SPLINE_CURVE_WITH_KNOTS('',3,(#20528,#20529,#20530,#20531,#20532,
#20533,#20534,#20535,#20536,#20537,#20538,#20539,#20540,#20541,#20542,#20543,
#20544,#20545,#20546,#20547,#20548,#20549),.UNSPECIFIED.,.F.,.F.,(4,3,3,
3,3,3,3,4),(177.051930407489,177.651526040077,178.649568321201,179.647610602325,
180.645652883449,181.643695164573,182.641737445697,183.335115714669),
 .UNSPECIFIED.);
#877=B_SPLINE_CURVE_WITH_KNOTS('',3,(#20555,#20556,#20557,#20558,#20559,
#20560,#20561,#20562,#20563,#20564),.UNSPECIFIED.,.F.,.F.,(4,1,1,1,1,1,
1,4),(197.920337176157,198.17515472821,199.172797589069,200.170440449928,
201.168083310788,202.165726171647,203.163369032507,204.161011893366),
 .UNSPECIFIED.);
#878=B_SPLINE_CURVE_WITH_KNOTS('',3,(#20567,#20568,#20569,#20570,#20571,
#20572,#20573,#20574,#20575),.UNSPECIFIED.,.F.,.F.,(4,1,1,1,1,1,4),(197.920337176157,
197.930069567874,198.928111848998,199.926154130122,200.924196411246,201.92223869237,
202.920280973494),.UNSPECIFIED.);
#879=B_SPLINE_CURVE_WITH_KNOTS('',3,(#20580,#20581,#20582,#20583,#20584,
#20585,#20586,#20587,#20588,#20589),.UNSPECIFIED.,.F.,.F.,(4,1,1,1,1,1,
1,4),(191.637151868977,192.189297563053,193.186940423913,194.184583284772,
195.182226145631,196.179869006491,197.17751186735,197.920337176157),
 .UNSPECIFIED.);
#880=B_SPLINE_CURVE_WITH_KNOTS('',3,(#20590,#20591,#20592,#20593,#20594,
#20595,#20596,#20597,#20598,#20599),.UNSPECIFIED.,.F.,.F.,(4,1,1,1,1,1,
1,4),(191.637151868977,191.94181588113,192.939858162254,193.937900443378,
194.935942724502,195.933985005626,196.93202728675,197.920337176157),
 .UNSPECIFIED.);
#881=B_SPLINE_CURVE_WITH_KNOTS('',3,(#20604,#20605,#20606,#20607,#20608,
#20609,#20610,#20611,#20612,#20613),.UNSPECIFIED.,.F.,.F.,(4,1,1,1,1,1,
1,4),(185.353966561798,186.203440397897,187.201083258756,188.198726119616,
189.196368980475,190.194011841334,191.191654702194,191.637151868977),
 .UNSPECIFIED.);
#882=B_SPLINE_CURVE_WITH_KNOTS('',3,(#20614,#20615,#20616,#20617,#20618,
#20619,#20620,#20621,#20622,#20623),.UNSPECIFIED.,.F.,.F.,(4,1,1,1,1,1,
1,4),(185.353966561798,185.953562194385,186.951604475509,187.949646756633,
188.947689037757,189.945731318881,190.943773600006,191.637151868977),
 .UNSPECIFIED.);
#883=B_SPLINE_CURVE_WITH_KNOTS('',3,(#20628,#20629,#20630,#20631,#20632,
#20633,#20634,#20635,#20636,#20637,#20638),.UNSPECIFIED.,.F.,.F.,(4,1,1,
1,1,1,1,1,4),(179.070781254618,179.219940371881,180.21758323274,181.2152260936,
182.212868954459,183.210511815318,184.208154676178,185.205797537037,185.353966561798),
 .UNSPECIFIED.);
#884=B_SPLINE_CURVE_WITH_KNOTS('',3,(#20639,#20640,#20641,#20642,#20643,
#20644,#20645,#20646,#20647,#20648),.UNSPECIFIED.,.F.,.F.,(4,1,1,1,1,1,
1,4),(179.070781254618,179.965308507641,180.963350788765,181.961393069889,
182.959435351013,183.957477632137,184.955519913261,185.353966561798),
 .UNSPECIFIED.);
#885=B_SPLINE_CURVE_WITH_KNOTS('',3,(#20653,#20654,#20655,#20656,#20657,
#20658,#20659,#20660,#20661,#20662),.UNSPECIFIED.,.F.,.F.,(4,1,1,1,1,1,
1,4),(172.787595947439,173.234083206724,174.231726067584,175.229368928443,
176.227011789303,177.224654650162,178.222297511021,179.070781254618),
 .UNSPECIFIED.);
#886=B_SPLINE_CURVE_WITH_KNOTS('',3,(#20663,#20664,#20665,#20666,#20667,
#20668,#20669,#20670,#20671,#20672,#20673),.UNSPECIFIED.,.F.,.F.,(4,1,1,
1,1,1,1,1,4),(172.787595947439,172.979012539773,173.977054820897,174.975097102021,
175.973139383145,176.971181664269,177.969223945393,178.967266226517,179.070781254618),
 .UNSPECIFIED.);
#887=B_SPLINE_CURVE_WITH_KNOTS('',3,(#20678,#20679,#20680,#20681,#20682,
#20683,#20684,#20685,#20686,#20687),.UNSPECIFIED.,.F.,.F.,(4,1,1,1,1,1,
1,4),(166.504410640259,167.248226041568,168.245868902427,169.243511763287,
170.241154624146,171.238797485006,172.236440345865,172.787595947439),
 .UNSPECIFIED.);
#888=B_SPLINE_CURVE_WITH_KNOTS('',3,(#20688,#20689,#20690,#20691,#20692,
#20693,#20694,#20695,#20696,#20697),.UNSPECIFIED.,.F.,.F.,(4,1,1,1,1,1,
1,4),(166.504410640259,166.990758853029,167.988801134153,168.986843415277,
169.984885696401,170.982927977525,171.980970258649,172.787595947439),
 .UNSPECIFIED.);
#889=B_SPLINE_CURVE_WITH_KNOTS('',3,(#20702,#20703,#20704,#20705,#20706,
#20707,#20708,#20709,#20710,#20711,#20712),.UNSPECIFIED.,.F.,.F.,(4,1,1,
1,1,1,1,1,4),(160.22122533308,160.264726015552,161.262368876412,162.260011737271,
163.25765459813,164.25529745899,165.252940319849,166.250583180709,166.504410640259),
 .UNSPECIFIED.);
#890=B_SPLINE_CURVE_WITH_KNOTS('',3,(#20713,#20714,#20715,#20716,#20717,
#20718,#20719,#20720,#20721,#20722),.UNSPECIFIED.,.F.,.F.,(4,1,1,1,1,1,
1,4),(160.22122533308,161.002505166285,162.000547447409,162.998589728533,
163.996632009657,164.994674290781,165.992716571905,166.504410640259),
 .UNSPECIFIED.);
#891=B_SPLINE_CURVE_WITH_KNOTS('',3,(#20727,#20728,#20729,#20730,#20731,
#20732,#20733,#20734,#20735,#20736),.UNSPECIFIED.,.F.,.F.,(4,1,1,1,1,1,
1,4),(153.9380400259,154.278868850396,155.276511711255,156.274154572115,
157.271797432974,158.269440293833,159.267083154693,160.22122533308),
 .UNSPECIFIED.);
#892=B_SPLINE_CURVE_WITH_KNOTS('',3,(#20737,#20738,#20739,#20740,#20741,
#20742,#20743,#20744,#20745,#20746,#20747),.UNSPECIFIED.,.F.,.F.,(4,1,1,
1,1,1,1,1,4),(153.9380400259,154.016209198417,155.014251479541,156.012293760665,
157.010336041789,158.008378322913,159.006420604037,160.004462885161,160.22122533308),
 .UNSPECIFIED.);
#893=B_SPLINE_CURVE_WITH_KNOTS('',3,(#20752,#20753,#20754,#20755,#20756,
#20757,#20758,#20759,#20760,#20761),.UNSPECIFIED.,.F.,.F.,(4,1,1,1,1,1,
1,4),(147.65485471872,148.293011685239,149.290654546099,150.288297406958,
151.285940267817,152.283583128677,153.281225989536,153.9380400259),
 .UNSPECIFIED.);
#894=B_SPLINE_CURVE_WITH_KNOTS('',3,(#20762,#20763,#20764,#20765,#20766,
#20767,#20768,#20769,#20770,#20771),.UNSPECIFIED.,.F.,.F.,(4,1,1,1,1,1,
1,4),(147.65485471872,148.027955511672,149.025997792796,150.02404007392,
151.022082355044,152.020124636168,153.018166917292,153.9380400259),
 .UNSPECIFIED.);
#895=B_SPLINE_CURVE_WITH_KNOTS('',3,(#20776,#20777,#20778,#20779,#20780,
#20781,#20782,#20783,#20784,#20785),.UNSPECIFIED.,.F.,.F.,(4,1,1,1,1,1,
1,4),(141.371669411541,142.307154520083,143.304797380942,144.302440241802,
145.300083102661,146.29772596352,147.29536882438,147.65485471872),
 .UNSPECIFIED.);
#896=B_SPLINE_CURVE_WITH_KNOTS('',3,(#20786,#20787,#20788,#20789,#20790,
#20791,#20792,#20793,#20794,#20795),.UNSPECIFIED.,.F.,.F.,(4,1,1,1,1,1,
1,4),(141.371669411541,142.039701824928,143.037744106052,144.035786387176,
145.0338286683,146.031870949424,147.029913230548,147.65485471872),
 .UNSPECIFIED.);
#897=B_SPLINE_CURVE_WITH_KNOTS('',3,(#20800,#20801,#20802,#20803,#20804,
#20805,#20806,#20807,#20808,#20809,#20810),.UNSPECIFIED.,.F.,.F.,(4,1,1,
1,1,1,1,1,4),(135.088484104361,135.323654494067,136.321297354926,137.318940215786,
138.316583076645,139.314225937505,140.311868798364,141.309511659223,141.371669411541),
 .UNSPECIFIED.);
#898=B_SPLINE_CURVE_WITH_KNOTS('',3,(#20811,#20812,#20813,#20814,#20815,
#20816,#20817,#20818,#20819,#20820),.UNSPECIFIED.,.F.,.F.,(4,1,1,1,1,1,
1,4),(135.088484104361,136.051448138184,137.049490419308,138.047532700432,
139.045574981556,140.04361726268,141.041659543804,141.371669411541),
 .UNSPECIFIED.);
#899=B_SPLINE_CURVE_WITH_KNOTS('',3,(#20825,#20826,#20827,#20828,#20829,
#20830,#20831,#20832,#20833,#20834),.UNSPECIFIED.,.F.,.F.,(4,1,1,1,1,1,
1,4),(128.805298797182,129.337797328911,130.33544018977,131.333083050629,
132.330725911489,133.328368772348,134.326011633208,135.088484104361),
 .UNSPECIFIED.);
#900=B_SPLINE_CURVE_WITH_KNOTS('',3,(#20835,#20836,#20837,#20838,#20839,
#20840,#20841,#20842,#20843,#20844,#20845),.UNSPECIFIED.,.F.,.F.,(4,1,1,
1,1,1,1,1,4),(128.805298797182,129.065152170316,130.06319445144,131.061236732564,
132.059279013688,133.057321294812,134.055363575936,135.05340585706,135.088484104361),
 .UNSPECIFIED.);
#901=B_SPLINE_CURVE_WITH_KNOTS('',3,(#20850,#20851,#20852,#20853,#20854,
#20855,#20856,#20857,#20858,#20859),.UNSPECIFIED.,.F.,.F.,(4,1,1,1,1,1,
1,4),(122.522113490002,123.351940163754,124.349583024614,125.347225885473,
126.344868746332,127.342511607192,128.340154468051,128.805298797182),
 .UNSPECIFIED.);
#902=B_SPLINE_CURVE_WITH_KNOTS('',3,(#20860,#20861,#20862,#20863,#20864,
#20865,#20866,#20867,#20868,#20869),.UNSPECIFIED.,.F.,.F.,(4,1,1,1,1,1,
1,4),(122.522113490002,123.076898483572,124.074940764696,125.07298304582,
126.071025326944,127.069067608068,128.067109889192,128.805298797182),
 .UNSPECIFIED.);
#903=B_SPLINE_CURVE_WITH_KNOTS('',3,(#20874,#20875,#20876,#20877,#20878,
#20879,#20880,#20881,#20882,#20883,#20884),.UNSPECIFIED.,.F.,.F.,(4,1,1,
1,1,1,1,1,4),(116.238928182823,116.368440137738,117.366082998598,118.363725859457,
119.361368720316,120.359011581176,121.356654442035,122.354297302895,122.522113490002),
 .UNSPECIFIED.);
#904=B_SPLINE_CURVE_WITH_KNOTS('',3,(#20885,#20886,#20887,#20888,#20889,
#20890,#20891,#20892,#20893,#20894),.UNSPECIFIED.,.F.,.F.,(4,1,1,1,1,1,
1,4),(116.238928182823,117.088644796828,118.086687077952,119.084729359076,
120.0827716402,121.080813921324,122.078856202448,122.522113490002),
 .UNSPECIFIED.);
#905=B_SPLINE_CURVE_WITH_KNOTS('',3,(#20899,#20900,#20901,#20902,#20903,
#20904,#20905,#20906,#20907,#20908),.UNSPECIFIED.,.F.,.F.,(4,1,1,1,1,1,
1,4),(109.955742875643,110.382582972582,111.380225833441,112.377868694301,
113.37551155516,114.373154416019,115.370797276879,116.238928182823),
 .UNSPECIFIED.);
#906=B_SPLINE_CURVE_WITH_KNOTS('',3,(#20909,#20910,#20911,#20912,#20913,
#20914,#20915,#20916,#20917,#20918,#20919),.UNSPECIFIED.,.F.,.F.,(4,1,1,
1,1,1,1,1,4),(109.955742875643,110.102348828959,111.100391110083,112.098433391207,
113.096475672331,114.094517953455,115.092560234579,116.090602515703,116.238928182823),
 .UNSPECIFIED.);
#907=B_SPLINE_CURVE_WITH_KNOTS('',3,(#20924,#20925,#20926,#20927,#20928,
#20929,#20930,#20931,#20932,#20933),.UNSPECIFIED.,.F.,.F.,(4,1,1,1,1,1,
1,4),(103.672557568463,104.396725807425,105.394368668285,106.392011529144,
107.389654390004,108.387297250863,109.384940111722,109.955742875643),
 .UNSPECIFIED.);
#908=B_SPLINE_CURVE_WITH_KNOTS('',3,(#20934,#20935,#20936,#20937,#20938,
#20939,#20940,#20941,#20942,#20943),.UNSPECIFIED.,.F.,.F.,(4,1,1,1,1,1,
1,4),(103.672557568463,104.114095142215,105.112137423339,106.110179704463,
107.108221985587,108.106264266711,109.104306547835,109.955742875643),
 .UNSPECIFIED.);
#909=B_SPLINE_CURVE_WITH_KNOTS('',3,(#20948,#20949,#20950,#20951,#20952,
#20953,#20954,#20955,#20956,#20957,#20958),.UNSPECIFIED.,.F.,.F.,(4,1,1,
1,1,1,1,1,4),(97.3893722612837,97.4132257814096,98.410868642269,99.4085115031284,
100.406154363988,101.403797224847,102.401440085707,103.399082946566,103.672557568463),
 .UNSPECIFIED.);
#910=B_SPLINE_CURVE_WITH_KNOTS('',3,(#20959,#20960,#20961,#20962,#20963,
#20964,#20965,#20966,#20967,#20968),.UNSPECIFIED.,.F.,.F.,(4,1,1,1,1,1,
1,4),(97.3893722612838,98.125841455471,99.123883736595,100.121926017719,
101.119968298843,102.118010579967,103.116052861091,103.672557568463),
 .UNSPECIFIED.);
#911=B_SPLINE_CURVE_WITH_KNOTS('',3,(#20973,#20974,#20975,#20976,#20977,
#20978,#20979,#20980,#20981,#20982),.UNSPECIFIED.,.F.,.F.,(4,1,1,1,1,1,
1,4),(91.1061869541041,91.4273686162531,92.4250114771125,93.4226543379719,
94.4202971988313,95.4179400596907,96.4155829205502,97.3893722612837),
 .UNSPECIFIED.);
#912=B_SPLINE_CURVE_WITH_KNOTS('',3,(#20983,#20984,#20985,#20986,#20987,
#20988,#20989,#20990,#20991,#20992,#20993),.UNSPECIFIED.,.F.,.F.,(4,1,1,
1,1,1,1,1,4),(91.1061869541042,91.1395454876028,92.1375877687268,93.1356300498508,
94.1336723309749,95.1317146120989,96.1297568932229,97.127799174347,97.3893722612838),
 .UNSPECIFIED.);
#913=B_SPLINE_CURVE_WITH_KNOTS('',3,(#20998,#20999,#21000,#21001,#21002,
#21003,#21004,#21005,#21006,#21007),.UNSPECIFIED.,.F.,.F.,(4,1,1,1,1,1,
1,4),(84.8230016469245,85.4415114510967,86.4391543119561,87.4367971728155,
88.4344400336749,89.4320828945343,90.4297257553937,91.1061869541041),
 .UNSPECIFIED.);
#914=B_SPLINE_CURVE_WITH_KNOTS('',3,(#21008,#21009,#21010,#21011,#21012,
#21013,#21014,#21015,#21016,#21017),.UNSPECIFIED.,.F.,.F.,(4,1,1,1,1,1,
1,4),(84.8230016469246,85.1512918008586,86.1493340819827,87.1473763631067,
88.1454186442307,89.1434609253548,90.1415032064788,91.1061869541042),
 .UNSPECIFIED.);
#915=B_SPLINE_CURVE_WITH_KNOTS('',3,(#21022,#21023,#21024,#21025,#21026,
#21027,#21028,#21029,#21030,#21031),.UNSPECIFIED.,.F.,.F.,(4,1,1,1,1,1,
1,4),(78.539816339745,79.4556542859402,80.4532971467996,81.4509400076591,
82.4485828685185,83.4462257293779,84.4438685902373,84.8230016469245),
 .UNSPECIFIED.);
#916=B_SPLINE_CURVE_WITH_KNOTS('',3,(#21032,#21033,#21034,#21035,#21036,
#21037,#21038,#21039,#21040,#21041),.UNSPECIFIED.,.F.,.F.,(4,1,1,1,1,1,
1,4),(78.539816339745,79.1630381141145,80.1610803952385,81.1591226763625,
82.1571649574865,83.1552072386106,84.1532495197346,84.8230016469246),
 .UNSPECIFIED.);
#917=B_SPLINE_CURVE_WITH_KNOTS('',3,(#21046,#21047,#21048,#21049,#21050,
#21051,#21052,#21053,#21054,#21055,#21056),.UNSPECIFIED.,.F.,.F.,(4,1,1,
1,1,1,1,1,4),(72.2566310325654,72.4721542599244,73.4697971207838,74.4674399816432,
75.4650828425026,76.462725703362,77.4603685642214,78.4580114250808,78.539816339745),
 .UNSPECIFIED.);
#918=B_SPLINE_CURVE_WITH_KNOTS('',3,(#21057,#21058,#21059,#21060,#21061,
#21062,#21063,#21064,#21065,#21066),.UNSPECIFIED.,.F.,.F.,(4,1,1,1,1,1,
1,4),(72.2566310325654,73.1747844273703,74.1728267084943,75.1708689896184,
76.1689112707424,77.1669535518664,78.1649958329905,78.539816339745),
 .UNSPECIFIED.);
#919=B_SPLINE_CURVE_WITH_KNOTS('',3,(#21071,#21072,#21073,#21074,#21075,
#21076,#21077,#21078,#21079,#21080),.UNSPECIFIED.,.F.,.F.,(4,1,1,1,1,1,
1,4),(65.9734457253858,66.486297094768,67.4839399556274,68.4815828164868,
69.4792256773462,70.4768685382056,71.474511399065,72.2566310325654),
 .UNSPECIFIED.);
#920=B_SPLINE_CURVE_WITH_KNOTS('',3,(#21081,#21082,#21083,#21084,#21085,
#21086,#21087,#21088,#21089,#21090,#21091),.UNSPECIFIED.,.F.,.F.,(4,1,1,
1,1,1,1,1,4),(65.9734457253858,66.1884884595021,67.1865307406262,68.1845730217502,
69.1826153028742,70.1806575839982,71.1786998651223,72.1767421462463,72.2566310325654),
 .UNSPECIFIED.);
#921=B_SPLINE_CURVE_WITH_KNOTS('',3,(#21096,#21097,#21098,#21099,#21100,
#21101,#21102,#21103,#21104,#21105),.UNSPECIFIED.,.F.,.F.,(4,1,1,1,1,1,
1,4),(59.6902604182062,60.5004399296115,61.4980827904709,62.4957256513303,
63.4933685121897,64.4910113730492,65.4886542339086,65.9734457253858),
 .UNSPECIFIED.);
#922=B_SPLINE_CURVE_WITH_KNOTS('',3,(#21106,#21107,#21108,#21109,#21110,
#21111,#21112,#21113,#21114,#21115),.UNSPECIFIED.,.F.,.F.,(4,1,1,1,1,1,
1,4),(59.6902604182062,60.200234772758,61.198277053882,62.196319335006,
63.19436161613,64.1924038972541,65.1904461783781,65.9734457253858),
 .UNSPECIFIED.);
#923=B_SPLINE_CURVE_WITH_KNOTS('',3,(#21120,#21121,#21122,#21123,#21124,
#21125,#21126,#21127,#21128,#21129,#21130),.UNSPECIFIED.,.F.,.F.,(4,1,1,
1,1,1,1,1,4),(53.4070751110266,53.5169399035957,54.5145827644551,55.5122256253145,
56.5098684861739,57.5075113470333,58.5051542078927,59.5027970687521,59.6902604182062),
 .UNSPECIFIED.);
#924=B_SPLINE_CURVE_WITH_KNOTS('',3,(#21131,#21132,#21133,#21134,#21135,
#21136,#21137,#21138,#21139,#21140),.UNSPECIFIED.,.F.,.F.,(4,1,1,1,1,1,
1,4),(53.4070751110266,54.2119810860138,55.2100233671378,56.2080656482619,
57.2061079293859,58.2041502105099,59.2021924916339,59.6902604182062),
 .UNSPECIFIED.);
#925=B_SPLINE_CURVE_WITH_KNOTS('',3,(#21145,#21146,#21147,#21148,#21149,
#21150,#21151,#21152,#21153,#21154),.UNSPECIFIED.,.F.,.F.,(4,1,1,1,1,1,
1,4),(47.123889803847,47.5310827384393,48.5287255992987,49.5263684601581,
50.5240113210175,51.5216541818769,52.5192970427363,53.4070751110266),
 .UNSPECIFIED.);
#926=B_SPLINE_CURVE_WITH_KNOTS('',3,(#21155,#21156,#21157,#21158,#21159,
#21160,#21161,#21162,#21163,#21164,#21165),.UNSPECIFIED.,.F.,.F.,(4,1,1,
1,1,1,1,1,4),(47.123889803847,47.2256851181456,48.2237273992696,49.2217696803937,
50.2198119615177,51.2178542426417,52.2158965237657,53.2139388048898,53.4070751110266),
 .UNSPECIFIED.);
#927=B_SPLINE_CURVE_WITH_KNOTS('',3,(#21170,#21171,#21172,#21173,#21174,
#21175,#21176,#21177,#21178,#21179),.UNSPECIFIED.,.F.,.F.,(4,1,1,1,1,1,
1,4),(40.8407044966674,41.5452255732828,42.5428684341422,43.5405112950016,
44.538154155861,45.5357970167204,46.5334398775799,47.123889803847),
 .UNSPECIFIED.);
#928=B_SPLINE_CURVE_WITH_KNOTS('',3,(#21180,#21181,#21182,#21183,#21184,
#21185,#21186,#21187,#21188,#21189),.UNSPECIFIED.,.F.,.F.,(4,1,1,1,1,1,
1,4),(40.8407044966675,41.2374314314014,42.2354737125255,43.2335159936495,
44.2315582747735,45.2296005558975,46.2276428370216,47.123889803847),
 .UNSPECIFIED.);
#929=B_SPLINE_CURVE_WITH_KNOTS('',3,(#21194,#21195,#21196,#21197,#21198,
#21199,#21200,#21201,#21202,#21203,#21204),.UNSPECIFIED.,.F.,.F.,(4,1,1,
1,1,1,1,1,4),(34.5575191894878,34.561725547267,35.5593684081264,36.5570112689858,
37.5546541298452,38.5522969907046,39.549939851564,40.5475827124234,40.8407044966674),
 .UNSPECIFIED.);
#930=B_SPLINE_CURVE_WITH_KNOTS('',3,(#21205,#21206,#21207,#21208,#21209,
#21210,#21211,#21212,#21213,#21214),.UNSPECIFIED.,.F.,.F.,(4,1,1,1,1,1,
1,4),(34.5575191894879,35.2491777446573,36.2472200257813,37.2452623069053,
38.2433045880294,39.2413468691534,40.2393891502774,40.8407044966675),
 .UNSPECIFIED.);
#931=B_SPLINE_CURVE_WITH_KNOTS('',3,(#21219,#21220,#21221,#21222,#21223,
#21224,#21225,#21226,#21227,#21228),.UNSPECIFIED.,.F.,.F.,(4,1,1,1,1,1,
1,4),(28.2743338823082,28.5758683821105,29.5735112429699,30.5711541038294,
31.5687969646888,32.5664398255482,33.5640826864076,34.5575191894878),
 .UNSPECIFIED.);
#932=B_SPLINE_CURVE_WITH_KNOTS('',3,(#21229,#21230,#21231,#21232,#21233,
#21234,#21235,#21236,#21237,#21238),.UNSPECIFIED.,.F.,.F.,(4,1,1,1,1,1,
1,4),(28.2743338823083,29.2609240579131,30.2589663390371,31.2570086201612,
32.2550509012852,33.2530931824092,34.2511354635333,34.5575191894879),
 .UNSPECIFIED.);
#933=B_SPLINE_CURVE_WITH_KNOTS('',3,(#21243,#21244,#21245,#21246,#21247,
#21248,#21249,#21250,#21251,#21252),.UNSPECIFIED.,.F.,.F.,(4,1,1,1,1,1,
1,4),(21.9911485751286,22.5900112169541,23.5876540778135,24.5852969386729,
25.5829397995323,26.5805826603917,27.5782255212511,28.2743338823082),
 .UNSPECIFIED.);
#934=B_SPLINE_CURVE_WITH_KNOTS('',3,(#21253,#21254,#21255,#21256,#21257,
#21258,#21259,#21260,#21261,#21262,#21263),.UNSPECIFIED.,.F.,.F.,(4,1,1,
1,1,1,1,1,4),(21.9911485751287,22.2746280900449,23.272670371169,24.270712652293,
25.268754933417,26.266797214541,27.2648394956651,28.2628817767891,28.2743338823083),
 .UNSPECIFIED.);
#935=B_SPLINE_CURVE_WITH_KNOTS('',3,(#21268,#21269,#21270,#21271,#21272,
#21273,#21274,#21275,#21276,#21277),.UNSPECIFIED.,.F.,.F.,(4,1,1,1,1,1,
1,4),(15.707963267949,16.6041540517977,17.6017969126571,18.5994397735165,
19.5970826343759,20.5947254952353,21.5923683560947,21.9911485751286),
 .UNSPECIFIED.);
#936=B_SPLINE_CURVE_WITH_KNOTS('',3,(#21278,#21279,#21280,#21281,#21282,
#21283,#21284,#21285,#21286,#21287),.UNSPECIFIED.,.F.,.F.,(4,1,1,1,1,1,
1,4),(15.7079632679491,16.2863744033008,17.2844166844248,18.2824589655488,
19.2805012466728,20.2785435277969,21.2765858089209,21.9911485751287),
 .UNSPECIFIED.);
#937=B_SPLINE_CURVE_WITH_KNOTS('',3,(#21290,#21291,#21292,#21293,#21294,
#21295,#21296,#21297,#21298,#21299,#21300,#21301,#21302,#21303,#21304,#21305,
#21306,#21307,#21308,#21309,#21310,#21311,#21312,#21313,#21314,#21315,#21316,
#21317,#21318,#21319,#21320,#21321,#21322,#21323,#21324,#21325,#21326,#21327,
#21328,#21329,#21330,#21331,#21332,#21333,#21334,#21335,#21336,#21337,#21338,
#21339,#21340,#21341,#21342,#21343,#21344,#21345,#21346,#21347,#21348,#21349,
#21350,#21351,#21352,#21353,#21354,#21355,#21356,#21357,#21358,#21359,#21360,
#21361,#21362,#21363,#21364,#21365,#21366,#21367,#21368,#21369,#21370,#21371,
#21372,#21373,#21374,#21375,#21376,#21377,#21378,#21379,#21380,#21381,#21382,
#21383,#21384,#21385,#21386,#21387,#21388,#21389,#21390,#21391,#21392,#21393,
#21394,#21395,#21396,#21397,#21398,#21399,#21400,#21401,#21402,#21403,#21404,
#21405,#21406,#21407,#21408,#21409,#21410),.UNSPECIFIED.,.F.,.F.,(4,3,3,
3,3,3,3,3,3,3,3,3,3,3,3,3,3,3,3,3,3,3,3,3,3,3,3,3,3,3,3,3,3,3,3,3,3,3,3,
3,4),(-0.753008129282056,-0.726412283548368,-0.715911613874471,-0.694893371653716,
-0.683361029549332,-0.673826434412814,-0.652889016486892,-0.639679181765185,
-0.63195159856097,-0.60480408471638,-0.59150990338668,-0.582561183693184,
-0.554067746128576,-0.540494882749548,-0.528208608719221,-0.505843484121927,
-0.4921308028701,-0.483102814228457,-0.456032674248847,-0.436199115577779,
-0.427073928162626,-0.400948091236321,-0.382860905241332,-0.374822254310016,
-0.34584221065474,-0.333939649620793,-0.324058619604945,-0.29393738163796,
-0.278576588250954,-0.269234263278142,-0.238815915606663,-0.225742435796944,
-0.216239773488962,-0.18666367230127,-0.170750005528772,-0.161294486761502,
-0.129614927749849,-0.114924930935507,-0.106250072717365,-0.0979353687381955,
-0.0965360155478562),.UNSPECIFIED.);
#938=B_SPLINE_CURVE_WITH_KNOTS('',3,(#21412,#21413,#21414,#21415,#21416,
#21417,#21418,#21419,#21420,#21421,#21422,#21423,#21424,#21425,#21426,#21427,
#21428,#21429,#21430,#21431,#21432,#21433,#21434,#21435,#21436,#21437,#21438,
#21439,#21440,#21441,#21442,#21443,#21444,#21445,#21446,#21447,#21448),
 .UNSPECIFIED.,.F.,.F.,(4,3,3,3,3,3,3,3,3,3,3,3,4),(-0.204609524178132,
-0.173922074105667,-0.152149392827302,-0.142793959810126,-0.12983323009626,
-0.11308637627832,-0.0998536142809363,-0.090547498816978,-0.0679106241127335,
-0.0514558350659385,-0.042025593252969,-0.0155529233063705,0.),
 .UNSPECIFIED.);
#939=B_SPLINE_CURVE_WITH_KNOTS('',3,(#21451,#21452,#21453,#21454,#21455,
#21456,#21457,#21458,#21459,#21460,#21461,#21462,#21463,#21464,#21465,#21466),
 .UNSPECIFIED.,.F.,.F.,(4,3,3,3,3,4),(-0.0965360155478562,-0.0724020116608921,
-0.0590232605257019,-0.050388474335024,-0.0186937936910934,0.),
 .UNSPECIFIED.);
#940=B_SPLINE_CURVE_WITH_KNOTS('',3,(#22255,#22256,#22257,#22258,#22259,
#22260,#22261,#22262),.UNSPECIFIED.,.F.,.F.,(4,1,1,1,1,4),(11.6159397475006,
12.61358260836,13.6112254692194,14.6088683300789,15.6065111909383,15.707963267949),
 .UNSPECIFIED.);
#941=B_SPLINE_CURVE_WITH_KNOTS('',3,(#22263,#22264,#22265,#22266,#22267,
#22268,#22269,#22270,#22271,#22272,#22273,#22274,#22275,#22276,#22277,#22278,
#22279,#22280,#22281,#22282,#22283,#22284,#22285,#22286,#22287,#22288,#22289,
#22290,#22291,#22292,#22293,#22294,#22295,#22296,#22297,#22298,#22299,#22300,
#22301,#22302,#22303,#22304,#22305,#22306,#22307,#22308,#22309,#22310,#22311),
 .UNSPECIFIED.,.F.,.F.,(4,3,3,3,3,3,3,3,3,3,3,3,3,3,3,3,4),(-0.275362278356892,
-0.263988733943187,-0.242277787653762,-0.228409792083558,-0.208856161945484,
-0.197709057767663,-0.168075464588018,-0.150222803571495,-0.140083955862437,
-0.125365894046572,-0.0997819296507484,-0.0889593225835958,-0.0667194919376969,
-0.0511923416312717,-0.0404361839568205,-0.0141940669149386,0.),
 .UNSPECIFIED.);
#942=B_SPLINE_CURVE_WITH_KNOTS('',3,(#22312,#22313,#22314,#22315,#22316,
#22317,#22318,#22319,#22320,#22321,#22322,#22323,#22324,#22325,#22326,#22327,
#22328,#22329,#22330),.UNSPECIFIED.,.F.,.F.,(4,3,3,3,3,3,4),(-191.027404416132,
-190.549786424147,-189.552143563287,-188.554500702428,-187.556857841568,
-186.559214980709,-186.304397428656),.UNSPECIFIED.);
#943=B_SPLINE_CURVE_WITH_KNOTS('',3,(#22333,#22334,#22335,#22336,#22337,
#22338,#22339,#22340,#22341),.UNSPECIFIED.,.F.,.F.,(4,1,1,1,1,1,4),(10.3752088276283,
11.2961629976806,12.2942052788047,13.2922475599287,14.2902898410527,15.2883321221767,
15.7079632679491),.UNSPECIFIED.);
#944=B_SPLINE_CURVE_WITH_KNOTS('',3,(#23135,#23136,#23137,#23138,#23139,
#23140,#23141,#23142,#23143,#23144,#23145,#23146,#23147,#23148,#23149,#23150,
#23151,#23152,#23153,#23154,#23155,#23156),.UNSPECIFIED.,.F.,.F.,(4,3,3,
3,3,3,3,4),(183.335115714669,183.639779726821,184.637822007945,185.635864289069,
186.633906570193,187.631948851317,188.629991132441,188.954231742812),
 .UNSPECIFIED.);
#945=B_SPLINE_CURVE_WITH_KNOTS('',3,(#23157,#23158,#23159,#23160,#23161,
#23162,#23163,#23164,#23165,#23166,#23167,#23168,#23169,#23170,#23171,#23172,
#23173,#23174,#23175,#23176,#23177,#23178,#23179,#23180,#23181,#23182,#23183,
#23184,#23185,#23186,#23187,#23188,#23189,#23190,#23191,#23192,#23193,#23194,
#23195,#23196,#23197,#23198,#23199,#23200,#23201,#23202,#23203,#23204,#23205,
#23206,#23207,#23208),.UNSPECIFIED.,.F.,.F.,(4,3,3,3,3,3,3,3,3,3,3,3,3,
3,3,3,3,4),(-0.276631791712714,-0.267404104599176,-0.245529112929484,-0.233826742508505,
-0.212230201958684,-0.201819484750363,-0.173281546649687,-0.162756755581661,
-0.152537502224722,-0.140478169692516,-0.120739781640826,-0.110641775261762,
-0.100726383882944,-0.0755447879122082,-0.0587891884452614,-0.0493012364577666,
-0.0182848522583483,0.),.UNSPECIFIED.);
#1278=PLANE('',#10556);
#1279=PLANE('',#10557);
#1280=PLANE('',#10558);
#1281=PLANE('',#10559);
#1282=PLANE('',#10560);
#1283=PLANE('',#10561);
#1284=PLANE('',#10562);
#1285=PLANE('',#10563);
#1286=PLANE('',#10567);
#1287=PLANE('',#10568);
#1725=FACE_OUTER_BOUND('',#2327,.T.);
#1726=FACE_OUTER_BOUND('',#2328,.T.);
#1727=FACE_OUTER_BOUND('',#2329,.T.);
#1728=FACE_OUTER_BOUND('',#2330,.T.);
#1729=FACE_OUTER_BOUND('',#2331,.T.);
#1730=FACE_OUTER_BOUND('',#2332,.T.);
#1731=FACE_OUTER_BOUND('',#2333,.T.);
#1732=FACE_OUTER_BOUND('',#2334,.T.);
#1733=FACE_OUTER_BOUND('',#2335,.T.);
#1734=FACE_OUTER_BOUND('',#2336,.T.);
#1735=FACE_OUTER_BOUND('',#2337,.T.);
#1736=FACE_OUTER_BOUND('',#2338,.T.);
#1737=FACE_OUTER_BOUND('',#2339,.T.);
#1738=FACE_OUTER_BOUND('',#2340,.T.);
#1739=FACE_OUTER_BOUND('',#2341,.T.);
#1740=FACE_OUTER_BOUND('',#2342,.T.);
#1741=FACE_OUTER_BOUND('',#2343,.T.);
#1742=FACE_OUTER_BOUND('',#2344,.T.);
#1743=FACE_OUTER_BOUND('',#2345,.T.);
#1744=FACE_OUTER_BOUND('',#2346,.T.);
#1745=FACE_OUTER_BOUND('',#2347,.T.);
#1746=FACE_OUTER_BOUND('',#2348,.T.);
#1747=FACE_OUTER_BOUND('',#2349,.T.);
#1748=FACE_OUTER_BOUND('',#2350,.T.);
#1749=FACE_OUTER_BOUND('',#2351,.T.);
#1750=FACE_OUTER_BOUND('',#2352,.T.);
#1751=FACE_OUTER_BOUND('',#2353,.T.);
#1752=FACE_OUTER_BOUND('',#2354,.T.);
#1753=FACE_OUTER_BOUND('',#2355,.T.);
#1754=FACE_OUTER_BOUND('',#2356,.T.);
#1755=FACE_OUTER_BOUND('',#2357,.T.);
#1756=FACE_OUTER_BOUND('',#2358,.T.);
#1757=FACE_OUTER_BOUND('',#2359,.T.);
#1758=FACE_OUTER_BOUND('',#2360,.T.);
#1759=FACE_OUTER_BOUND('',#2361,.T.);
#1760=FACE_OUTER_BOUND('',#2362,.T.);
#1761=FACE_OUTER_BOUND('',#2363,.T.);
#1762=FACE_OUTER_BOUND('',#2364,.T.);
#1763=FACE_OUTER_BOUND('',#2365,.T.);
#1764=FACE_OUTER_BOUND('',#2366,.T.);
#1765=FACE_OUTER_BOUND('',#2367,.T.);
#1766=FACE_OUTER_BOUND('',#2368,.T.);
#1767=FACE_OUTER_BOUND('',#2369,.T.);
#1768=FACE_OUTER_BOUND('',#2370,.T.);
#1769=FACE_OUTER_BOUND('',#2371,.T.);
#1770=FACE_OUTER_BOUND('',#2372,.T.);
#1771=FACE_OUTER_BOUND('',#2373,.T.);
#1772=FACE_OUTER_BOUND('',#2374,.T.);
#1773=FACE_OUTER_BOUND('',#2375,.T.);
#1774=FACE_OUTER_BOUND('',#2376,.T.);
#1775=FACE_OUTER_BOUND('',#2377,.T.);
#1776=FACE_OUTER_BOUND('',#2378,.T.);
#1777=FACE_OUTER_BOUND('',#2379,.T.);
#1778=FACE_OUTER_BOUND('',#2380,.T.);
#1779=FACE_OUTER_BOUND('',#2381,.T.);
#1780=FACE_OUTER_BOUND('',#2382,.T.);
#1781=FACE_OUTER_BOUND('',#2383,.T.);
#1782=FACE_OUTER_BOUND('',#2384,.T.);
#1783=FACE_OUTER_BOUND('',#2385,.T.);
#1784=FACE_OUTER_BOUND('',#2386,.T.);
#1785=FACE_OUTER_BOUND('',#2387,.T.);
#1786=FACE_OUTER_BOUND('',#2388,.T.);
#1787=FACE_OUTER_BOUND('',#2389,.T.);
#1788=FACE_OUTER_BOUND('',#2390,.T.);
#1789=FACE_OUTER_BOUND('',#2391,.T.);
#1790=FACE_OUTER_BOUND('',#2392,.T.);
#1791=FACE_OUTER_BOUND('',#2393,.T.);
#1792=FACE_OUTER_BOUND('',#2394,.T.);
#1793=FACE_OUTER_BOUND('',#2395,.T.);
#1794=FACE_OUTER_BOUND('',#2396,.T.);
#1795=FACE_OUTER_BOUND('',#2397,.T.);
#1796=FACE_OUTER_BOUND('',#2398,.T.);
#1797=FACE_OUTER_BOUND('',#2399,.T.);
#1798=FACE_OUTER_BOUND('',#2401,.T.);
#1799=FACE_OUTER_BOUND('',#2402,.T.);
#1800=FACE_OUTER_BOUND('',#2404,.T.);
#2327=EDGE_LOOP('',(#8493,#8494,#8495,#8496));
#2328=EDGE_LOOP('',(#8497,#8498,#8499,#8500));
#2329=EDGE_LOOP('',(#8501,#8502,#8503,#8504));
#2330=EDGE_LOOP('',(#8505,#8506,#8507,#8508));
#2331=EDGE_LOOP('',(#8509,#8510,#8511,#8512));
#2332=EDGE_LOOP('',(#8513,#8514,#8515,#8516));
#2333=EDGE_LOOP('',(#8517,#8518,#8519,#8520));
#2334=EDGE_LOOP('',(#8521,#8522,#8523,#8524));
#2335=EDGE_LOOP('',(#8525,#8526,#8527,#8528));
#2336=EDGE_LOOP('',(#8529,#8530,#8531,#8532));
#2337=EDGE_LOOP('',(#8533,#8534,#8535,#8536));
#2338=EDGE_LOOP('',(#8537,#8538,#8539,#8540));
#2339=EDGE_LOOP('',(#8541,#8542,#8543,#8544));
#2340=EDGE_LOOP('',(#8545,#8546,#8547,#8548));
#2341=EDGE_LOOP('',(#8549,#8550,#8551,#8552));
#2342=EDGE_LOOP('',(#8553,#8554,#8555,#8556));
#2343=EDGE_LOOP('',(#8557,#8558,#8559,#8560));
#2344=EDGE_LOOP('',(#8561,#8562,#8563,#8564));
#2345=EDGE_LOOP('',(#8565,#8566,#8567,#8568));
#2346=EDGE_LOOP('',(#8569,#8570,#8571,#8572));
#2347=EDGE_LOOP('',(#8573,#8574,#8575,#8576));
#2348=EDGE_LOOP('',(#8577,#8578,#8579,#8580));
#2349=EDGE_LOOP('',(#8581,#8582,#8583,#8584));
#2350=EDGE_LOOP('',(#8585,#8586,#8587,#8588));
#2351=EDGE_LOOP('',(#8589,#8590,#8591,#8592));
#2352=EDGE_LOOP('',(#8593,#8594,#8595,#8596));
#2353=EDGE_LOOP('',(#8597,#8598,#8599,#8600));
#2354=EDGE_LOOP('',(#8601,#8602,#8603,#8604));
#2355=EDGE_LOOP('',(#8605,#8606,#8607,#8608));
#2356=EDGE_LOOP('',(#8609,#8610,#8611,#8612));
#2357=EDGE_LOOP('',(#8613,#8614,#8615,#8616));
#2358=EDGE_LOOP('',(#8617,#8618,#8619,#8620));
#2359=EDGE_LOOP('',(#8621,#8622,#8623,#8624));
#2360=EDGE_LOOP('',(#8625,#8626,#8627,#8628));
#2361=EDGE_LOOP('',(#8629,#8630,#8631,#8632));
#2362=EDGE_LOOP('',(#8633,#8634,#8635,#8636));
#2363=EDGE_LOOP('',(#8637,#8638,#8639,#8640));
#2364=EDGE_LOOP('',(#8641,#8642,#8643,#8644));
#2365=EDGE_LOOP('',(#8645,#8646,#8647,#8648));
#2366=EDGE_LOOP('',(#8649,#8650,#8651,#8652));
#2367=EDGE_LOOP('',(#8653,#8654,#8655,#8656));
#2368=EDGE_LOOP('',(#8657,#8658,#8659,#8660));
#2369=EDGE_LOOP('',(#8661,#8662,#8663,#8664));
#2370=EDGE_LOOP('',(#8665,#8666,#8667,#8668));
#2371=EDGE_LOOP('',(#8669,#8670,#8671,#8672));
#2372=EDGE_LOOP('',(#8673,#8674,#8675,#8676));
#2373=EDGE_LOOP('',(#8677,#8678,#8679,#8680));
#2374=EDGE_LOOP('',(#8681,#8682,#8683,#8684));
#2375=EDGE_LOOP('',(#8685,#8686,#8687,#8688));
#2376=EDGE_LOOP('',(#8689,#8690,#8691,#8692));
#2377=EDGE_LOOP('',(#8693,#8694,#8695,#8696));
#2378=EDGE_LOOP('',(#8697,#8698,#8699,#8700));
#2379=EDGE_LOOP('',(#8701,#8702,#8703,#8704));
#2380=EDGE_LOOP('',(#8705,#8706,#8707,#8708));
#2381=EDGE_LOOP('',(#8709,#8710,#8711,#8712));
#2382=EDGE_LOOP('',(#8713,#8714,#8715,#8716));
#2383=EDGE_LOOP('',(#8717,#8718,#8719,#8720));
#2384=EDGE_LOOP('',(#8721,#8722,#8723,#8724));
#2385=EDGE_LOOP('',(#8725,#8726,#8727,#8728));
#2386=EDGE_LOOP('',(#8729,#8730,#8731,#8732));
#2387=EDGE_LOOP('',(#8733,#8734,#8735,#8736,#8737,#8738,#8739,#8740));
#2388=EDGE_LOOP('',(#8741,#8742,#8743,#8744,#8745,#8746,#8747,#8748,#8749,
#8750,#8751,#8752,#8753,#8754,#8755,#8756,#8757,#8758,#8759,#8760,#8761,
#8762,#8763,#8764,#8765,#8766,#8767,#8768,#8769,#8770,#8771,#8772,#8773,
#8774,#8775,#8776,#8777,#8778,#8779,#8780,#8781,#8782,#8783,#8784,#8785,
#8786,#8787,#8788,#8789,#8790,#8791,#8792,#8793,#8794,#8795,#8796,#8797,
#8798,#8799,#8800,#8801,#8802,#8803,#8804));
#2389=EDGE_LOOP('',(#8805,#8806,#8807,#8808));
#2390=EDGE_LOOP('',(#8809,#8810,#8811,#8812,#8813,#8814,#8815,#8816,#8817,
#8818,#8819,#8820,#8821,#8822,#8823,#8824,#8825,#8826,#8827,#8828,#8829,
#8830,#8831,#8832,#8833,#8834,#8835,#8836,#8837,#8838,#8839,#8840,#8841,
#8842,#8843,#8844,#8845,#8846,#8847,#8848,#8849,#8850,#8851,#8852,#8853,
#8854,#8855,#8856,#8857,#8858,#8859,#8860,#8861,#8862,#8863,#8864,#8865,
#8866,#8867,#8868,#8869,#8870,#8871,#8872,#8873));
#2391=EDGE_LOOP('',(#8874,#8875,#8876,#8877));
#2392=EDGE_LOOP('',(#8878,#8879,#8880,#8881));
#2393=EDGE_LOOP('',(#8882,#8883,#8884,#8885));
#2394=EDGE_LOOP('',(#8886,#8887,#8888,#8889));
#2395=EDGE_LOOP('',(#8890,#8891,#8892,#8893));
#2396=EDGE_LOOP('',(#8894,#8895,#8896,#8897));
#2397=EDGE_LOOP('',(#8898,#8899,#8900,#8901));
#2398=EDGE_LOOP('',(#8902,#8903,#8904,#8905,#8906,#8907));
#2399=EDGE_LOOP('',(#8908));
#2400=EDGE_LOOP('',(#8909,#8910,#8911,#8912));
#2401=EDGE_LOOP('',(#8913,#8914,#8915,#8916));
#2402=EDGE_LOOP('',(#8917));
#2403=EDGE_LOOP('',(#8918,#8919,#8920,#8921,#8922,#8923));
#2404=EDGE_LOOP('',(#8924));
#2945=LINE('',#19092,#3533);
#2946=LINE('',#19116,#3534);
#2947=LINE('',#19164,#3535);
#2948=LINE('',#19212,#3536);
#2949=LINE('',#19263,#3537);
#2950=LINE('',#19311,#3538);
#2951=LINE('',#19359,#3539);
#2952=LINE('',#19407,#3540);
#2953=LINE('',#19461,#3541);
#2954=LINE('',#19509,#3542);
#2955=LINE('',#19557,#3543);
#2956=LINE('',#19611,#3544);
#2957=LINE('',#19659,#3545);
#2958=LINE('',#19707,#3546);
#2959=LINE('',#19755,#3547);
#2960=LINE('',#19809,#3548);
#2961=LINE('',#19857,#3549);
#2962=LINE('',#19905,#3550);
#2963=LINE('',#19959,#3551);
#2964=LINE('',#20007,#3552);
#2965=LINE('',#20055,#3553);
#2966=LINE('',#20109,#3554);
#2967=LINE('',#20157,#3555);
#2968=LINE('',#20205,#3556);
#2969=LINE('',#20253,#3557);
#2970=LINE('',#20307,#3558);
#2971=LINE('',#20355,#3559);
#2972=LINE('',#20403,#3560);
#2973=LINE('',#20457,#3561);
#2974=LINE('',#20505,#3562);
#2975=LINE('',#20553,#3563);
#2976=LINE('',#20579,#3564);
#2977=LINE('',#20603,#3565);
#2978=LINE('',#20627,#3566);
#2979=LINE('',#20652,#3567);
#2980=LINE('',#20677,#3568);
#2981=LINE('',#20701,#3569);
#2982=LINE('',#20726,#3570);
#2983=LINE('',#20751,#3571);
#2984=LINE('',#20775,#3572);
#2985=LINE('',#20799,#3573);
#2986=LINE('',#20824,#3574);
#2987=LINE('',#20849,#3575);
#2988=LINE('',#20873,#3576);
#2989=LINE('',#20898,#3577);
#2990=LINE('',#20923,#3578);
#2991=LINE('',#20947,#3579);
#2992=LINE('',#20972,#3580);
#2993=LINE('',#20997,#3581);
#2994=LINE('',#21021,#3582);
#2995=LINE('',#21045,#3583);
#2996=LINE('',#21070,#3584);
#2997=LINE('',#21095,#3585);
#2998=LINE('',#21119,#3586);
#2999=LINE('',#21144,#3587);
#3000=LINE('',#21169,#3588);
#3001=LINE('',#21193,#3589);
#3002=LINE('',#21218,#3590);
#3003=LINE('',#21242,#3591);
#3004=LINE('',#21267,#3592);
#3005=LINE('',#21468,#3593);
#3006=LINE('',#23213,#3594);
#3007=LINE('',#23215,#3595);
#3008=LINE('',#23217,#3596);
#3009=LINE('',#23218,#3597);
#3010=LINE('',#23221,#3598);
#3011=LINE('',#23223,#3599);
#3012=LINE('',#23224,#3600);
#3013=LINE('',#23227,#3601);
#3014=LINE('',#23229,#3602);
#3015=LINE('',#23230,#3603);
#3016=LINE('',#23233,#3604);
#3017=LINE('',#23235,#3605);
#3018=LINE('',#23236,#3606);
#3019=LINE('',#23239,#3607);
#3020=LINE('',#23241,#3608);
#3021=LINE('',#23242,#3609);
#3022=LINE('',#23244,#3610);
#3023=LINE('',#23245,#3611);
#3024=LINE('',#23252,#3612);
#3533=VECTOR('',#12093,0.15);
#3534=VECTOR('',#12098,0.15);
#3535=VECTOR('',#12101,0.15);
#3536=VECTOR('',#12104,0.15);
#3537=VECTOR('',#12107,0.15);
#3538=VECTOR('',#12110,0.15);
#3539=VECTOR('',#12113,0.15);
#3540=VECTOR('',#12116,0.15);
#3541=VECTOR('',#12119,0.15);
#3542=VECTOR('',#12122,0.15);
#3543=VECTOR('',#12125,0.15);
#3544=VECTOR('',#12128,0.15);
#3545=VECTOR('',#12131,0.15);
#3546=VECTOR('',#12134,0.15);
#3547=VECTOR('',#12137,0.15);
#3548=VECTOR('',#12140,0.15);
#3549=VECTOR('',#12143,0.15);
#3550=VECTOR('',#12146,0.15);
#3551=VECTOR('',#12149,0.15);
#3552=VECTOR('',#12152,0.15);
#3553=VECTOR('',#12155,0.15);
#3554=VECTOR('',#12158,0.15);
#3555=VECTOR('',#12161,0.15);
#3556=VECTOR('',#12164,0.15);
#3557=VECTOR('',#12167,0.15);
#3558=VECTOR('',#12170,0.15);
#3559=VECTOR('',#12173,0.15);
#3560=VECTOR('',#12176,0.15);
#3561=VECTOR('',#12179,0.15);
#3562=VECTOR('',#12182,0.15);
#3563=VECTOR('',#12185,0.117775);
#3564=VECTOR('',#12190,0.117775);
#3565=VECTOR('',#12193,0.117775);
#3566=VECTOR('',#12196,0.117775);
#3567=VECTOR('',#12199,0.117775);
#3568=VECTOR('',#12202,0.117775);
#3569=VECTOR('',#12205,0.117775);
#3570=VECTOR('',#12208,0.117775);
#3571=VECTOR('',#12211,0.117775);
#3572=VECTOR('',#12214,0.117775);
#3573=VECTOR('',#12217,0.117775);
#3574=VECTOR('',#12220,0.117775);
#3575=VECTOR('',#12223,0.117775);
#3576=VECTOR('',#12226,0.117775);
#3577=VECTOR('',#12229,0.117775);
#3578=VECTOR('',#12232,0.117775);
#3579=VECTOR('',#12235,0.117775);
#3580=VECTOR('',#12238,0.117775);
#3581=VECTOR('',#12241,0.117775);
#3582=VECTOR('',#12244,0.117775);
#3583=VECTOR('',#12247,0.117775);
#3584=VECTOR('',#12250,0.117775);
#3585=VECTOR('',#12253,0.117775);
#3586=VECTOR('',#12256,0.117775);
#3587=VECTOR('',#12259,0.117775);
#3588=VECTOR('',#12262,0.117775);
#3589=VECTOR('',#12265,0.117775);
#3590=VECTOR('',#12268,0.117775);
#3591=VECTOR('',#12271,0.117775);
#3592=VECTOR('',#12274,0.117775);
#3593=VECTOR('',#12279,0.1);
#3594=VECTOR('',#12290,1.);
#3595=VECTOR('',#12291,1.);
#3596=VECTOR('',#12292,1.);
#3597=VECTOR('',#12293,1.);
#3598=VECTOR('',#12296,1.);
#3599=VECTOR('',#12297,1.);
#3600=VECTOR('',#12298,1.);
#3601=VECTOR('',#12301,1.);
#3602=VECTOR('',#12302,1.);
#3603=VECTOR('',#12303,1.);
#3604=VECTOR('',#12306,1.);
#3605=VECTOR('',#12307,1.);
#3606=VECTOR('',#12308,1.);
#3607=VECTOR('',#12311,1.);
#3608=VECTOR('',#12312,1.);
#3609=VECTOR('',#12313,1.);
#3610=VECTOR('',#12316,1.);
#3611=VECTOR('',#12317,1.);
#3612=VECTOR('',#12326,0.275);
#3783=CIRCLE('',#10489,0.14635);
#3784=CIRCLE('',#10520,0.117775);
#3785=CIRCLE('',#10551,0.14635);
#3786=CIRCLE('',#10552,0.05);
#3787=CIRCLE('',#10554,0.117775);
#3788=CIRCLE('',#10564,0.275);
#3789=CIRCLE('',#10566,0.275);
#4555=VERTEX_POINT('',#19090);
#4556=VERTEX_POINT('',#19091);
#4557=VERTEX_POINT('',#19093);
#4558=VERTEX_POINT('',#19104);
#4559=VERTEX_POINT('',#19114);
#4560=VERTEX_POINT('',#19115);
#4561=VERTEX_POINT('',#19162);
#4562=VERTEX_POINT('',#19163);
#4563=VERTEX_POINT('',#19210);
#4564=VERTEX_POINT('',#19211);
#4565=VERTEX_POINT('',#19261);
#4566=VERTEX_POINT('',#19262);
#4567=VERTEX_POINT('',#19309);
#4568=VERTEX_POINT('',#19310);
#4569=VERTEX_POINT('',#19357);
#4570=VERTEX_POINT('',#19358);
#4571=VERTEX_POINT('',#19405);
#4572=VERTEX_POINT('',#19406);
#4573=VERTEX_POINT('',#19459);
#4574=VERTEX_POINT('',#19460);
#4575=VERTEX_POINT('',#19507);
#4576=VERTEX_POINT('',#19508);
#4577=VERTEX_POINT('',#19555);
#4578=VERTEX_POINT('',#19556);
#4579=VERTEX_POINT('',#19609);
#4580=VERTEX_POINT('',#19610);
#4581=VERTEX_POINT('',#19657);
#4582=VERTEX_POINT('',#19658);
#4583=VERTEX_POINT('',#19705);
#4584=VERTEX_POINT('',#19706);
#4585=VERTEX_POINT('',#19753);
#4586=VERTEX_POINT('',#19754);
#4587=VERTEX_POINT('',#19807);
#4588=VERTEX_POINT('',#19808);
#4589=VERTEX_POINT('',#19855);
#4590=VERTEX_POINT('',#19856);
#4591=VERTEX_POINT('',#19903);
#4592=VERTEX_POINT('',#19904);
#4593=VERTEX_POINT('',#19957);
#4594=VERTEX_POINT('',#19958);
#4595=VERTEX_POINT('',#20005);
#4596=VERTEX_POINT('',#20006);
#4597=VERTEX_POINT('',#20053);
#4598=VERTEX_POINT('',#20054);
#4599=VERTEX_POINT('',#20107);
#4600=VERTEX_POINT('',#20108);
#4601=VERTEX_POINT('',#20155);
#4602=VERTEX_POINT('',#20156);
#4603=VERTEX_POINT('',#20203);
#4604=VERTEX_POINT('',#20204);
#4605=VERTEX_POINT('',#20251);
#4606=VERTEX_POINT('',#20252);
#4607=VERTEX_POINT('',#20305);
#4608=VERTEX_POINT('',#20306);
#4609=VERTEX_POINT('',#20353);
#4610=VERTEX_POINT('',#20354);
#4611=VERTEX_POINT('',#20401);
#4612=VERTEX_POINT('',#20402);
#4613=VERTEX_POINT('',#20455);
#4614=VERTEX_POINT('',#20456);
#4615=VERTEX_POINT('',#20503);
#4616=VERTEX_POINT('',#20504);
#4617=VERTEX_POINT('',#20551);
#4618=VERTEX_POINT('',#20552);
#4619=VERTEX_POINT('',#20554);
#4620=VERTEX_POINT('',#20565);
#4621=VERTEX_POINT('',#20577);
#4622=VERTEX_POINT('',#20578);
#4623=VERTEX_POINT('',#20601);
#4624=VERTEX_POINT('',#20602);
#4625=VERTEX_POINT('',#20625);
#4626=VERTEX_POINT('',#20626);
#4627=VERTEX_POINT('',#20650);
#4628=VERTEX_POINT('',#20651);
#4629=VERTEX_POINT('',#20675);
#4630=VERTEX_POINT('',#20676);
#4631=VERTEX_POINT('',#20699);
#4632=VERTEX_POINT('',#20700);
#4633=VERTEX_POINT('',#20724);
#4634=VERTEX_POINT('',#20725);
#4635=VERTEX_POINT('',#20749);
#4636=VERTEX_POINT('',#20750);
#4637=VERTEX_POINT('',#20773);
#4638=VERTEX_POINT('',#20774);
#4639=VERTEX_POINT('',#20797);
#4640=VERTEX_POINT('',#20798);
#4641=VERTEX_POINT('',#20822);
#4642=VERTEX_POINT('',#20823);
#4643=VERTEX_POINT('',#20847);
#4644=VERTEX_POINT('',#20848);
#4645=VERTEX_POINT('',#20871);
#4646=VERTEX_POINT('',#20872);
#4647=VERTEX_POINT('',#20896);
#4648=VERTEX_POINT('',#20897);
#4649=VERTEX_POINT('',#20921);
#4650=VERTEX_POINT('',#20922);
#4651=VERTEX_POINT('',#20945);
#4652=VERTEX_POINT('',#20946);
#4653=VERTEX_POINT('',#20970);
#4654=VERTEX_POINT('',#20971);
#4655=VERTEX_POINT('',#20995);
#4656=VERTEX_POINT('',#20996);
#4657=VERTEX_POINT('',#21019);
#4658=VERTEX_POINT('',#21020);
#4659=VERTEX_POINT('',#21043);
#4660=VERTEX_POINT('',#21044);
#4661=VERTEX_POINT('',#21068);
#4662=VERTEX_POINT('',#21069);
#4663=VERTEX_POINT('',#21093);
#4664=VERTEX_POINT('',#21094);
#4665=VERTEX_POINT('',#21117);
#4666=VERTEX_POINT('',#21118);
#4667=VERTEX_POINT('',#21142);
#4668=VERTEX_POINT('',#21143);
#4669=VERTEX_POINT('',#21167);
#4670=VERTEX_POINT('',#21168);
#4671=VERTEX_POINT('',#21191);
#4672=VERTEX_POINT('',#21192);
#4673=VERTEX_POINT('',#21216);
#4674=VERTEX_POINT('',#21217);
#4675=VERTEX_POINT('',#21240);
#4676=VERTEX_POINT('',#21241);
#4677=VERTEX_POINT('',#21265);
#4678=VERTEX_POINT('',#21266);
#4679=VERTEX_POINT('',#21289);
#4680=VERTEX_POINT('',#21411);
#4681=VERTEX_POINT('',#21449);
#4682=VERTEX_POINT('',#21467);
#4683=VERTEX_POINT('',#22254);
#4684=VERTEX_POINT('',#22332);
#4685=VERTEX_POINT('',#23211);
#4686=VERTEX_POINT('',#23212);
#4687=VERTEX_POINT('',#23214);
#4688=VERTEX_POINT('',#23216);
#4689=VERTEX_POINT('',#23220);
#4690=VERTEX_POINT('',#23222);
#4691=VERTEX_POINT('',#23226);
#4692=VERTEX_POINT('',#23228);
#4693=VERTEX_POINT('',#23232);
#4694=VERTEX_POINT('',#23234);
#4695=VERTEX_POINT('',#23238);
#4696=VERTEX_POINT('',#23240);
#4697=VERTEX_POINT('',#23248);
#4698=VERTEX_POINT('',#23251);
#5905=EDGE_CURVE('',#4555,#4556,#2945,.T.);
#5906=EDGE_CURVE('',#4555,#4557,#817,.T.);
#5907=EDGE_CURVE('',#4557,#4558,#3783,.F.);
#5908=EDGE_CURVE('',#4558,#4556,#818,.T.);
#5909=EDGE_CURVE('',#4559,#4560,#2946,.T.);
#5910=EDGE_CURVE('',#4559,#4555,#819,.T.);
#5911=EDGE_CURVE('',#4556,#4560,#820,.T.);
#5912=EDGE_CURVE('',#4561,#4562,#2947,.T.);
#5913=EDGE_CURVE('',#4561,#4559,#821,.T.);
#5914=EDGE_CURVE('',#4560,#4562,#822,.T.);
#5915=EDGE_CURVE('',#4563,#4564,#2948,.T.);
#5916=EDGE_CURVE('',#4563,#4561,#823,.T.);
#5917=EDGE_CURVE('',#4562,#4564,#824,.T.);
#5918=EDGE_CURVE('',#4565,#4566,#2949,.T.);
#5919=EDGE_CURVE('',#4565,#4563,#825,.T.);
#5920=EDGE_CURVE('',#4564,#4566,#826,.T.);
#5921=EDGE_CURVE('',#4567,#4568,#2950,.T.);
#5922=EDGE_CURVE('',#4567,#4565,#827,.T.);
#5923=EDGE_CURVE('',#4566,#4568,#828,.T.);
#5924=EDGE_CURVE('',#4569,#4570,#2951,.T.);
#5925=EDGE_CURVE('',#4569,#4567,#829,.T.);
#5926=EDGE_CURVE('',#4568,#4570,#830,.T.);
#5927=EDGE_CURVE('',#4571,#4572,#2952,.T.);
#5928=EDGE_CURVE('',#4571,#4569,#831,.T.);
#5929=EDGE_CURVE('',#4570,#4572,#832,.T.);
#5930=EDGE_CURVE('',#4573,#4574,#2953,.T.);
#5931=EDGE_CURVE('',#4573,#4571,#833,.T.);
#5932=EDGE_CURVE('',#4572,#4574,#834,.T.);
#5933=EDGE_CURVE('',#4575,#4576,#2954,.T.);
#5934=EDGE_CURVE('',#4575,#4573,#835,.T.);
#5935=EDGE_CURVE('',#4574,#4576,#836,.T.);
#5936=EDGE_CURVE('',#4577,#4578,#2955,.T.);
#5937=EDGE_CURVE('',#4577,#4575,#837,.T.);
#5938=EDGE_CURVE('',#4576,#4578,#838,.T.);
#5939=EDGE_CURVE('',#4579,#4580,#2956,.T.);
#5940=EDGE_CURVE('',#4579,#4577,#839,.T.);
#5941=EDGE_CURVE('',#4578,#4580,#840,.T.);
#5942=EDGE_CURVE('',#4581,#4582,#2957,.T.);
#5943=EDGE_CURVE('',#4581,#4579,#841,.T.);
#5944=EDGE_CURVE('',#4580,#4582,#842,.T.);
#5945=EDGE_CURVE('',#4583,#4584,#2958,.T.);
#5946=EDGE_CURVE('',#4583,#4581,#843,.T.);
#5947=EDGE_CURVE('',#4582,#4584,#844,.T.);
#5948=EDGE_CURVE('',#4585,#4586,#2959,.T.);
#5949=EDGE_CURVE('',#4585,#4583,#845,.T.);
#5950=EDGE_CURVE('',#4584,#4586,#846,.T.);
#5951=EDGE_CURVE('',#4587,#4588,#2960,.T.);
#5952=EDGE_CURVE('',#4587,#4585,#847,.T.);
#5953=EDGE_CURVE('',#4586,#4588,#848,.T.);
#5954=EDGE_CURVE('',#4589,#4590,#2961,.T.);
#5955=EDGE_CURVE('',#4589,#4587,#849,.T.);
#5956=EDGE_CURVE('',#4588,#4590,#850,.T.);
#5957=EDGE_CURVE('',#4591,#4592,#2962,.T.);
#5958=EDGE_CURVE('',#4591,#4589,#851,.T.);
#5959=EDGE_CURVE('',#4590,#4592,#852,.T.);
#5960=EDGE_CURVE('',#4593,#4594,#2963,.T.);
#5961=EDGE_CURVE('',#4593,#4591,#853,.T.);
#5962=EDGE_CURVE('',#4592,#4594,#854,.T.);
#5963=EDGE_CURVE('',#4595,#4596,#2964,.T.);
#5964=EDGE_CURVE('',#4595,#4593,#855,.T.);
#5965=EDGE_CURVE('',#4594,#4596,#856,.T.);
#5966=EDGE_CURVE('',#4597,#4598,#2965,.T.);
#5967=EDGE_CURVE('',#4597,#4595,#857,.T.);
#5968=EDGE_CURVE('',#4596,#4598,#858,.T.);
#5969=EDGE_CURVE('',#4599,#4600,#2966,.T.);
#5970=EDGE_CURVE('',#4599,#4597,#859,.T.);
#5971=EDGE_CURVE('',#4598,#4600,#860,.T.);
#5972=EDGE_CURVE('',#4601,#4602,#2967,.T.);
#5973=EDGE_CURVE('',#4601,#4599,#861,.T.);
#5974=EDGE_CURVE('',#4600,#4602,#862,.T.);
#5975=EDGE_CURVE('',#4603,#4604,#2968,.T.);
#5976=EDGE_CURVE('',#4603,#4601,#863,.T.);
#5977=EDGE_CURVE('',#4602,#4604,#864,.T.);
#5978=EDGE_CURVE('',#4605,#4606,#2969,.T.);
#5979=EDGE_CURVE('',#4605,#4603,#865,.T.);
#5980=EDGE_CURVE('',#4604,#4606,#866,.T.);
#5981=EDGE_CURVE('',#4607,#4608,#2970,.T.);
#5982=EDGE_CURVE('',#4607,#4605,#867,.T.);
#5983=EDGE_CURVE('',#4606,#4608,#868,.T.);
#5984=EDGE_CURVE('',#4609,#4610,#2971,.T.);
#5985=EDGE_CURVE('',#4609,#4607,#869,.T.);
#5986=EDGE_CURVE('',#4608,#4610,#870,.T.);
#5987=EDGE_CURVE('',#4611,#4612,#2972,.T.);
#5988=EDGE_CURVE('',#4611,#4609,#871,.T.);
#5989=EDGE_CURVE('',#4610,#4612,#872,.T.);
#5990=EDGE_CURVE('',#4613,#4614,#2973,.T.);
#5991=EDGE_CURVE('',#4613,#4611,#873,.T.);
#5992=EDGE_CURVE('',#4612,#4614,#874,.T.);
#5993=EDGE_CURVE('',#4615,#4616,#2974,.T.);
#5994=EDGE_CURVE('',#4615,#4613,#875,.T.);
#5995=EDGE_CURVE('',#4614,#4616,#876,.T.);
#5996=EDGE_CURVE('',#4617,#4618,#2975,.T.);
#5997=EDGE_CURVE('',#4617,#4619,#877,.T.);
#5998=EDGE_CURVE('',#4619,#4620,#3784,.T.);
#5999=EDGE_CURVE('',#4618,#4620,#878,.T.);
#6000=EDGE_CURVE('',#4621,#4622,#2976,.T.);
#6001=EDGE_CURVE('',#4621,#4617,#879,.T.);
#6002=EDGE_CURVE('',#4622,#4618,#880,.T.);
#6003=EDGE_CURVE('',#4623,#4624,#2977,.T.);
#6004=EDGE_CURVE('',#4623,#4621,#881,.T.);
#6005=EDGE_CURVE('',#4624,#4622,#882,.T.);
#6006=EDGE_CURVE('',#4625,#4626,#2978,.T.);
#6007=EDGE_CURVE('',#4625,#4623,#883,.T.);
#6008=EDGE_CURVE('',#4626,#4624,#884,.T.);
#6009=EDGE_CURVE('',#4627,#4628,#2979,.T.);
#6010=EDGE_CURVE('',#4627,#4625,#885,.T.);
#6011=EDGE_CURVE('',#4628,#4626,#886,.T.);
#6012=EDGE_CURVE('',#4629,#4630,#2980,.T.);
#6013=EDGE_CURVE('',#4629,#4627,#887,.T.);
#6014=EDGE_CURVE('',#4630,#4628,#888,.T.);
#6015=EDGE_CURVE('',#4631,#4632,#2981,.T.);
#6016=EDGE_CURVE('',#4631,#4629,#889,.T.);
#6017=EDGE_CURVE('',#4632,#4630,#890,.T.);
#6018=EDGE_CURVE('',#4633,#4634,#2982,.T.);
#6019=EDGE_CURVE('',#4633,#4631,#891,.T.);
#6020=EDGE_CURVE('',#4634,#4632,#892,.T.);
#6021=EDGE_CURVE('',#4635,#4636,#2983,.T.);
#6022=EDGE_CURVE('',#4635,#4633,#893,.T.);
#6023=EDGE_CURVE('',#4636,#4634,#894,.T.);
#6024=EDGE_CURVE('',#4637,#4638,#2984,.T.);
#6025=EDGE_CURVE('',#4637,#4635,#895,.T.);
#6026=EDGE_CURVE('',#4638,#4636,#896,.T.);
#6027=EDGE_CURVE('',#4639,#4640,#2985,.T.);
#6028=EDGE_CURVE('',#4639,#4637,#897,.T.);
#6029=EDGE_CURVE('',#4640,#4638,#898,.T.);
#6030=EDGE_CURVE('',#4641,#4642,#2986,.T.);
#6031=EDGE_CURVE('',#4641,#4639,#899,.T.);
#6032=EDGE_CURVE('',#4642,#4640,#900,.T.);
#6033=EDGE_CURVE('',#4643,#4644,#2987,.T.);
#6034=EDGE_CURVE('',#4643,#4641,#901,.T.);
#6035=EDGE_CURVE('',#4644,#4642,#902,.T.);
#6036=EDGE_CURVE('',#4645,#4646,#2988,.T.);
#6037=EDGE_CURVE('',#4645,#4643,#903,.T.);
#6038=EDGE_CURVE('',#4646,#4644,#904,.T.);
#6039=EDGE_CURVE('',#4647,#4648,#2989,.T.);
#6040=EDGE_CURVE('',#4647,#4645,#905,.T.);
#6041=EDGE_CURVE('',#4648,#4646,#906,.T.);
#6042=EDGE_CURVE('',#4649,#4650,#2990,.T.);
#6043=EDGE_CURVE('',#4649,#4647,#907,.T.);
#6044=EDGE_CURVE('',#4650,#4648,#908,.T.);
#6045=EDGE_CURVE('',#4651,#4652,#2991,.T.);
#6046=EDGE_CURVE('',#4651,#4649,#909,.T.);
#6047=EDGE_CURVE('',#4652,#4650,#910,.T.);
#6048=EDGE_CURVE('',#4653,#4654,#2992,.T.);
#6049=EDGE_CURVE('',#4653,#4651,#911,.T.);
#6050=EDGE_CURVE('',#4654,#4652,#912,.T.);
#6051=EDGE_CURVE('',#4655,#4656,#2993,.T.);
#6052=EDGE_CURVE('',#4655,#4653,#913,.T.);
#6053=EDGE_CURVE('',#4656,#4654,#914,.T.);
#6054=EDGE_CURVE('',#4657,#4658,#2994,.T.);
#6055=EDGE_CURVE('',#4657,#4655,#915,.T.);
#6056=EDGE_CURVE('',#4658,#4656,#916,.T.);
#6057=EDGE_CURVE('',#4659,#4660,#2995,.T.);
#6058=EDGE_CURVE('',#4659,#4657,#917,.T.);
#6059=EDGE_CURVE('',#4660,#4658,#918,.T.);
#6060=EDGE_CURVE('',#4661,#4662,#2996,.T.);
#6061=EDGE_CURVE('',#4661,#4659,#919,.T.);
#6062=EDGE_CURVE('',#4662,#4660,#920,.T.);
#6063=EDGE_CURVE('',#4663,#4664,#2997,.T.);
#6064=EDGE_CURVE('',#4663,#4661,#921,.T.);
#6065=EDGE_CURVE('',#4664,#4662,#922,.T.);
#6066=EDGE_CURVE('',#4665,#4666,#2998,.T.);
#6067=EDGE_CURVE('',#4665,#4663,#923,.T.);
#6068=EDGE_CURVE('',#4666,#4664,#924,.T.);
#6069=EDGE_CURVE('',#4667,#4668,#2999,.T.);
#6070=EDGE_CURVE('',#4667,#4665,#925,.T.);
#6071=EDGE_CURVE('',#4668,#4666,#926,.T.);
#6072=EDGE_CURVE('',#4669,#4670,#3000,.T.);
#6073=EDGE_CURVE('',#4669,#4667,#927,.T.);
#6074=EDGE_CURVE('',#4670,#4668,#928,.T.);
#6075=EDGE_CURVE('',#4671,#4672,#3001,.T.);
#6076=EDGE_CURVE('',#4671,#4669,#929,.T.);
#6077=EDGE_CURVE('',#4672,#4670,#930,.T.);
#6078=EDGE_CURVE('',#4673,#4674,#3002,.T.);
#6079=EDGE_CURVE('',#4673,#4671,#931,.T.);
#6080=EDGE_CURVE('',#4674,#4672,#932,.T.);
#6081=EDGE_CURVE('',#4675,#4676,#3003,.T.);
#6082=EDGE_CURVE('',#4675,#4673,#933,.T.);
#6083=EDGE_CURVE('',#4676,#4674,#934,.T.);
#6084=EDGE_CURVE('',#4677,#4678,#3004,.T.);
#6085=EDGE_CURVE('',#4677,#4675,#935,.T.);
#6086=EDGE_CURVE('',#4678,#4676,#936,.T.);
#6087=EDGE_CURVE('',#4620,#4679,#937,.T.);
#6088=EDGE_CURVE('',#4680,#4619,#938,.T.);
#6089=EDGE_CURVE('',#4681,#4680,#3785,.T.);
#6090=EDGE_CURVE('',#4679,#4681,#939,.T.);
#6091=EDGE_CURVE('',#4679,#4682,#3005,.T.);
#6092=EDGE_CURVE('',#4682,#4682,#3786,.T.);
#6093=EDGE_CURVE('',#4683,#4677,#940,.T.);
#6094=EDGE_CURVE('',#4557,#4683,#941,.T.);
#6095=EDGE_CURVE('',#4680,#4615,#942,.T.);
#6096=EDGE_CURVE('',#4684,#4678,#943,.T.);
#6097=EDGE_CURVE('',#4683,#4684,#3787,.T.);
#6098=EDGE_CURVE('',#4616,#4681,#944,.T.);
#6099=EDGE_CURVE('',#4684,#4558,#945,.T.);
#6100=EDGE_CURVE('',#4685,#4686,#3006,.T.);
#6101=EDGE_CURVE('',#4685,#4687,#3007,.T.);
#6102=EDGE_CURVE('',#4687,#4688,#3008,.T.);
#6103=EDGE_CURVE('',#4686,#4688,#3009,.T.);
#6104=EDGE_CURVE('',#4689,#4685,#3010,.T.);
#6105=EDGE_CURVE('',#4689,#4690,#3011,.T.);
#6106=EDGE_CURVE('',#4690,#4687,#3012,.T.);
#6107=EDGE_CURVE('',#4691,#4689,#3013,.T.);
#6108=EDGE_CURVE('',#4691,#4692,#3014,.T.);
#6109=EDGE_CURVE('',#4692,#4690,#3015,.T.);
#6110=EDGE_CURVE('',#4693,#4691,#3016,.T.);
#6111=EDGE_CURVE('',#4693,#4694,#3017,.T.);
#6112=EDGE_CURVE('',#4694,#4692,#3018,.T.);
#6113=EDGE_CURVE('',#4695,#4693,#3019,.T.);
#6114=EDGE_CURVE('',#4695,#4696,#3020,.T.);
#6115=EDGE_CURVE('',#4696,#4694,#3021,.T.);
#6116=EDGE_CURVE('',#4686,#4695,#3022,.T.);
#6117=EDGE_CURVE('',#4688,#4696,#3023,.T.);
#6118=EDGE_CURVE('',#4697,#4697,#3788,.T.);
#6119=EDGE_CURVE('',#4697,#4698,#3024,.T.);
#6120=EDGE_CURVE('',#4698,#4698,#3789,.T.);
#8493=ORIENTED_EDGE('',*,*,#5905,.F.);
#8494=ORIENTED_EDGE('',*,*,#5906,.T.);
#8495=ORIENTED_EDGE('',*,*,#5907,.T.);
#8496=ORIENTED_EDGE('',*,*,#5908,.T.);
#8497=ORIENTED_EDGE('',*,*,#5909,.F.);
#8498=ORIENTED_EDGE('',*,*,#5910,.T.);
#8499=ORIENTED_EDGE('',*,*,#5905,.T.);
#8500=ORIENTED_EDGE('',*,*,#5911,.T.);
#8501=ORIENTED_EDGE('',*,*,#5912,.F.);
#8502=ORIENTED_EDGE('',*,*,#5913,.T.);
#8503=ORIENTED_EDGE('',*,*,#5909,.T.);
#8504=ORIENTED_EDGE('',*,*,#5914,.T.);
#8505=ORIENTED_EDGE('',*,*,#5915,.F.);
#8506=ORIENTED_EDGE('',*,*,#5916,.T.);
#8507=ORIENTED_EDGE('',*,*,#5912,.T.);
#8508=ORIENTED_EDGE('',*,*,#5917,.T.);
#8509=ORIENTED_EDGE('',*,*,#5918,.F.);
#8510=ORIENTED_EDGE('',*,*,#5919,.T.);
#8511=ORIENTED_EDGE('',*,*,#5915,.T.);
#8512=ORIENTED_EDGE('',*,*,#5920,.T.);
#8513=ORIENTED_EDGE('',*,*,#5921,.F.);
#8514=ORIENTED_EDGE('',*,*,#5922,.T.);
#8515=ORIENTED_EDGE('',*,*,#5918,.T.);
#8516=ORIENTED_EDGE('',*,*,#5923,.T.);
#8517=ORIENTED_EDGE('',*,*,#5924,.F.);
#8518=ORIENTED_EDGE('',*,*,#5925,.T.);
#8519=ORIENTED_EDGE('',*,*,#5921,.T.);
#8520=ORIENTED_EDGE('',*,*,#5926,.T.);
#8521=ORIENTED_EDGE('',*,*,#5927,.F.);
#8522=ORIENTED_EDGE('',*,*,#5928,.T.);
#8523=ORIENTED_EDGE('',*,*,#5924,.T.);
#8524=ORIENTED_EDGE('',*,*,#5929,.T.);
#8525=ORIENTED_EDGE('',*,*,#5930,.F.);
#8526=ORIENTED_EDGE('',*,*,#5931,.T.);
#8527=ORIENTED_EDGE('',*,*,#5927,.T.);
#8528=ORIENTED_EDGE('',*,*,#5932,.T.);
#8529=ORIENTED_EDGE('',*,*,#5933,.F.);
#8530=ORIENTED_EDGE('',*,*,#5934,.T.);
#8531=ORIENTED_EDGE('',*,*,#5930,.T.);
#8532=ORIENTED_EDGE('',*,*,#5935,.T.);
#8533=ORIENTED_EDGE('',*,*,#5936,.F.);
#8534=ORIENTED_EDGE('',*,*,#5937,.T.);
#8535=ORIENTED_EDGE('',*,*,#5933,.T.);
#8536=ORIENTED_EDGE('',*,*,#5938,.T.);
#8537=ORIENTED_EDGE('',*,*,#5939,.F.);
#8538=ORIENTED_EDGE('',*,*,#5940,.T.);
#8539=ORIENTED_EDGE('',*,*,#5936,.T.);
#8540=ORIENTED_EDGE('',*,*,#5941,.T.);
#8541=ORIENTED_EDGE('',*,*,#5942,.F.);
#8542=ORIENTED_EDGE('',*,*,#5943,.T.);
#8543=ORIENTED_EDGE('',*,*,#5939,.T.);
#8544=ORIENTED_EDGE('',*,*,#5944,.T.);
#8545=ORIENTED_EDGE('',*,*,#5945,.F.);
#8546=ORIENTED_EDGE('',*,*,#5946,.T.);
#8547=ORIENTED_EDGE('',*,*,#5942,.T.);
#8548=ORIENTED_EDGE('',*,*,#5947,.T.);
#8549=ORIENTED_EDGE('',*,*,#5948,.F.);
#8550=ORIENTED_EDGE('',*,*,#5949,.T.);
#8551=ORIENTED_EDGE('',*,*,#5945,.T.);
#8552=ORIENTED_EDGE('',*,*,#5950,.T.);
#8553=ORIENTED_EDGE('',*,*,#5951,.F.);
#8554=ORIENTED_EDGE('',*,*,#5952,.T.);
#8555=ORIENTED_EDGE('',*,*,#5948,.T.);
#8556=ORIENTED_EDGE('',*,*,#5953,.T.);
#8557=ORIENTED_EDGE('',*,*,#5954,.F.);
#8558=ORIENTED_EDGE('',*,*,#5955,.T.);
#8559=ORIENTED_EDGE('',*,*,#5951,.T.);
#8560=ORIENTED_EDGE('',*,*,#5956,.T.);
#8561=ORIENTED_EDGE('',*,*,#5957,.F.);
#8562=ORIENTED_EDGE('',*,*,#5958,.T.);
#8563=ORIENTED_EDGE('',*,*,#5954,.T.);
#8564=ORIENTED_EDGE('',*,*,#5959,.T.);
#8565=ORIENTED_EDGE('',*,*,#5960,.F.);
#8566=ORIENTED_EDGE('',*,*,#5961,.T.);
#8567=ORIENTED_EDGE('',*,*,#5957,.T.);
#8568=ORIENTED_EDGE('',*,*,#5962,.T.);
#8569=ORIENTED_EDGE('',*,*,#5963,.F.);
#8570=ORIENTED_EDGE('',*,*,#5964,.T.);
#8571=ORIENTED_EDGE('',*,*,#5960,.T.);
#8572=ORIENTED_EDGE('',*,*,#5965,.T.);
#8573=ORIENTED_EDGE('',*,*,#5966,.F.);
#8574=ORIENTED_EDGE('',*,*,#5967,.T.);
#8575=ORIENTED_EDGE('',*,*,#5963,.T.);
#8576=ORIENTED_EDGE('',*,*,#5968,.T.);
#8577=ORIENTED_EDGE('',*,*,#5969,.F.);
#8578=ORIENTED_EDGE('',*,*,#5970,.T.);
#8579=ORIENTED_EDGE('',*,*,#5966,.T.);
#8580=ORIENTED_EDGE('',*,*,#5971,.T.);
#8581=ORIENTED_EDGE('',*,*,#5972,.F.);
#8582=ORIENTED_EDGE('',*,*,#5973,.T.);
#8583=ORIENTED_EDGE('',*,*,#5969,.T.);
#8584=ORIENTED_EDGE('',*,*,#5974,.T.);
#8585=ORIENTED_EDGE('',*,*,#5975,.F.);
#8586=ORIENTED_EDGE('',*,*,#5976,.T.);
#8587=ORIENTED_EDGE('',*,*,#5972,.T.);
#8588=ORIENTED_EDGE('',*,*,#5977,.T.);
#8589=ORIENTED_EDGE('',*,*,#5978,.F.);
#8590=ORIENTED_EDGE('',*,*,#5979,.T.);
#8591=ORIENTED_EDGE('',*,*,#5975,.T.);
#8592=ORIENTED_EDGE('',*,*,#5980,.T.);
#8593=ORIENTED_EDGE('',*,*,#5981,.F.);
#8594=ORIENTED_EDGE('',*,*,#5982,.T.);
#8595=ORIENTED_EDGE('',*,*,#5978,.T.);
#8596=ORIENTED_EDGE('',*,*,#5983,.T.);
#8597=ORIENTED_EDGE('',*,*,#5984,.F.);
#8598=ORIENTED_EDGE('',*,*,#5985,.T.);
#8599=ORIENTED_EDGE('',*,*,#5981,.T.);
#8600=ORIENTED_EDGE('',*,*,#5986,.T.);
#8601=ORIENTED_EDGE('',*,*,#5987,.F.);
#8602=ORIENTED_EDGE('',*,*,#5988,.T.);
#8603=ORIENTED_EDGE('',*,*,#5984,.T.);
#8604=ORIENTED_EDGE('',*,*,#5989,.T.);
#8605=ORIENTED_EDGE('',*,*,#5990,.F.);
#8606=ORIENTED_EDGE('',*,*,#5991,.T.);
#8607=ORIENTED_EDGE('',*,*,#5987,.T.);
#8608=ORIENTED_EDGE('',*,*,#5992,.T.);
#8609=ORIENTED_EDGE('',*,*,#5993,.F.);
#8610=ORIENTED_EDGE('',*,*,#5994,.T.);
#8611=ORIENTED_EDGE('',*,*,#5990,.T.);
#8612=ORIENTED_EDGE('',*,*,#5995,.T.);
#8613=ORIENTED_EDGE('',*,*,#5996,.F.);
#8614=ORIENTED_EDGE('',*,*,#5997,.T.);
#8615=ORIENTED_EDGE('',*,*,#5998,.T.);
#8616=ORIENTED_EDGE('',*,*,#5999,.F.);
#8617=ORIENTED_EDGE('',*,*,#6000,.F.);
#8618=ORIENTED_EDGE('',*,*,#6001,.T.);
#8619=ORIENTED_EDGE('',*,*,#5996,.T.);
#8620=ORIENTED_EDGE('',*,*,#6002,.F.);
#8621=ORIENTED_EDGE('',*,*,#6003,.F.);
#8622=ORIENTED_EDGE('',*,*,#6004,.T.);
#8623=ORIENTED_EDGE('',*,*,#6000,.T.);
#8624=ORIENTED_EDGE('',*,*,#6005,.F.);
#8625=ORIENTED_EDGE('',*,*,#6006,.F.);
#8626=ORIENTED_EDGE('',*,*,#6007,.T.);
#8627=ORIENTED_EDGE('',*,*,#6003,.T.);
#8628=ORIENTED_EDGE('',*,*,#6008,.F.);
#8629=ORIENTED_EDGE('',*,*,#6009,.F.);
#8630=ORIENTED_EDGE('',*,*,#6010,.T.);
#8631=ORIENTED_EDGE('',*,*,#6006,.T.);
#8632=ORIENTED_EDGE('',*,*,#6011,.F.);
#8633=ORIENTED_EDGE('',*,*,#6012,.F.);
#8634=ORIENTED_EDGE('',*,*,#6013,.T.);
#8635=ORIENTED_EDGE('',*,*,#6009,.T.);
#8636=ORIENTED_EDGE('',*,*,#6014,.F.);
#8637=ORIENTED_EDGE('',*,*,#6015,.F.);
#8638=ORIENTED_EDGE('',*,*,#6016,.T.);
#8639=ORIENTED_EDGE('',*,*,#6012,.T.);
#8640=ORIENTED_EDGE('',*,*,#6017,.F.);
#8641=ORIENTED_EDGE('',*,*,#6018,.F.);
#8642=ORIENTED_EDGE('',*,*,#6019,.T.);
#8643=ORIENTED_EDGE('',*,*,#6015,.T.);
#8644=ORIENTED_EDGE('',*,*,#6020,.F.);
#8645=ORIENTED_EDGE('',*,*,#6021,.F.);
#8646=ORIENTED_EDGE('',*,*,#6022,.T.);
#8647=ORIENTED_EDGE('',*,*,#6018,.T.);
#8648=ORIENTED_EDGE('',*,*,#6023,.F.);
#8649=ORIENTED_EDGE('',*,*,#6024,.F.);
#8650=ORIENTED_EDGE('',*,*,#6025,.T.);
#8651=ORIENTED_EDGE('',*,*,#6021,.T.);
#8652=ORIENTED_EDGE('',*,*,#6026,.F.);
#8653=ORIENTED_EDGE('',*,*,#6027,.F.);
#8654=ORIENTED_EDGE('',*,*,#6028,.T.);
#8655=ORIENTED_EDGE('',*,*,#6024,.T.);
#8656=ORIENTED_EDGE('',*,*,#6029,.F.);
#8657=ORIENTED_EDGE('',*,*,#6030,.F.);
#8658=ORIENTED_EDGE('',*,*,#6031,.T.);
#8659=ORIENTED_EDGE('',*,*,#6027,.T.);
#8660=ORIENTED_EDGE('',*,*,#6032,.F.);
#8661=ORIENTED_EDGE('',*,*,#6033,.F.);
#8662=ORIENTED_EDGE('',*,*,#6034,.T.);
#8663=ORIENTED_EDGE('',*,*,#6030,.T.);
#8664=ORIENTED_EDGE('',*,*,#6035,.F.);
#8665=ORIENTED_EDGE('',*,*,#6036,.F.);
#8666=ORIENTED_EDGE('',*,*,#6037,.T.);
#8667=ORIENTED_EDGE('',*,*,#6033,.T.);
#8668=ORIENTED_EDGE('',*,*,#6038,.F.);
#8669=ORIENTED_EDGE('',*,*,#6039,.F.);
#8670=ORIENTED_EDGE('',*,*,#6040,.T.);
#8671=ORIENTED_EDGE('',*,*,#6036,.T.);
#8672=ORIENTED_EDGE('',*,*,#6041,.F.);
#8673=ORIENTED_EDGE('',*,*,#6042,.F.);
#8674=ORIENTED_EDGE('',*,*,#6043,.T.);
#8675=ORIENTED_EDGE('',*,*,#6039,.T.);
#8676=ORIENTED_EDGE('',*,*,#6044,.F.);
#8677=ORIENTED_EDGE('',*,*,#6045,.F.);
#8678=ORIENTED_EDGE('',*,*,#6046,.T.);
#8679=ORIENTED_EDGE('',*,*,#6042,.T.);
#8680=ORIENTED_EDGE('',*,*,#6047,.F.);
#8681=ORIENTED_EDGE('',*,*,#6048,.F.);
#8682=ORIENTED_EDGE('',*,*,#6049,.T.);
#8683=ORIENTED_EDGE('',*,*,#6045,.T.);
#8684=ORIENTED_EDGE('',*,*,#6050,.F.);
#8685=ORIENTED_EDGE('',*,*,#6051,.F.);
#8686=ORIENTED_EDGE('',*,*,#6052,.T.);
#8687=ORIENTED_EDGE('',*,*,#6048,.T.);
#8688=ORIENTED_EDGE('',*,*,#6053,.F.);
#8689=ORIENTED_EDGE('',*,*,#6054,.F.);
#8690=ORIENTED_EDGE('',*,*,#6055,.T.);
#8691=ORIENTED_EDGE('',*,*,#6051,.T.);
#8692=ORIENTED_EDGE('',*,*,#6056,.F.);
#8693=ORIENTED_EDGE('',*,*,#6057,.F.);
#8694=ORIENTED_EDGE('',*,*,#6058,.T.);
#8695=ORIENTED_EDGE('',*,*,#6054,.T.);
#8696=ORIENTED_EDGE('',*,*,#6059,.F.);
#8697=ORIENTED_EDGE('',*,*,#6060,.F.);
#8698=ORIENTED_EDGE('',*,*,#6061,.T.);
#8699=ORIENTED_EDGE('',*,*,#6057,.T.);
#8700=ORIENTED_EDGE('',*,*,#6062,.F.);
#8701=ORIENTED_EDGE('',*,*,#6063,.F.);
#8702=ORIENTED_EDGE('',*,*,#6064,.T.);
#8703=ORIENTED_EDGE('',*,*,#6060,.T.);
#8704=ORIENTED_EDGE('',*,*,#6065,.F.);
#8705=ORIENTED_EDGE('',*,*,#6066,.F.);
#8706=ORIENTED_EDGE('',*,*,#6067,.T.);
#8707=ORIENTED_EDGE('',*,*,#6063,.T.);
#8708=ORIENTED_EDGE('',*,*,#6068,.F.);
#8709=ORIENTED_EDGE('',*,*,#6069,.F.);
#8710=ORIENTED_EDGE('',*,*,#6070,.T.);
#8711=ORIENTED_EDGE('',*,*,#6066,.T.);
#8712=ORIENTED_EDGE('',*,*,#6071,.F.);
#8713=ORIENTED_EDGE('',*,*,#6072,.F.);
#8714=ORIENTED_EDGE('',*,*,#6073,.T.);
#8715=ORIENTED_EDGE('',*,*,#6069,.T.);
#8716=ORIENTED_EDGE('',*,*,#6074,.F.);
#8717=ORIENTED_EDGE('',*,*,#6075,.F.);
#8718=ORIENTED_EDGE('',*,*,#6076,.T.);
#8719=ORIENTED_EDGE('',*,*,#6072,.T.);
#8720=ORIENTED_EDGE('',*,*,#6077,.F.);
#8721=ORIENTED_EDGE('',*,*,#6078,.F.);
#8722=ORIENTED_EDGE('',*,*,#6079,.T.);
#8723=ORIENTED_EDGE('',*,*,#6075,.T.);
#8724=ORIENTED_EDGE('',*,*,#6080,.F.);
#8725=ORIENTED_EDGE('',*,*,#6081,.F.);
#8726=ORIENTED_EDGE('',*,*,#6082,.T.);
#8727=ORIENTED_EDGE('',*,*,#6078,.T.);
#8728=ORIENTED_EDGE('',*,*,#6083,.F.);
#8729=ORIENTED_EDGE('',*,*,#6084,.F.);
#8730=ORIENTED_EDGE('',*,*,#6085,.T.);
#8731=ORIENTED_EDGE('',*,*,#6081,.T.);
#8732=ORIENTED_EDGE('',*,*,#6086,.F.);
#8733=ORIENTED_EDGE('',*,*,#6087,.F.);
#8734=ORIENTED_EDGE('',*,*,#5998,.F.);
#8735=ORIENTED_EDGE('',*,*,#6088,.F.);
#8736=ORIENTED_EDGE('',*,*,#6089,.F.);
#8737=ORIENTED_EDGE('',*,*,#6090,.F.);
#8738=ORIENTED_EDGE('',*,*,#6091,.T.);
#8739=ORIENTED_EDGE('',*,*,#6092,.F.);
#8740=ORIENTED_EDGE('',*,*,#6091,.F.);
#8741=ORIENTED_EDGE('',*,*,#6088,.T.);
#8742=ORIENTED_EDGE('',*,*,#5997,.F.);
#8743=ORIENTED_EDGE('',*,*,#6001,.F.);
#8744=ORIENTED_EDGE('',*,*,#6004,.F.);
#8745=ORIENTED_EDGE('',*,*,#6007,.F.);
#8746=ORIENTED_EDGE('',*,*,#6010,.F.);
#8747=ORIENTED_EDGE('',*,*,#6013,.F.);
#8748=ORIENTED_EDGE('',*,*,#6016,.F.);
#8749=ORIENTED_EDGE('',*,*,#6019,.F.);
#8750=ORIENTED_EDGE('',*,*,#6022,.F.);
#8751=ORIENTED_EDGE('',*,*,#6025,.F.);
#8752=ORIENTED_EDGE('',*,*,#6028,.F.);
#8753=ORIENTED_EDGE('',*,*,#6031,.F.);
#8754=ORIENTED_EDGE('',*,*,#6034,.F.);
#8755=ORIENTED_EDGE('',*,*,#6037,.F.);
#8756=ORIENTED_EDGE('',*,*,#6040,.F.);
#8757=ORIENTED_EDGE('',*,*,#6043,.F.);
#8758=ORIENTED_EDGE('',*,*,#6046,.F.);
#8759=ORIENTED_EDGE('',*,*,#6049,.F.);
#8760=ORIENTED_EDGE('',*,*,#6052,.F.);
#8761=ORIENTED_EDGE('',*,*,#6055,.F.);
#8762=ORIENTED_EDGE('',*,*,#6058,.F.);
#8763=ORIENTED_EDGE('',*,*,#6061,.F.);
#8764=ORIENTED_EDGE('',*,*,#6064,.F.);
#8765=ORIENTED_EDGE('',*,*,#6067,.F.);
#8766=ORIENTED_EDGE('',*,*,#6070,.F.);
#8767=ORIENTED_EDGE('',*,*,#6073,.F.);
#8768=ORIENTED_EDGE('',*,*,#6076,.F.);
#8769=ORIENTED_EDGE('',*,*,#6079,.F.);
#8770=ORIENTED_EDGE('',*,*,#6082,.F.);
#8771=ORIENTED_EDGE('',*,*,#6085,.F.);
#8772=ORIENTED_EDGE('',*,*,#6093,.F.);
#8773=ORIENTED_EDGE('',*,*,#6094,.F.);
#8774=ORIENTED_EDGE('',*,*,#5906,.F.);
#8775=ORIENTED_EDGE('',*,*,#5910,.F.);
#8776=ORIENTED_EDGE('',*,*,#5913,.F.);
#8777=ORIENTED_EDGE('',*,*,#5916,.F.);
#8778=ORIENTED_EDGE('',*,*,#5919,.F.);
#8779=ORIENTED_EDGE('',*,*,#5922,.F.);
#8780=ORIENTED_EDGE('',*,*,#5925,.F.);
#8781=ORIENTED_EDGE('',*,*,#5928,.F.);
#8782=ORIENTED_EDGE('',*,*,#5931,.F.);
#8783=ORIENTED_EDGE('',*,*,#5934,.F.);
#8784=ORIENTED_EDGE('',*,*,#5937,.F.);
#8785=ORIENTED_EDGE('',*,*,#5940,.F.);
#8786=ORIENTED_EDGE('',*,*,#5943,.F.);
#8787=ORIENTED_EDGE('',*,*,#5946,.F.);
#8788=ORIENTED_EDGE('',*,*,#5949,.F.);
#8789=ORIENTED_EDGE('',*,*,#5952,.F.);
#8790=ORIENTED_EDGE('',*,*,#5955,.F.);
#8791=ORIENTED_EDGE('',*,*,#5958,.F.);
#8792=ORIENTED_EDGE('',*,*,#5961,.F.);
#8793=ORIENTED_EDGE('',*,*,#5964,.F.);
#8794=ORIENTED_EDGE('',*,*,#5967,.F.);
#8795=ORIENTED_EDGE('',*,*,#5970,.F.);
#8796=ORIENTED_EDGE('',*,*,#5973,.F.);
#8797=ORIENTED_EDGE('',*,*,#5976,.F.);
#8798=ORIENTED_EDGE('',*,*,#5979,.F.);
#8799=ORIENTED_EDGE('',*,*,#5982,.F.);
#8800=ORIENTED_EDGE('',*,*,#5985,.F.);
#8801=ORIENTED_EDGE('',*,*,#5988,.F.);
#8802=ORIENTED_EDGE('',*,*,#5991,.F.);
#8803=ORIENTED_EDGE('',*,*,#5994,.F.);
#8804=ORIENTED_EDGE('',*,*,#6095,.F.);
#8805=ORIENTED_EDGE('',*,*,#6084,.T.);
#8806=ORIENTED_EDGE('',*,*,#6096,.F.);
#8807=ORIENTED_EDGE('',*,*,#6097,.F.);
#8808=ORIENTED_EDGE('',*,*,#6093,.T.);
#8809=ORIENTED_EDGE('',*,*,#6087,.T.);
#8810=ORIENTED_EDGE('',*,*,#6090,.T.);
#8811=ORIENTED_EDGE('',*,*,#6098,.F.);
#8812=ORIENTED_EDGE('',*,*,#5995,.F.);
#8813=ORIENTED_EDGE('',*,*,#5992,.F.);
#8814=ORIENTED_EDGE('',*,*,#5989,.F.);
#8815=ORIENTED_EDGE('',*,*,#5986,.F.);
#8816=ORIENTED_EDGE('',*,*,#5983,.F.);
#8817=ORIENTED_EDGE('',*,*,#5980,.F.);
#8818=ORIENTED_EDGE('',*,*,#5977,.F.);
#8819=ORIENTED_EDGE('',*,*,#5974,.F.);
#8820=ORIENTED_EDGE('',*,*,#5971,.F.);
#8821=ORIENTED_EDGE('',*,*,#5968,.F.);
#8822=ORIENTED_EDGE('',*,*,#5965,.F.);
#8823=ORIENTED_EDGE('',*,*,#5962,.F.);
#8824=ORIENTED_EDGE('',*,*,#5959,.F.);
#8825=ORIENTED_EDGE('',*,*,#5956,.F.);
#8826=ORIENTED_EDGE('',*,*,#5953,.F.);
#8827=ORIENTED_EDGE('',*,*,#5950,.F.);
#8828=ORIENTED_EDGE('',*,*,#5947,.F.);
#8829=ORIENTED_EDGE('',*,*,#5944,.F.);
#8830=ORIENTED_EDGE('',*,*,#5941,.F.);
#8831=ORIENTED_EDGE('',*,*,#5938,.F.);
#8832=ORIENTED_EDGE('',*,*,#5935,.F.);
#8833=ORIENTED_EDGE('',*,*,#5932,.F.);
#8834=ORIENTED_EDGE('',*,*,#5929,.F.);
#8835=ORIENTED_EDGE('',*,*,#5926,.F.);
#8836=ORIENTED_EDGE('',*,*,#5923,.F.);
#8837=ORIENTED_EDGE('',*,*,#5920,.F.);
#8838=ORIENTED_EDGE('',*,*,#5917,.F.);
#8839=ORIENTED_EDGE('',*,*,#5914,.F.);
#8840=ORIENTED_EDGE('',*,*,#5911,.F.);
#8841=ORIENTED_EDGE('',*,*,#5908,.F.);
#8842=ORIENTED_EDGE('',*,*,#6099,.F.);
#8843=ORIENTED_EDGE('',*,*,#6096,.T.);
#8844=ORIENTED_EDGE('',*,*,#6086,.T.);
#8845=ORIENTED_EDGE('',*,*,#6083,.T.);
#8846=ORIENTED_EDGE('',*,*,#6080,.T.);
#8847=ORIENTED_EDGE('',*,*,#6077,.T.);
#8848=ORIENTED_EDGE('',*,*,#6074,.T.);
#8849=ORIENTED_EDGE('',*,*,#6071,.T.);
#8850=ORIENTED_EDGE('',*,*,#6068,.T.);
#8851=ORIENTED_EDGE('',*,*,#6065,.T.);
#8852=ORIENTED_EDGE('',*,*,#6062,.T.);
#8853=ORIENTED_EDGE('',*,*,#6059,.T.);
#8854=ORIENTED_EDGE('',*,*,#6056,.T.);
#8855=ORIENTED_EDGE('',*,*,#6053,.T.);
#8856=ORIENTED_EDGE('',*,*,#6050,.T.);
#8857=ORIENTED_EDGE('',*,*,#6047,.T.);
#8858=ORIENTED_EDGE('',*,*,#6044,.T.);
#8859=ORIENTED_EDGE('',*,*,#6041,.T.);
#8860=ORIENTED_EDGE('',*,*,#6038,.T.);
#8861=ORIENTED_EDGE('',*,*,#6035,.T.);
#8862=ORIENTED_EDGE('',*,*,#6032,.T.);
#8863=ORIENTED_EDGE('',*,*,#6029,.T.);
#8864=ORIENTED_EDGE('',*,*,#6026,.T.);
#8865=ORIENTED_EDGE('',*,*,#6023,.T.);
#8866=ORIENTED_EDGE('',*,*,#6020,.T.);
#8867=ORIENTED_EDGE('',*,*,#6017,.T.);
#8868=ORIENTED_EDGE('',*,*,#6014,.T.);
#8869=ORIENTED_EDGE('',*,*,#6011,.T.);
#8870=ORIENTED_EDGE('',*,*,#6008,.T.);
#8871=ORIENTED_EDGE('',*,*,#6005,.T.);
#8872=ORIENTED_EDGE('',*,*,#6002,.T.);
#8873=ORIENTED_EDGE('',*,*,#5999,.T.);
#8874=ORIENTED_EDGE('',*,*,#5993,.T.);
#8875=ORIENTED_EDGE('',*,*,#6098,.T.);
#8876=ORIENTED_EDGE('',*,*,#6089,.T.);
#8877=ORIENTED_EDGE('',*,*,#6095,.T.);
#8878=ORIENTED_EDGE('',*,*,#6100,.F.);
#8879=ORIENTED_EDGE('',*,*,#6101,.T.);
#8880=ORIENTED_EDGE('',*,*,#6102,.T.);
#8881=ORIENTED_EDGE('',*,*,#6103,.F.);
#8882=ORIENTED_EDGE('',*,*,#6104,.F.);
#8883=ORIENTED_EDGE('',*,*,#6105,.T.);
#8884=ORIENTED_EDGE('',*,*,#6106,.T.);
#8885=ORIENTED_EDGE('',*,*,#6101,.F.);
#8886=ORIENTED_EDGE('',*,*,#6107,.F.);
#8887=ORIENTED_EDGE('',*,*,#6108,.T.);
#8888=ORIENTED_EDGE('',*,*,#6109,.T.);
#8889=ORIENTED_EDGE('',*,*,#6105,.F.);
#8890=ORIENTED_EDGE('',*,*,#6110,.F.);
#8891=ORIENTED_EDGE('',*,*,#6111,.T.);
#8892=ORIENTED_EDGE('',*,*,#6112,.T.);
#8893=ORIENTED_EDGE('',*,*,#6108,.F.);
#8894=ORIENTED_EDGE('',*,*,#6113,.F.);
#8895=ORIENTED_EDGE('',*,*,#6114,.T.);
#8896=ORIENTED_EDGE('',*,*,#6115,.T.);
#8897=ORIENTED_EDGE('',*,*,#6111,.F.);
#8898=ORIENTED_EDGE('',*,*,#6116,.F.);
#8899=ORIENTED_EDGE('',*,*,#6103,.T.);
#8900=ORIENTED_EDGE('',*,*,#6117,.T.);
#8901=ORIENTED_EDGE('',*,*,#6114,.F.);
#8902=ORIENTED_EDGE('',*,*,#6117,.F.);
#8903=ORIENTED_EDGE('',*,*,#6102,.F.);
#8904=ORIENTED_EDGE('',*,*,#6106,.F.);
#8905=ORIENTED_EDGE('',*,*,#6109,.F.);
#8906=ORIENTED_EDGE('',*,*,#6112,.F.);
#8907=ORIENTED_EDGE('',*,*,#6115,.F.);
#8908=ORIENTED_EDGE('',*,*,#6118,.T.);
#8909=ORIENTED_EDGE('',*,*,#6094,.T.);
#8910=ORIENTED_EDGE('',*,*,#6097,.T.);
#8911=ORIENTED_EDGE('',*,*,#6099,.T.);
#8912=ORIENTED_EDGE('',*,*,#5907,.F.);
#8913=ORIENTED_EDGE('',*,*,#6118,.F.);
#8914=ORIENTED_EDGE('',*,*,#6119,.T.);
#8915=ORIENTED_EDGE('',*,*,#6120,.T.);
#8916=ORIENTED_EDGE('',*,*,#6119,.F.);
#8917=ORIENTED_EDGE('',*,*,#6120,.F.);
#8918=ORIENTED_EDGE('',*,*,#6100,.T.);
#8919=ORIENTED_EDGE('',*,*,#6116,.T.);
#8920=ORIENTED_EDGE('',*,*,#6113,.T.);
#8921=ORIENTED_EDGE('',*,*,#6110,.T.);
#8922=ORIENTED_EDGE('',*,*,#6107,.T.);
#8923=ORIENTED_EDGE('',*,*,#6104,.T.);
#8924=ORIENTED_EDGE('',*,*,#6092,.T.);
#9247=CYLINDRICAL_SURFACE('',#10488,0.14635);
#9248=CYLINDRICAL_SURFACE('',#10490,0.14635);
#9249=CYLINDRICAL_SURFACE('',#10491,0.14635);
#9250=CYLINDRICAL_SURFACE('',#10492,0.14635);
#9251=CYLINDRICAL_SURFACE('',#10493,0.14635);
#9252=CYLINDRICAL_SURFACE('',#10494,0.14635);
#9253=CYLINDRICAL_SURFACE('',#10495,0.14635);
#9254=CYLINDRICAL_SURFACE('',#10496,0.14635);
#9255=CYLINDRICAL_SURFACE('',#10497,0.14635);
#9256=CYLINDRICAL_SURFACE('',#10498,0.14635);
#9257=CYLINDRICAL_SURFACE('',#10499,0.14635);
#9258=CYLINDRICAL_SURFACE('',#10500,0.14635);
#9259=CYLINDRICAL_SURFACE('',#10501,0.14635);
#9260=CYLINDRICAL_SURFACE('',#10502,0.14635);
#9261=CYLINDRICAL_SURFACE('',#10503,0.14635);
#9262=CYLINDRICAL_SURFACE('',#10504,0.14635);
#9263=CYLINDRICAL_SURFACE('',#10505,0.14635);
#9264=CYLINDRICAL_SURFACE('',#10506,0.14635);
#9265=CYLINDRICAL_SURFACE('',#10507,0.14635);
#9266=CYLINDRICAL_SURFACE('',#10508,0.14635);
#9267=CYLINDRICAL_SURFACE('',#10509,0.14635);
#9268=CYLINDRICAL_SURFACE('',#10510,0.14635);
#9269=CYLINDRICAL_SURFACE('',#10511,0.14635);
#9270=CYLINDRICAL_SURFACE('',#10512,0.14635);
#9271=CYLINDRICAL_SURFACE('',#10513,0.14635);
#9272=CYLINDRICAL_SURFACE('',#10514,0.14635);
#9273=CYLINDRICAL_SURFACE('',#10515,0.14635);
#9274=CYLINDRICAL_SURFACE('',#10516,0.14635);
#9275=CYLINDRICAL_SURFACE('',#10517,0.14635);
#9276=CYLINDRICAL_SURFACE('',#10518,0.14635);
#9277=CYLINDRICAL_SURFACE('',#10519,0.117775);
#9278=CYLINDRICAL_SURFACE('',#10521,0.117775);
#9279=CYLINDRICAL_SURFACE('',#10522,0.117775);
#9280=CYLINDRICAL_SURFACE('',#10523,0.117775);
#9281=CYLINDRICAL_SURFACE('',#10524,0.117775);
#9282=CYLINDRICAL_SURFACE('',#10525,0.117775);
#9283=CYLINDRICAL_SURFACE('',#10526,0.117775);
#9284=CYLINDRICAL_SURFACE('',#10527,0.117775);
#9285=CYLINDRICAL_SURFACE('',#10528,0.117775);
#9286=CYLINDRICAL_SURFACE('',#10529,0.117775);
#9287=CYLINDRICAL_SURFACE('',#10530,0.117775);
#9288=CYLINDRICAL_SURFACE('',#10531,0.117775);
#9289=CYLINDRICAL_SURFACE('',#10532,0.117775);
#9290=CYLINDRICAL_SURFACE('',#10533,0.117775);
#9291=CYLINDRICAL_SURFACE('',#10534,0.117775);
#9292=CYLINDRICAL_SURFACE('',#10535,0.117775);
#9293=CYLINDRICAL_SURFACE('',#10536,0.117775);
#9294=CYLINDRICAL_SURFACE('',#10537,0.117775);
#9295=CYLINDRICAL_SURFACE('',#10538,0.117775);
#9296=CYLINDRICAL_SURFACE('',#10539,0.117775);
#9297=CYLINDRICAL_SURFACE('',#10540,0.117775);
#9298=CYLINDRICAL_SURFACE('',#10541,0.117775);
#9299=CYLINDRICAL_SURFACE('',#10542,0.117775);
#9300=CYLINDRICAL_SURFACE('',#10543,0.117775);
#9301=CYLINDRICAL_SURFACE('',#10544,0.117775);
#9302=CYLINDRICAL_SURFACE('',#10545,0.117775);
#9303=CYLINDRICAL_SURFACE('',#10546,0.117775);
#9304=CYLINDRICAL_SURFACE('',#10547,0.117775);
#9305=CYLINDRICAL_SURFACE('',#10548,0.117775);
#9306=CYLINDRICAL_SURFACE('',#10549,0.117775);
#9307=CYLINDRICAL_SURFACE('',#10553,0.117775);
#9308=CYLINDRICAL_SURFACE('',#10555,0.14635);
#9309=CYLINDRICAL_SURFACE('',#10565,0.275);
#9751=ADVANCED_FACE('',(#1725),#9247,.T.);
#9752=ADVANCED_FACE('',(#1726),#9248,.T.);
#9753=ADVANCED_FACE('',(#1727),#9249,.T.);
#9754=ADVANCED_FACE('',(#1728),#9250,.T.);
#9755=ADVANCED_FACE('',(#1729),#9251,.T.);
#9756=ADVANCED_FACE('',(#1730),#9252,.T.);
#9757=ADVANCED_FACE('',(#1731),#9253,.T.);
#9758=ADVANCED_FACE('',(#1732),#9254,.T.);
#9759=ADVANCED_FACE('',(#1733),#9255,.T.);
#9760=ADVANCED_FACE('',(#1734),#9256,.T.);
#9761=ADVANCED_FACE('',(#1735),#9257,.T.);
#9762=ADVANCED_FACE('',(#1736),#9258,.T.);
#9763=ADVANCED_FACE('',(#1737),#9259,.T.);
#9764=ADVANCED_FACE('',(#1738),#9260,.T.);
#9765=ADVANCED_FACE('',(#1739),#9261,.T.);
#9766=ADVANCED_FACE('',(#1740),#9262,.T.);
#9767=ADVANCED_FACE('',(#1741),#9263,.T.);
#9768=ADVANCED_FACE('',(#1742),#9264,.T.);
#9769=ADVANCED_FACE('',(#1743),#9265,.T.);
#9770=ADVANCED_FACE('',(#1744),#9266,.T.);
#9771=ADVANCED_FACE('',(#1745),#9267,.T.);
#9772=ADVANCED_FACE('',(#1746),#9268,.T.);
#9773=ADVANCED_FACE('',(#1747),#9269,.T.);
#9774=ADVANCED_FACE('',(#1748),#9270,.T.);
#9775=ADVANCED_FACE('',(#1749),#9271,.T.);
#9776=ADVANCED_FACE('',(#1750),#9272,.T.);
#9777=ADVANCED_FACE('',(#1751),#9273,.T.);
#9778=ADVANCED_FACE('',(#1752),#9274,.T.);
#9779=ADVANCED_FACE('',(#1753),#9275,.T.);
#9780=ADVANCED_FACE('',(#1754),#9276,.T.);
#9781=ADVANCED_FACE('',(#1755),#9277,.T.);
#9782=ADVANCED_FACE('',(#1756),#9278,.T.);
#9783=ADVANCED_FACE('',(#1757),#9279,.T.);
#9784=ADVANCED_FACE('',(#1758),#9280,.T.);
#9785=ADVANCED_FACE('',(#1759),#9281,.T.);
#9786=ADVANCED_FACE('',(#1760),#9282,.T.);
#9787=ADVANCED_FACE('',(#1761),#9283,.T.);
#9788=ADVANCED_FACE('',(#1762),#9284,.T.);
#9789=ADVANCED_FACE('',(#1763),#9285,.T.);
#9790=ADVANCED_FACE('',(#1764),#9286,.T.);
#9791=ADVANCED_FACE('',(#1765),#9287,.T.);
#9792=ADVANCED_FACE('',(#1766),#9288,.T.);
#9793=ADVANCED_FACE('',(#1767),#9289,.T.);
#9794=ADVANCED_FACE('',(#1768),#9290,.T.);
#9795=ADVANCED_FACE('',(#1769),#9291,.T.);
#9796=ADVANCED_FACE('',(#1770),#9292,.T.);
#9797=ADVANCED_FACE('',(#1771),#9293,.T.);
#9798=ADVANCED_FACE('',(#1772),#9294,.T.);
#9799=ADVANCED_FACE('',(#1773),#9295,.T.);
#9800=ADVANCED_FACE('',(#1774),#9296,.T.);
#9801=ADVANCED_FACE('',(#1775),#9297,.T.);
#9802=ADVANCED_FACE('',(#1776),#9298,.T.);
#9803=ADVANCED_FACE('',(#1777),#9299,.T.);
#9804=ADVANCED_FACE('',(#1778),#9300,.T.);
#9805=ADVANCED_FACE('',(#1779),#9301,.T.);
#9806=ADVANCED_FACE('',(#1780),#9302,.T.);
#9807=ADVANCED_FACE('',(#1781),#9303,.T.);
#9808=ADVANCED_FACE('',(#1782),#9304,.T.);
#9809=ADVANCED_FACE('',(#1783),#9305,.T.);
#9810=ADVANCED_FACE('',(#1784),#9306,.T.);
#9811=ADVANCED_FACE('',(#1785),#75,.T.);
#9812=ADVANCED_FACE('',(#1786),#269,.F.);
#9813=ADVANCED_FACE('',(#1787),#9307,.T.);
#9814=ADVANCED_FACE('',(#1788),#270,.F.);
#9815=ADVANCED_FACE('',(#1789),#9308,.T.);
#9816=ADVANCED_FACE('',(#1790),#1278,.F.);
#9817=ADVANCED_FACE('',(#1791),#1279,.F.);
#9818=ADVANCED_FACE('',(#1792),#1280,.F.);
#9819=ADVANCED_FACE('',(#1793),#1281,.F.);
#9820=ADVANCED_FACE('',(#1794),#1282,.F.);
#9821=ADVANCED_FACE('',(#1795),#1283,.F.);
#9822=ADVANCED_FACE('',(#1796),#1284,.F.);
#9823=ADVANCED_FACE('',(#1797,#181),#1285,.T.);
#9824=ADVANCED_FACE('',(#1798),#9309,.T.);
#9825=ADVANCED_FACE('',(#1799,#182),#1286,.F.);
#9826=ADVANCED_FACE('',(#1800),#1287,.T.);
#9895=CLOSED_SHELL('',(#9751,#9752,#9753,#9754,#9755,#9756,#9757,#9758,
#9759,#9760,#9761,#9762,#9763,#9764,#9765,#9766,#9767,#9768,#9769,#9770,
#9771,#9772,#9773,#9774,#9775,#9776,#9777,#9778,#9779,#9780,#9781,#9782,
#9783,#9784,#9785,#9786,#9787,#9788,#9789,#9790,#9791,#9792,#9793,#9794,
#9795,#9796,#9797,#9798,#9799,#9800,#9801,#9802,#9803,#9804,#9805,#9806,
#9807,#9808,#9809,#9810,#9811,#9812,#9813,#9814,#9815,#9816,#9817,#9818,
#9819,#9820,#9821,#9822,#9823,#9824,#9825,#9826));
#10487=AXIS2_PLACEMENT_3D('',#19088,#12089,#12090);
#10488=AXIS2_PLACEMENT_3D('',#19089,#12091,#12092);
#10489=AXIS2_PLACEMENT_3D('',#19105,#12094,#12095);
#10490=AXIS2_PLACEMENT_3D('',#19113,#12096,#12097);
#10491=AXIS2_PLACEMENT_3D('',#19161,#12099,#12100);
#10492=AXIS2_PLACEMENT_3D('',#19209,#12102,#12103);
#10493=AXIS2_PLACEMENT_3D('',#19260,#12105,#12106);
#10494=AXIS2_PLACEMENT_3D('',#19308,#12108,#12109);
#10495=AXIS2_PLACEMENT_3D('',#19356,#12111,#12112);
#10496=AXIS2_PLACEMENT_3D('',#19404,#12114,#12115);
#10497=AXIS2_PLACEMENT_3D('',#19458,#12117,#12118);
#10498=AXIS2_PLACEMENT_3D('',#19506,#12120,#12121);
#10499=AXIS2_PLACEMENT_3D('',#19554,#12123,#12124);
#10500=AXIS2_PLACEMENT_3D('',#19608,#12126,#12127);
#10501=AXIS2_PLACEMENT_3D('',#19656,#12129,#12130);
#10502=AXIS2_PLACEMENT_3D('',#19704,#12132,#12133);
#10503=AXIS2_PLACEMENT_3D('',#19752,#12135,#12136);
#10504=AXIS2_PLACEMENT_3D('',#19806,#12138,#12139);
#10505=AXIS2_PLACEMENT_3D('',#19854,#12141,#12142);
#10506=AXIS2_PLACEMENT_3D('',#19902,#12144,#12145);
#10507=AXIS2_PLACEMENT_3D('',#19956,#12147,#12148);
#10508=AXIS2_PLACEMENT_3D('',#20004,#12150,#12151);
#10509=AXIS2_PLACEMENT_3D('',#20052,#12153,#12154);
#10510=AXIS2_PLACEMENT_3D('',#20106,#12156,#12157);
#10511=AXIS2_PLACEMENT_3D('',#20154,#12159,#12160);
#10512=AXIS2_PLACEMENT_3D('',#20202,#12162,#12163);
#10513=AXIS2_PLACEMENT_3D('',#20250,#12165,#12166);
#10514=AXIS2_PLACEMENT_3D('',#20304,#12168,#12169);
#10515=AXIS2_PLACEMENT_3D('',#20352,#12171,#12172);
#10516=AXIS2_PLACEMENT_3D('',#20400,#12174,#12175);
#10517=AXIS2_PLACEMENT_3D('',#20454,#12177,#12178);
#10518=AXIS2_PLACEMENT_3D('',#20502,#12180,#12181);
#10519=AXIS2_PLACEMENT_3D('',#20550,#12183,#12184);
#10520=AXIS2_PLACEMENT_3D('',#20566,#12186,#12187);
#10521=AXIS2_PLACEMENT_3D('',#20576,#12188,#12189);
#10522=AXIS2_PLACEMENT_3D('',#20600,#12191,#12192);
#10523=AXIS2_PLACEMENT_3D('',#20624,#12194,#12195);
#10524=AXIS2_PLACEMENT_3D('',#20649,#12197,#12198);
#10525=AXIS2_PLACEMENT_3D('',#20674,#12200,#12201);
#10526=AXIS2_PLACEMENT_3D('',#20698,#12203,#12204);
#10527=AXIS2_PLACEMENT_3D('',#20723,#12206,#12207);
#10528=AXIS2_PLACEMENT_3D('',#20748,#12209,#12210);
#10529=AXIS2_PLACEMENT_3D('',#20772,#12212,#12213);
#10530=AXIS2_PLACEMENT_3D('',#20796,#12215,#12216);
#10531=AXIS2_PLACEMENT_3D('',#20821,#12218,#12219);
#10532=AXIS2_PLACEMENT_3D('',#20846,#12221,#12222);
#10533=AXIS2_PLACEMENT_3D('',#20870,#12224,#12225);
#10534=AXIS2_PLACEMENT_3D('',#20895,#12227,#12228);
#10535=AXIS2_PLACEMENT_3D('',#20920,#12230,#12231);
#10536=AXIS2_PLACEMENT_3D('',#20944,#12233,#12234);
#10537=AXIS2_PLACEMENT_3D('',#20969,#12236,#12237);
#10538=AXIS2_PLACEMENT_3D('',#20994,#12239,#12240);
#10539=AXIS2_PLACEMENT_3D('',#21018,#12242,#12243);
#10540=AXIS2_PLACEMENT_3D('',#21042,#12245,#12246);
#10541=AXIS2_PLACEMENT_3D('',#21067,#12248,#12249);
#10542=AXIS2_PLACEMENT_3D('',#21092,#12251,#12252);
#10543=AXIS2_PLACEMENT_3D('',#21116,#12254,#12255);
#10544=AXIS2_PLACEMENT_3D('',#21141,#12257,#12258);
#10545=AXIS2_PLACEMENT_3D('',#21166,#12260,#12261);
#10546=AXIS2_PLACEMENT_3D('',#21190,#12263,#12264);
#10547=AXIS2_PLACEMENT_3D('',#21215,#12266,#12267);
#10548=AXIS2_PLACEMENT_3D('',#21239,#12269,#12270);
#10549=AXIS2_PLACEMENT_3D('',#21264,#12272,#12273);
#10550=AXIS2_PLACEMENT_3D('',#21288,#12275,#12276);
#10551=AXIS2_PLACEMENT_3D('',#21450,#12277,#12278);
#10552=AXIS2_PLACEMENT_3D('',#21469,#12280,#12281);
#10553=AXIS2_PLACEMENT_3D('',#22331,#12282,#12283);
#10554=AXIS2_PLACEMENT_3D('',#22342,#12284,#12285);
#10555=AXIS2_PLACEMENT_3D('',#23209,#12286,#12287);
#10556=AXIS2_PLACEMENT_3D('',#23210,#12288,#12289);
#10557=AXIS2_PLACEMENT_3D('',#23219,#12294,#12295);
#10558=AXIS2_PLACEMENT_3D('',#23225,#12299,#12300);
#10559=AXIS2_PLACEMENT_3D('',#23231,#12304,#12305);
#10560=AXIS2_PLACEMENT_3D('',#23237,#12309,#12310);
#10561=AXIS2_PLACEMENT_3D('',#23243,#12314,#12315);
#10562=AXIS2_PLACEMENT_3D('',#23246,#12318,#12319);
#10563=AXIS2_PLACEMENT_3D('',#23247,#12320,#12321);
#10564=AXIS2_PLACEMENT_3D('',#23249,#12322,#12323);
#10565=AXIS2_PLACEMENT_3D('',#23250,#12324,#12325);
#10566=AXIS2_PLACEMENT_3D('',#23253,#12327,#12328);
#10567=AXIS2_PLACEMENT_3D('',#23254,#12329,#12330);
#10568=AXIS2_PLACEMENT_3D('',#23255,#12331,#12332);
#12089=DIRECTION('axis',(0.,0.,1.));
#12090=DIRECTION('refdir',(1.,0.,0.));
#12091=DIRECTION('center_axis',(0.,0.,1.));
#12092=DIRECTION('ref_axis',(1.,0.,0.));
#12093=DIRECTION('',(0.,0.,-1.));
#12094=DIRECTION('center_axis',(0.,0.,-1.));
#12095=DIRECTION('ref_axis',(1.,0.,0.));
#12096=DIRECTION('center_axis',(0.,0.,1.));
#12097=DIRECTION('ref_axis',(1.,0.,0.));
#12098=DIRECTION('',(0.,0.,-1.));
#12099=DIRECTION('center_axis',(0.,0.,1.));
#12100=DIRECTION('ref_axis',(1.,0.,0.));
#12101=DIRECTION('',(0.,0.,-1.));
#12102=DIRECTION('center_axis',(0.,0.,1.));
#12103=DIRECTION('ref_axis',(1.,0.,0.));
#12104=DIRECTION('',(0.,0.,-1.));
#12105=DIRECTION('center_axis',(0.,0.,1.));
#12106=DIRECTION('ref_axis',(1.,0.,0.));
#12107=DIRECTION('',(0.,0.,-1.));
#12108=DIRECTION('center_axis',(0.,0.,1.));
#12109=DIRECTION('ref_axis',(1.,0.,0.));
#12110=DIRECTION('',(0.,0.,-1.));
#12111=DIRECTION('center_axis',(0.,0.,1.));
#12112=DIRECTION('ref_axis',(1.,0.,0.));
#12113=DIRECTION('',(0.,0.,-1.));
#12114=DIRECTION('center_axis',(0.,0.,1.));
#12115=DIRECTION('ref_axis',(1.,0.,0.));
#12116=DIRECTION('',(0.,0.,-1.));
#12117=DIRECTION('center_axis',(0.,0.,1.));
#12118=DIRECTION('ref_axis',(1.,0.,0.));
#12119=DIRECTION('',(0.,0.,-1.));
#12120=DIRECTION('center_axis',(0.,0.,1.));
#12121=DIRECTION('ref_axis',(1.,0.,0.));
#12122=DIRECTION('',(0.,0.,-1.));
#12123=DIRECTION('center_axis',(0.,0.,1.));
#12124=DIRECTION('ref_axis',(1.,0.,0.));
#12125=DIRECTION('',(0.,0.,-1.));
#12126=DIRECTION('center_axis',(0.,0.,1.));
#12127=DIRECTION('ref_axis',(1.,0.,0.));
#12128=DIRECTION('',(0.,0.,-1.));
#12129=DIRECTION('center_axis',(0.,0.,1.));
#12130=DIRECTION('ref_axis',(1.,0.,0.));
#12131=DIRECTION('',(0.,0.,-1.));
#12132=DIRECTION('center_axis',(0.,0.,1.));
#12133=DIRECTION('ref_axis',(1.,0.,0.));
#12134=DIRECTION('',(0.,0.,-1.));
#12135=DIRECTION('center_axis',(0.,0.,1.));
#12136=DIRECTION('ref_axis',(1.,0.,0.));
#12137=DIRECTION('',(0.,0.,-1.));
#12138=DIRECTION('center_axis',(0.,0.,1.));
#12139=DIRECTION('ref_axis',(1.,0.,0.));
#12140=DIRECTION('',(0.,0.,-1.));
#12141=DIRECTION('center_axis',(0.,0.,1.));
#12142=DIRECTION('ref_axis',(1.,0.,0.));
#12143=DIRECTION('',(0.,0.,-1.));
#12144=DIRECTION('center_axis',(0.,0.,1.));
#12145=DIRECTION('ref_axis',(1.,0.,0.));
#12146=DIRECTION('',(0.,0.,-1.));
#12147=DIRECTION('center_axis',(0.,0.,1.));
#12148=DIRECTION('ref_axis',(1.,0.,0.));
#12149=DIRECTION('',(0.,0.,-1.));
#12150=DIRECTION('center_axis',(0.,0.,1.));
#12151=DIRECTION('ref_axis',(1.,0.,0.));
#12152=DIRECTION('',(0.,0.,-1.));
#12153=DIRECTION('center_axis',(0.,0.,1.));
#12154=DIRECTION('ref_axis',(1.,0.,0.));
#12155=DIRECTION('',(0.,0.,-1.));
#12156=DIRECTION('center_axis',(0.,0.,1.));
#12157=DIRECTION('ref_axis',(1.,0.,0.));
#12158=DIRECTION('',(0.,0.,-1.));
#12159=DIRECTION('center_axis',(0.,0.,1.));
#12160=DIRECTION('ref_axis',(1.,0.,0.));
#12161=DIRECTION('',(0.,0.,-1.));
#12162=DIRECTION('center_axis',(0.,0.,1.));
#12163=DIRECTION('ref_axis',(1.,0.,0.));
#12164=DIRECTION('',(0.,0.,-1.));
#12165=DIRECTION('center_axis',(0.,0.,1.));
#12166=DIRECTION('ref_axis',(1.,0.,0.));
#12167=DIRECTION('',(0.,0.,-1.));
#12168=DIRECTION('center_axis',(0.,0.,1.));
#12169=DIRECTION('ref_axis',(1.,0.,0.));
#12170=DIRECTION('',(0.,0.,-1.));
#12171=DIRECTION('center_axis',(0.,0.,1.));
#12172=DIRECTION('ref_axis',(1.,0.,0.));
#12173=DIRECTION('',(0.,0.,-1.));
#12174=DIRECTION('center_axis',(0.,0.,1.));
#12175=DIRECTION('ref_axis',(1.,0.,0.));
#12176=DIRECTION('',(0.,0.,-1.));
#12177=DIRECTION('center_axis',(0.,0.,1.));
#12178=DIRECTION('ref_axis',(1.,0.,0.));
#12179=DIRECTION('',(0.,0.,-1.));
#12180=DIRECTION('center_axis',(0.,0.,1.));
#12181=DIRECTION('ref_axis',(1.,0.,0.));
#12182=DIRECTION('',(0.,0.,-1.));
#12183=DIRECTION('center_axis',(0.,0.,1.));
#12184=DIRECTION('ref_axis',(1.,-2.42503376499884E-13,0.));
#12185=DIRECTION('',(0.,0.,1.));
#12186=DIRECTION('center_axis',(0.,0.,-1.));
#12187=DIRECTION('ref_axis',(1.,-2.42503376499884E-13,0.));
#12188=DIRECTION('center_axis',(0.,0.,1.));
#12189=DIRECTION('ref_axis',(1.,-2.42503376499884E-13,0.));
#12190=DIRECTION('',(0.,0.,1.));
#12191=DIRECTION('center_axis',(0.,0.,1.));
#12192=DIRECTION('ref_axis',(1.,-2.42503376499884E-13,0.));
#12193=DIRECTION('',(0.,0.,1.));
#12194=DIRECTION('center_axis',(0.,0.,1.));
#12195=DIRECTION('ref_axis',(1.,-2.42503376499884E-13,0.));
#12196=DIRECTION('',(0.,0.,1.));
#12197=DIRECTION('center_axis',(0.,0.,1.));
#12198=DIRECTION('ref_axis',(1.,-2.42503376499884E-13,0.));
#12199=DIRECTION('',(0.,0.,1.));
#12200=DIRECTION('center_axis',(0.,0.,1.));
#12201=DIRECTION('ref_axis',(1.,-2.42503376499884E-13,0.));
#12202=DIRECTION('',(0.,0.,1.));
#12203=DIRECTION('center_axis',(0.,0.,1.));
#12204=DIRECTION('ref_axis',(1.,-2.42503376499884E-13,0.));
#12205=DIRECTION('',(0.,0.,1.));
#12206=DIRECTION('center_axis',(0.,0.,1.));
#12207=DIRECTION('ref_axis',(1.,-2.42503376499884E-13,0.));
#12208=DIRECTION('',(0.,0.,1.));
#12209=DIRECTION('center_axis',(0.,0.,1.));
#12210=DIRECTION('ref_axis',(1.,-2.42503376499884E-13,0.));
#12211=DIRECTION('',(0.,0.,1.));
#12212=DIRECTION('center_axis',(0.,0.,1.));
#12213=DIRECTION('ref_axis',(1.,-2.42503376499884E-13,0.));
#12214=DIRECTION('',(0.,0.,1.));
#12215=DIRECTION('center_axis',(0.,0.,1.));
#12216=DIRECTION('ref_axis',(1.,-2.42503376499884E-13,0.));
#12217=DIRECTION('',(0.,0.,1.));
#12218=DIRECTION('center_axis',(0.,0.,1.));
#12219=DIRECTION('ref_axis',(1.,-2.42503376499884E-13,0.));
#12220=DIRECTION('',(0.,0.,1.));
#12221=DIRECTION('center_axis',(0.,0.,1.));
#12222=DIRECTION('ref_axis',(1.,-2.42503376499884E-13,0.));
#12223=DIRECTION('',(0.,0.,1.));
#12224=DIRECTION('center_axis',(0.,0.,1.));
#12225=DIRECTION('ref_axis',(1.,-2.42503376499884E-13,0.));
#12226=DIRECTION('',(0.,0.,1.));
#12227=DIRECTION('center_axis',(0.,0.,1.));
#12228=DIRECTION('ref_axis',(1.,-2.42503376499884E-13,0.));
#12229=DIRECTION('',(0.,0.,1.));
#12230=DIRECTION('center_axis',(0.,0.,1.));
#12231=DIRECTION('ref_axis',(1.,-2.42503376499884E-13,0.));
#12232=DIRECTION('',(0.,0.,1.));
#12233=DIRECTION('center_axis',(0.,0.,1.));
#12234=DIRECTION('ref_axis',(1.,-2.42503376499884E-13,0.));
#12235=DIRECTION('',(0.,0.,1.));
#12236=DIRECTION('center_axis',(0.,0.,1.));
#12237=DIRECTION('ref_axis',(1.,-2.42503376499884E-13,0.));
#12238=DIRECTION('',(0.,0.,1.));
#12239=DIRECTION('center_axis',(0.,0.,1.));
#12240=DIRECTION('ref_axis',(1.,-2.42503376499884E-13,0.));
#12241=DIRECTION('',(0.,0.,1.));
#12242=DIRECTION('center_axis',(0.,0.,1.));
#12243=DIRECTION('ref_axis',(1.,-2.42503376499884E-13,0.));
#12244=DIRECTION('',(0.,0.,1.));
#12245=DIRECTION('center_axis',(0.,0.,1.));
#12246=DIRECTION('ref_axis',(1.,-2.42503376499884E-13,0.));
#12247=DIRECTION('',(0.,0.,1.));
#12248=DIRECTION('center_axis',(0.,0.,1.));
#12249=DIRECTION('ref_axis',(1.,-2.42503376499884E-13,0.));
#12250=DIRECTION('',(0.,0.,1.));
#12251=DIRECTION('center_axis',(0.,0.,1.));
#12252=DIRECTION('ref_axis',(1.,-2.42503376499884E-13,0.));
#12253=DIRECTION('',(0.,0.,1.));
#12254=DIRECTION('center_axis',(0.,0.,1.));
#12255=DIRECTION('ref_axis',(1.,-2.42503376499884E-13,0.));
#12256=DIRECTION('',(0.,0.,1.));
#12257=DIRECTION('center_axis',(0.,0.,1.));
#12258=DIRECTION('ref_axis',(1.,-2.42503376499884E-13,0.));
#12259=DIRECTION('',(0.,0.,1.));
#12260=DIRECTION('center_axis',(0.,0.,1.));
#12261=DIRECTION('ref_axis',(1.,-2.42503376499884E-13,0.));
#12262=DIRECTION('',(0.,0.,1.));
#12263=DIRECTION('center_axis',(0.,0.,1.));
#12264=DIRECTION('ref_axis',(1.,-2.42503376499884E-13,0.));
#12265=DIRECTION('',(0.,0.,1.));
#12266=DIRECTION('center_axis',(0.,0.,1.));
#12267=DIRECTION('ref_axis',(1.,-2.42503376499884E-13,0.));
#12268=DIRECTION('',(0.,0.,1.));
#12269=DIRECTION('center_axis',(0.,0.,1.));
#12270=DIRECTION('ref_axis',(1.,-2.42503376499884E-13,0.));
#12271=DIRECTION('',(0.,0.,1.));
#12272=DIRECTION('center_axis',(0.,0.,1.));
#12273=DIRECTION('ref_axis',(1.,-2.42503376499884E-13,0.));
#12274=DIRECTION('',(0.,0.,1.));
#12275=DIRECTION('center_axis',(0.,0.,-1.));
#12276=DIRECTION('ref_axis',(1.,0.,0.));
#12277=DIRECTION('center_axis',(0.,0.,-1.));
#12278=DIRECTION('ref_axis',(1.,0.,0.));
#12279=DIRECTION('',(0.707106781186547,8.65956056235493E-17,0.707106781186548));
#12280=DIRECTION('center_axis',(0.,0.,1.));
#12281=DIRECTION('ref_axis',(1.,0.,0.));
#12282=DIRECTION('center_axis',(0.,0.,1.));
#12283=DIRECTION('ref_axis',(1.,-2.42503376499884E-13,0.));
#12284=DIRECTION('center_axis',(0.,0.,-1.));
#12285=DIRECTION('ref_axis',(1.,-2.42503376499884E-13,0.));
#12286=DIRECTION('center_axis',(0.,0.,1.));
#12287=DIRECTION('ref_axis',(1.,0.,0.));
#12288=DIRECTION('center_axis',(-1.92296268638356E-16,-1.,0.));
#12289=DIRECTION('ref_axis',(1.,-1.92296268638356E-16,0.));
#12290=DIRECTION('',(1.,-1.92296268638356E-16,0.));
#12291=DIRECTION('',(0.,0.,1.));
#12292=DIRECTION('',(1.,-1.92296268638356E-16,0.));
#12293=DIRECTION('',(0.,0.,1.));
#12294=DIRECTION('center_axis',(-0.866025403784439,-0.5,0.));
#12295=DIRECTION('ref_axis',(0.5,-0.866025403784439,0.));
#12296=DIRECTION('',(0.5,-0.866025403784439,0.));
#12297=DIRECTION('',(0.,0.,1.));
#12298=DIRECTION('',(0.5,-0.866025403784439,0.));
#12299=DIRECTION('center_axis',(-0.866025403784439,0.5,0.));
#12300=DIRECTION('ref_axis',(-0.5,-0.866025403784439,0.));
#12301=DIRECTION('',(-0.5,-0.866025403784439,0.));
#12302=DIRECTION('',(0.,0.,1.));
#12303=DIRECTION('',(-0.5,-0.866025403784438,0.));
#12304=DIRECTION('center_axis',(1.92296268638356E-16,1.,0.));
#12305=DIRECTION('ref_axis',(-1.,1.92296268638356E-16,0.));
#12306=DIRECTION('',(-1.,1.92296268638356E-16,0.));
#12307=DIRECTION('',(0.,0.,1.));
#12308=DIRECTION('',(-1.,1.92296268638356E-16,0.));
#12309=DIRECTION('center_axis',(0.866025403784439,0.5,0.));
#12310=DIRECTION('ref_axis',(-0.5,0.866025403784439,0.));
#12311=DIRECTION('',(-0.5,0.866025403784439,0.));
#12312=DIRECTION('',(0.,0.,1.));
#12313=DIRECTION('',(-0.5,0.866025403784439,0.));
#12314=DIRECTION('center_axis',(0.866025403784439,-0.5,0.));
#12315=DIRECTION('ref_axis',(0.5,0.866025403784439,0.));
#12316=DIRECTION('',(0.5,0.866025403784439,0.));
#12317=DIRECTION('',(0.5,0.866025403784439,0.));
#12318=DIRECTION('center_axis',(0.,0.,1.));
#12319=DIRECTION('ref_axis',(1.,0.,0.));
#12320=DIRECTION('center_axis',(0.,0.,1.));
#12321=DIRECTION('ref_axis',(1.,0.,0.));
#12322=DIRECTION('center_axis',(0.,0.,1.));
#12323=DIRECTION('ref_axis',(1.,0.,0.));
#12324=DIRECTION('center_axis',(0.,0.,1.));
#12325=DIRECTION('ref_axis',(1.,0.,0.));
#12326=DIRECTION('',(0.,0.,-1.));
#12327=DIRECTION('center_axis',(0.,0.,1.));
#12328=DIRECTION('ref_axis',(1.,0.,0.));
#12329=DIRECTION('center_axis',(0.,0.,1.));
#12330=DIRECTION('ref_axis',(1.,0.,0.));
#12331=DIRECTION('center_axis',(0.,0.,1.));
#12332=DIRECTION('ref_axis',(1.,0.,0.));
#19088=CARTESIAN_POINT('',(0.,0.,0.));
#19089=CARTESIAN_POINT('Origin',(0.,0.,0.));
#19090=CARTESIAN_POINT('',(-0.14652705620645,9.44412402177196E-5,0.0160655045842905));
#19091=CARTESIAN_POINT('',(-0.146479946776166,0.000162062070299865,0.00893449541571059));
#19092=CARTESIAN_POINT('',(-0.14635,-1.79227059055215E-17,0.));
#19093=CARTESIAN_POINT('',(0.0634007094575209,0.131904027763685,0.));
#19094=CARTESIAN_POINT('Ctrl Pts',(-0.14652705620645,9.44412402177196E-5,
0.0160655045842905));
#19095=CARTESIAN_POINT('Ctrl Pts',(-0.146560923555419,0.00502618404349199,
0.0157963945919035));
#19096=CARTESIAN_POINT('Ctrl Pts',(-0.146333578783787,0.00995455679532004,
0.0155272845995164));
#19097=CARTESIAN_POINT('Ctrl Pts',(-0.14583475180505,0.0148550342388422,
0.0152581746071293));
#19098=CARTESIAN_POINT('Ctrl Pts',(-0.140929468554047,0.0630445487404258,
0.0126118447280274));
#19099=CARTESIAN_POINT('Ctrl Pts',(-0.10977174472993,0.108536575508351,
0.0099655148489255));
#19100=CARTESIAN_POINT('Ctrl Pts',(-0.0666135938566871,0.13056551637767,
0.00731918496982359));
#19101=CARTESIAN_POINT('Ctrl Pts',(-0.0268248419338395,0.150874636338504,
0.00487945664654906));
#19102=CARTESIAN_POINT('Ctrl Pts',(0.0231637104697219,0.151241233100125,
0.00243972832327453));
#19103=CARTESIAN_POINT('Ctrl Pts',(0.0635546915223951,0.132092229195826,
-2.16840434497101E-19));
#19104=CARTESIAN_POINT('',(-0.0634007094575146,0.131904027763688,0.));
#19105=CARTESIAN_POINT('Origin',(0.,0.,0.));
#19106=CARTESIAN_POINT('Ctrl Pts',(-0.0634007094575145,0.131904027763688,
-3.88578058618805E-16));
#19107=CARTESIAN_POINT('Ctrl Pts',(-0.107282641710421,0.110811831533068,
0.00264738937425961));
#19108=CARTESIAN_POINT('Ctrl Pts',(-0.139432201149969,0.0662847592091173,
0.00529477874851962));
#19109=CARTESIAN_POINT('Ctrl Pts',(-0.145436119191498,0.0182745223106641,
0.00794216812277962));
#19110=CARTESIAN_POINT('Ctrl Pts',(-0.146186273512714,0.0122759249909008,
0.00827294388708994));
#19111=CARTESIAN_POINT('Ctrl Pts',(-0.146528267289359,0.00622295186417552,
0.00860371965140026));
#19112=CARTESIAN_POINT('Ctrl Pts',(-0.146479946776166,0.000162062070299865,
0.00893449541571059));
#19113=CARTESIAN_POINT('Origin',(0.,0.,0.));
#19114=CARTESIAN_POINT('',(-0.146148830924315,7.59978318484386E-5,0.0660655045842905));
#19115=CARTESIAN_POINT('',(-0.146133770585873,6.2751561688711E-5,0.0589344954157103));
#19116=CARTESIAN_POINT('',(-0.14635,-1.79227059055215E-17,0.));
#19117=CARTESIAN_POINT('Ctrl Pts',(-0.146148830924315,7.59978318484386E-5,
0.0660655045842905));
#19118=CARTESIAN_POINT('Ctrl Pts',(-0.146240443598182,0.0195917497831913,
0.0650077071998482));
#19119=CARTESIAN_POINT('Ctrl Pts',(-0.142607114239671,0.0390747476468127,
0.0639499098154059));
#19120=CARTESIAN_POINT('Ctrl Pts',(-0.135087779856993,0.056920264102034,
0.0628921124309636));
#19121=CARTESIAN_POINT('Ctrl Pts',(-0.116276389754784,0.10156503643559,
0.0602457825518617));
#19122=CARTESIAN_POINT('Ctrl Pts',(-0.073143724514267,0.135961331060063,
0.0575994526727599));
#19123=CARTESIAN_POINT('Ctrl Pts',(-0.025432083612881,0.144366623974243,
0.054953122793658));
#19124=CARTESIAN_POINT('Ctrl Pts',(0.0222795572885053,0.152771916888423,
0.0523067929145561));
#19125=CARTESIAN_POINT('Ctrl Pts',(0.0745701738507606,0.135186208092309,
0.0496604630354541));
#19126=CARTESIAN_POINT('Ctrl Pts',(0.107505148494886,0.0996564726649905,
0.0470141331563522));
#19127=CARTESIAN_POINT('Ctrl Pts',(0.140440123139012,0.0641267372376721,
0.0443678032772503));
#19128=CARTESIAN_POINT('Ctrl Pts',(0.154019455865009,0.010652975179149,
0.0417214733981484));
#19129=CARTESIAN_POINT('Ctrl Pts',(0.14202839331759,-0.0362847016460775,
0.0390751435190465));
#19130=CARTESIAN_POINT('Ctrl Pts',(0.130037330770172,-0.0832223784713041,
0.0364288136399446));
#19131=CARTESIAN_POINT('Ctrl Pts',(0.0924758729493388,-0.123623970063234,
0.0337824837608427));
#19132=CARTESIAN_POINT('Ctrl Pts',(0.0465351214488668,-0.139005253038876,
0.0311361538817407));
#19133=CARTESIAN_POINT('Ctrl Pts',(0.000594369948394902,-0.154386536014517,
0.0284898240026388));
#19134=CARTESIAN_POINT('Ctrl Pts',(-0.0537256752317158,-0.144747510373871,
0.025843494123537));
#19135=CARTESIAN_POINT('Ctrl Pts',(-0.0915592764828275,-0.114484496435928,
0.0231971642444351));
#19136=CARTESIAN_POINT('Ctrl Pts',(-0.125545511528741,-0.0872989822136326,
0.0208199443577202));
#19137=CARTESIAN_POINT('Ctrl Pts',(-0.146227884351973,-0.0434707826450544,
0.0184427244710054));
#19138=CARTESIAN_POINT('Ctrl Pts',(-0.14652705620645,9.44412402177196E-5,
0.0160655045842905));
#19139=CARTESIAN_POINT('Ctrl Pts',(-0.146479946776166,0.000162062070299865,
0.00893449541571059));
#19140=CARTESIAN_POINT('Ctrl Pts',(-0.146141530330399,-0.0422858476614564,
0.0112511090256603));
#19141=CARTESIAN_POINT('Ctrl Pts',(-0.126658161292025,-0.0851220706608281,
0.0135677226356099));
#19142=CARTESIAN_POINT('Ctrl Pts',(-0.0941604943243988,-0.112386678841155,
0.0158843362455596));
#19143=CARTESIAN_POINT('Ctrl Pts',(-0.0570226747722624,-0.143544241621566,
0.0185317256198196));
#19144=CARTESIAN_POINT('Ctrl Pts',(-0.00288875902448078,-0.154365965709432,
0.0211791149940796));
#19145=CARTESIAN_POINT('Ctrl Pts',(0.0434083729543798,-0.140002007265973,
0.0238265043683396));
#19146=CARTESIAN_POINT('Ctrl Pts',(0.0897055049332404,-0.125638048822514,
0.0264738937425996));
#19147=CARTESIAN_POINT('Ctrl Pts',(0.12816585314318,-0.0860884078477292,
0.0291212831168596));
#19148=CARTESIAN_POINT('Ctrl Pts',(0.141191617966992,-0.0394144013492358,
0.0317686724911196));
#19149=CARTESIAN_POINT('Ctrl Pts',(0.154217382790803,0.00725960514925768,
0.0344160618653796));
#19150=CARTESIAN_POINT('Ctrl Pts',(0.141808564228487,0.0610579771714599,
0.0370634512396396));
#19151=CARTESIAN_POINT('Ctrl Pts',(0.109639063769471,0.0973098477439542,
0.0397108406138996));
#19152=CARTESIAN_POINT('Ctrl Pts',(0.0774695633104545,0.133561718316448,
0.0423582299881596));
#19153=CARTESIAN_POINT('Ctrl Pts',(0.0255393809547383,0.152267087439235,
0.0450056193624196));
#19154=CARTESIAN_POINT('Ctrl Pts',(-0.0223595433272462,0.144872892294413,
0.0476530087366796));
#19155=CARTESIAN_POINT('Ctrl Pts',(-0.070258467609231,0.137478697149591,
0.0503003981109396));
#19156=CARTESIAN_POINT('Ctrl Pts',(-0.114126133817484,0.10398493773716,
0.0529477874851996));
#19157=CARTESIAN_POINT('Ctrl Pts',(-0.133871661545403,0.059725601630819,
0.0555951768594596));
#19158=CARTESIAN_POINT('Ctrl Pts',(-0.142173753131161,0.0411165744656389,
0.0567082830448765));
#19159=CARTESIAN_POINT('Ctrl Pts',(-0.146211489678532,0.0206043892842972,
0.0578213892302934));
#19160=CARTESIAN_POINT('Ctrl Pts',(-0.146133770585873,6.2751561688711E-5,
0.0589344954157103));
#19161=CARTESIAN_POINT('Origin',(0.,0.,0.));
#19162=CARTESIAN_POINT('',(-0.146252097264499,-0.000124487410312429,0.116065504584291));
#19163=CARTESIAN_POINT('',(-0.146276374479508,-0.000129480650117819,0.10893449541571));
#19164=CARTESIAN_POINT('',(-0.14635,-1.79227059055215E-17,0.));
#19165=CARTESIAN_POINT('Ctrl Pts',(-0.146252097264499,-0.000124487410312429,
0.116065504584291));
#19166=CARTESIAN_POINT('Ctrl Pts',(-0.145977101830714,0.0338815411246725,
0.114219019807793));
#19167=CARTESIAN_POINT('Ctrl Pts',(-0.134160879762789,0.0680598926014691,
0.112372535031295));
#19168=CARTESIAN_POINT('Ctrl Pts',(-0.112484833627769,0.0939988017516943,
0.110526050254798));
#19169=CARTESIAN_POINT('Ctrl Pts',(-0.0814193359437304,0.131173714423195,
0.107879720375696));
#19170=CARTESIAN_POINT('Ctrl Pts',(-0.0301019434218634,0.151424966146533,
0.105233390496594));
#19171=CARTESIAN_POINT('Ctrl Pts',(0.0179785702873004,0.145483266051774,
0.102587060617492));
#19172=CARTESIAN_POINT('Ctrl Pts',(0.0660590839964643,0.139541565957016,
0.0999407307383904));
#19173=CARTESIAN_POINT('Ctrl Pts',(0.110902718892925,0.107406914044162,
0.0972944008592884));
#19174=CARTESIAN_POINT('Ctrl Pts',(0.131983829661647,0.0637877973597534,
0.0946480709801865));
#19175=CARTESIAN_POINT('Ctrl Pts',(0.15306494043037,0.0201686806753445,
0.0920017411010846));
#19176=CARTESIAN_POINT('Ctrl Pts',(0.150383527071356,-0.0349349007806195,
0.0893554112219828));
#19177=CARTESIAN_POINT('Ctrl Pts',(0.125166930059577,-0.0763010783846813,
0.0867090813428809));
#19178=CARTESIAN_POINT('Ctrl Pts',(0.0999503330477985,-0.117667255988743,
0.084062751463779));
#19179=CARTESIAN_POINT('Ctrl Pts',(0.0521985523832557,-0.145296029740903,
0.081416421584677));
#19180=CARTESIAN_POINT('Ctrl Pts',(0.00376830011669856,-0.146541450754272,
0.0787700917055751));
#19181=CARTESIAN_POINT('Ctrl Pts',(-0.0446619521498586,-0.147786871767642,
0.0761237618264732));
#19182=CARTESIAN_POINT('Ctrl Pts',(-0.09377067601843,-0.122648940042221,
0.0734774319473713));
#19183=CARTESIAN_POINT('Ctrl Pts',(-0.121079980470766,-0.0826333491581908,
0.0708311020682694));
#19184=CARTESIAN_POINT('Ctrl Pts',(-0.137473143648068,-0.0586128871159229,
0.0692425695736098));
#19185=CARTESIAN_POINT('Ctrl Pts',(-0.146011252866834,-0.02923151094855,
0.0676540370789502));
#19186=CARTESIAN_POINT('Ctrl Pts',(-0.146148830924315,7.59978318484386E-5,
0.0660655045842905));
#19187=CARTESIAN_POINT('Ctrl Pts',(-0.146133770585873,6.2751561688711E-5,
0.0589344954157103));
#19188=CARTESIAN_POINT('Ctrl Pts',(-0.146026644150963,-0.0282514289199324,
0.0604687786045534));
#19189=CARTESIAN_POINT('Ctrl Pts',(-0.138100435392092,-0.0566215672018456,
0.0620030617933965));
#19190=CARTESIAN_POINT('Ctrl Pts',(-0.122745086057252,-0.0801407530065182,
0.0635373449822396));
#19191=CARTESIAN_POINT('Ctrl Pts',(-0.0962495935935968,-0.120722858737265,
0.0661847343564996));
#19192=CARTESIAN_POINT('Ctrl Pts',(-0.0476352194187008,-0.146862157398507,
0.0688321237307596));
#19193=CARTESIAN_POINT('Ctrl Pts',(0.00082938917649622,-0.146587691816784,
0.0714795131050196));
#19194=CARTESIAN_POINT('Ctrl Pts',(0.0492939977716932,-0.146313226235061,
0.0741269024792796));
#19195=CARTESIAN_POINT('Ctrl Pts',(0.0976088407871913,-0.119624996410372,
0.0767742918535397));
#19196=CARTESIAN_POINT('Ctrl Pts',(0.123643642180798,-0.0787464320231966,
0.0794216812277997));
#19197=CARTESIAN_POINT('Ctrl Pts',(0.149678443574405,-0.0378678676360213,
0.0820690706020596));
#19198=CARTESIAN_POINT('Ctrl Pts',(0.153433203346121,0.0172010313136401,
0.0847164599763195));
#19199=CARTESIAN_POINT('Ctrl Pts',(0.133187835944515,0.06123527443138,0.0873638493505795));
#19200=CARTESIAN_POINT('Ctrl Pts',(0.11294246854291,0.10526951754912,0.0900112387248395));
#19201=CARTESIAN_POINT('Ctrl Pts',(0.0686969739679828,0.138269104834938,
0.0926586280990997));
#19202=CARTESIAN_POINT('Ctrl Pts',(0.0207181735233275,0.145118849380084,
0.0953060174733597));
#19203=CARTESIAN_POINT('Ctrl Pts',(-0.027260626921328,0.151968593925229,
0.0979534068476197));
#19204=CARTESIAN_POINT('Ctrl Pts',(-0.0789727332357116,0.132668495729702,
0.10060079622188));
#19205=CARTESIAN_POINT('Ctrl Pts',(-0.110731403441959,0.0960588230543748,
0.10324818559614));
#19206=CARTESIAN_POINT('Ctrl Pts',(-0.133469481440122,0.0698475998711364,
0.105143622202663));
#19207=CARTESIAN_POINT('Ctrl Pts',(-0.145979327216774,0.0347634013028336,
0.107039058809187));
#19208=CARTESIAN_POINT('Ctrl Pts',(-0.146276374479508,-0.000129480650117819,
0.10893449541571));
#19209=CARTESIAN_POINT('Origin',(0.,0.,0.));
#19210=CARTESIAN_POINT('',(-0.146589818999335,-3.81787486967988E-6,0.166065504584291));
#19211=CARTESIAN_POINT('',(-0.146589453522336,1.04004190909306E-5,0.15893449541571));
#19212=CARTESIAN_POINT('',(-0.14635,-1.79227059055215E-17,0.));
#19213=CARTESIAN_POINT('Ctrl Pts',(-0.146589818999335,-3.81787486967988E-6,
0.166065504584291));
#19214=CARTESIAN_POINT('Ctrl Pts',(-0.146571339149733,0.0482382848470949,
0.163430332415738));
#19215=CARTESIAN_POINT('Ctrl Pts',(-0.120433071521034,0.0964975486977609,
0.160795160247185));
#19216=CARTESIAN_POINT('Ctrl Pts',(-0.0800107885095625,0.122828684230981,
0.158159988078632));
#19217=CARTESIAN_POINT('Ctrl Pts',(-0.0394173515450545,0.149271309704865,
0.15551365819953));
#19218=CARTESIAN_POINT('Ctrl Pts',(0.0155813181737399,0.153599719825856,
0.152867328320428));
#19219=CARTESIAN_POINT('Ctrl Pts',(0.0598114643267532,0.133832733731537,
0.150220998441327));
#19220=CARTESIAN_POINT('Ctrl Pts',(0.104041610479766,0.114065747637217,
0.147574668562225));
#19221=CARTESIAN_POINT('Ctrl Pts',(0.137503233066998,0.0702033653275883,
0.144928338683123));
#19222=CARTESIAN_POINT('Ctrl Pts',(0.144880420813362,0.0223220882221681,
0.142282008804021));
#19223=CARTESIAN_POINT('Ctrl Pts',(0.152257608559726,-0.0255591888832524,
0.139635678924919));
#19224=CARTESIAN_POINT('Ctrl Pts',(0.133550361465222,-0.077459360784464,
0.136989349045817));
#19225=CARTESIAN_POINT('Ctrl Pts',(0.0973212811704284,-0.109622900294719,
0.134343019166715));
#19226=CARTESIAN_POINT('Ctrl Pts',(0.0610922008756344,-0.141786439804975,
0.131696689287613));
#19227=CARTESIAN_POINT('Ctrl Pts',(0.00734128738055008,-0.154213346924274,
0.129050359408511));
#19228=CARTESIAN_POINT('Ctrl Pts',(-0.0393288211819405,-0.141215634503184,
0.126404029529409));
#19229=CARTESIAN_POINT('Ctrl Pts',(-0.0859989297444312,-0.128217922082094,
0.123757699650308));
#19230=CARTESIAN_POINT('Ctrl Pts',(-0.125588233374328,-0.0897955901206149,
0.121111369771206));
#19231=CARTESIAN_POINT('Ctrl Pts',(-0.139976083766172,-0.043535137330043,
0.118465039892104));
#19232=CARTESIAN_POINT('Ctrl Pts',(-0.144324767489921,-0.0295530571287048,
0.117665194789499));
#19233=CARTESIAN_POINT('Ctrl Pts',(-0.146371217526823,-0.0148549394177889,
0.116865349686895));
#19234=CARTESIAN_POINT('Ctrl Pts',(-0.146252097264499,-0.000124487410312429,
0.116065504584291));
#19235=CARTESIAN_POINT('Ctrl Pts',(-0.146276374479508,-0.000129480650117819,
0.10893449541571));
#19236=CARTESIAN_POINT('Ctrl Pts',(-0.14639421831063,-0.0139720956278579,
0.109686448183447));
#19237=CARTESIAN_POINT('Ctrl Pts',(-0.14458995413065,-0.0277846002915201,
0.110438400951183));
#19238=CARTESIAN_POINT('Ctrl Pts',(-0.140739671041232,-0.041001045008257,
0.11119035371892));
#19239=CARTESIAN_POINT('Ctrl Pts',(-0.127184034336146,-0.0875319932404337,
0.11383774309318));
#19240=CARTESIAN_POINT('Ctrl Pts',(-0.0882675268278623,-0.12667464254966,
0.11648513246744));
#19241=CARTESIAN_POINT('Ctrl Pts',(-0.0418159243469935,-0.140499695546946,
0.1191325218417));
#19242=CARTESIAN_POINT('Ctrl Pts',(0.00463567813387508,-0.154324748544231,
0.12177991121596));
#19243=CARTESIAN_POINT('Ctrl Pts',(0.0586223755873289,-0.142832205229577,
0.12442730059022));
#19244=CARTESIAN_POINT('Ctrl Pts',(0.0954154960694136,-0.111286216216264,
0.12707468996448));
#19245=CARTESIAN_POINT('Ctrl Pts',(0.132208616551499,-0.0797402272029501,
0.12972207933874));
#19246=CARTESIAN_POINT('Ctrl Pts',(0.151808160062214,-0.0281407924909768,
0.132369468712999));
#19247=CARTESIAN_POINT('Ctrl Pts',(0.145236524363737,0.0198768833792122,
0.135016858087259));
#19248=CARTESIAN_POINT('Ctrl Pts',(0.138664888665259,0.0678945592494009,
0.13766424746152));
#19249=CARTESIAN_POINT('Ctrl Pts',(0.105922073757589,0.112330476277805,
0.14031163683578));
#19250=CARTESIAN_POINT('Ctrl Pts',(0.062005973158836,0.132830708741579,
0.14295902621004));
#19251=CARTESIAN_POINT('Ctrl Pts',(0.0180898725600832,0.153330941205352,
0.1456064155843));
#19252=CARTESIAN_POINT('Ctrl Pts',(-0.0369995137297515,0.149895489104495,
0.14825380495856));
#19253=CARTESIAN_POINT('Ctrl Pts',(-0.0780284182758478,0.124097962381086,
0.15090119433282));
#19254=CARTESIAN_POINT('Ctrl Pts',(-0.119057322821944,0.0983004356576776,
0.153548583707079));
#19255=CARTESIAN_POINT('Ctrl Pts',(-0.146025745624302,0.0501408343117172,
0.15619597308134));
#19256=CARTESIAN_POINT('Ctrl Pts',(-0.14658076309025,0.00167873146180186,
0.1588433624556));
#19257=CARTESIAN_POINT('Ctrl Pts',(-0.146587131676737,0.00112264969450139,
0.15887374010897));
#19258=CARTESIAN_POINT('Ctrl Pts',(-0.146590022522527,0.000566528098114988,
0.15890411776234));
#19259=CARTESIAN_POINT('Ctrl Pts',(-0.146589453522336,1.04004190909306E-5,
0.15893449541571));
#19260=CARTESIAN_POINT('Origin',(0.,0.,0.));
#19261=CARTESIAN_POINT('',(-0.146263250741535,0.000126870157254357,0.21606550458429));
#19262=CARTESIAN_POINT('',(-0.146245769975643,0.000123264779366826,0.20893449541571));
#19263=CARTESIAN_POINT('',(-0.14635,-1.79227059055215E-17,0.));
#19264=CARTESIAN_POINT('Ctrl Pts',(-0.146263250741535,0.000126870157254357,
0.21606550458429));
#19265=CARTESIAN_POINT('Ctrl Pts',(-0.146381923100139,0.0144435832128767,
0.215287974902784));
#19266=CARTESIAN_POINT('Ctrl Pts',(-0.144450237714319,0.0287289633064517,
0.214510445221278));
#19267=CARTESIAN_POINT('Ctrl Pts',(-0.140337374518256,0.0423560295890773,
0.213732915539772));
#19268=CARTESIAN_POINT('Ctrl Pts',(-0.126339204386259,0.0887358830222778,
0.21108658566067));
#19269=CARTESIAN_POINT('Ctrl Pts',(-0.0870745347363382,0.127489909020004,
0.208440255781569));
#19270=CARTESIAN_POINT('Ctrl Pts',(-0.0405154226099946,0.140879780169064,
0.205793925902467));
#19271=CARTESIAN_POINT('Ctrl Pts',(0.00604368951634975,0.154269651318124,
0.203147596023365));
#19272=CARTESIAN_POINT('Ctrl Pts',(0.0598972441191175,0.142295367618517,
0.200501266144263));
#19273=CARTESIAN_POINT('Ctrl Pts',(0.0963956219934077,0.110437747119808,
0.197854936265161));
#19274=CARTESIAN_POINT('Ctrl Pts',(0.132893999867697,0.0785801266211,0.195208606386059));
#19275=CARTESIAN_POINT('Ctrl Pts',(0.15203720101351,0.0268391693232909,
0.192562276506957));
#19276=CARTESIAN_POINT('Ctrl Pts',(0.145063081087281,-0.0211024746124516,
0.189915946627855));
#19277=CARTESIAN_POINT('Ctrl Pts',(0.138088961161051,-0.0690441185481943,
0.187269616748753));
#19278=CARTESIAN_POINT('Ctrl Pts',(0.10499752016278,-0.11318644912187,0.184623286869651));
#19279=CARTESIAN_POINT('Ctrl Pts',(0.060935231264163,-0.133324827106958,
0.181976956990549));
#19280=CARTESIAN_POINT('Ctrl Pts',(0.0168729423655461,-0.153463205092045,
0.179330627111448));
#19281=CARTESIAN_POINT('Ctrl Pts',(-0.0381601944334158,-0.149597630488544,
0.176684297232346));
#19282=CARTESIAN_POINT('Ctrl Pts',(-0.0789746466099193,-0.123497437688695,
0.174037967353244));
#19283=CARTESIAN_POINT('Ctrl Pts',(-0.119961184605052,-0.0972871987457574,
0.171380479763593));
#19284=CARTESIAN_POINT('Ctrl Pts',(-0.146608455341797,-0.0486544490602708,
0.168722992173942));
#19285=CARTESIAN_POINT('Ctrl Pts',(-0.146589818999335,-3.81787486967988E-6,
0.166065504584291));
#19286=CARTESIAN_POINT('Ctrl Pts',(-0.146589453522336,1.04004190909306E-5,
0.15893449541571));
#19287=CARTESIAN_POINT('Ctrl Pts',(-0.146540434588914,-0.0478995759235739,
0.1615515071366));
#19288=CARTESIAN_POINT('Ctrl Pts',(-0.120813506558866,-0.0958546957256878,
0.16416851885749));
#19289=CARTESIAN_POINT('Ctrl Pts',(-0.0808500697395765,-0.122278388912248,
0.16678553057838));
#19290=CARTESIAN_POINT('Ctrl Pts',(-0.0404227467934142,-0.149008802082514,
0.16943291995264));
#19291=CARTESIAN_POINT('Ctrl Pts',(0.0145735112284506,-0.153705024069172,
0.1720803093269));
#19292=CARTESIAN_POINT('Ctrl Pts',(0.0589475933459444,-0.134215943447351,
0.17472769870116));
#19293=CARTESIAN_POINT('Ctrl Pts',(0.103321675463438,-0.11472686282553,
0.17737508807542));
#19294=CARTESIAN_POINT('Ctrl Pts',(0.137073581676561,-0.0710524795952304,
0.18002247744968));
#19295=CARTESIAN_POINT('Ctrl Pts',(0.144743205110219,-0.0231979049720499,
0.18266986682394));
#19296=CARTESIAN_POINT('Ctrl Pts',(0.152412828543877,0.024656669651131,
0.1853172561982));
#19297=CARTESIAN_POINT('Ctrl Pts',(0.13400016919807,0.0766914356671922,
0.18796464557246));
#19298=CARTESIAN_POINT('Ctrl Pts',(0.0979391709064228,0.109071797518936,
0.19061203494672));
#19299=CARTESIAN_POINT('Ctrl Pts',(0.0618781726147763,0.141452159370678,
0.19325942432098));
#19300=CARTESIAN_POINT('Ctrl Pts',(0.00816883537729064,0.154178117058104,
0.195906813695239));
#19301=CARTESIAN_POINT('Ctrl Pts',(-0.0385872054932313,0.1414205281901,
0.198554203069499));
#19302=CARTESIAN_POINT('Ctrl Pts',(-0.0853432463637543,0.128662939322095,
0.201201592443759));
#19303=CARTESIAN_POINT('Ctrl Pts',(-0.125145990867313,0.0904218038986596,
0.20384898181802));
#19304=CARTESIAN_POINT('Ctrl Pts',(-0.139763737461459,0.0442135263146365,
0.20649637119228));
#19305=CARTESIAN_POINT('Ctrl Pts',(-0.144251162244238,0.030028291356252,
0.207309079266757));
#19306=CARTESIAN_POINT('Ctrl Pts',(-0.146365162502875,0.0150922359825044,
0.208121787341234));
#19307=CARTESIAN_POINT('Ctrl Pts',(-0.146245769975643,0.000123264779366826,
0.20893449541571));
#19308=CARTESIAN_POINT('Origin',(0.,0.,0.));
#19309=CARTESIAN_POINT('',(-0.146142672279203,-7.01165389862951E-5,0.266065504584291));
#19310=CARTESIAN_POINT('',(-0.146150215784492,-7.74481165901552E-5,0.258934495415711));
#19311=CARTESIAN_POINT('',(-0.14635,-1.79227059055215E-17,0.));
#19312=CARTESIAN_POINT('Ctrl Pts',(-0.146142672279203,-7.01165389862951E-5,
0.266065504584291));
#19313=CARTESIAN_POINT('Ctrl Pts',(-0.146017527260215,0.028828671850369,
0.264499287510729));
#19314=CARTESIAN_POINT('Ctrl Pts',(-0.137733916992107,0.0577936173630845,
0.262933070437168));
#19315=CARTESIAN_POINT('Ctrl Pts',(-0.121770841384076,0.0816117278206753,
0.261366853363607));
#19316=CARTESIAN_POINT('Ctrl Pts',(-0.0947991242083451,0.121855560193383,
0.258720523484505));
#19317=CARTESIAN_POINT('Ctrl Pts',(-0.0459036471244643,0.147405924851771,
0.256074193605403));
#19318=CARTESIAN_POINT('Ctrl Pts',(0.0025353607453442,0.146568017913755,
0.253427863726301));
#19319=CARTESIAN_POINT('Ctrl Pts',(0.050974368615152,0.145730110975738,
0.250781533847199));
#19320=CARTESIAN_POINT('Ctrl Pts',(0.0989569072708876,0.118503932441319,
0.248135203968097));
#19321=CARTESIAN_POINT('Ctrl Pts',(0.124520613871998,0.0773513325689396,
0.245488874088995));
#19322=CARTESIAN_POINT('Ctrl Pts',(0.150084320473109,0.0361987326965595,
0.242842544209893));
#19323=CARTESIAN_POINT('Ctrl Pts',(0.153229195019594,-0.0188802885137813,
0.240196214330791));
#19324=CARTESIAN_POINT('Ctrl Pts',(0.132515778953886,-0.0626751965094481,
0.237549884451689));
#19325=CARTESIAN_POINT('Ctrl Pts',(0.111802362888177,-0.106470104505115,
0.234903554572587));
#19326=CARTESIAN_POINT('Ctrl Pts',(0.0672306562102751,-0.138980899286108,
0.232257224693486));
#19327=CARTESIAN_POINT('Ctrl Pts',(0.0192018303028616,-0.145326878595667,
0.229610894814384));
#19328=CARTESIAN_POINT('Ctrl Pts',(-0.0288269956045516,-0.151672857905225,
0.226964564935282));
#19329=CARTESIAN_POINT('Ctrl Pts',(-0.0803129407414762,-0.131854021743351,
0.22431823505618));
#19330=CARTESIAN_POINT('Ctrl Pts',(-0.111690078002902,-0.0949417632280756,
0.221671905177078));
#19331=CARTESIAN_POINT('Ctrl Pts',(-0.133848162215005,-0.0688748557907962,
0.219803104979482));
#19332=CARTESIAN_POINT('Ctrl Pts',(-0.145978020566425,-0.0342834897603843,
0.217934304781886));
#19333=CARTESIAN_POINT('Ctrl Pts',(-0.146263250741535,0.000126870157254357,
0.21606550458429));
#19334=CARTESIAN_POINT('Ctrl Pts',(-0.146245769975643,0.000123264779366826,
0.20893449541571));
#19335=CARTESIAN_POINT('Ctrl Pts',(-0.145976242399967,-0.03366905549635,
0.210769176715493));
#19336=CARTESIAN_POINT('Ctrl Pts',(-0.134324750276972,-0.067629123606452,
0.212603858015276));
#19337=CARTESIAN_POINT('Ctrl Pts',(-0.112902327433,-0.0934976078712483,
0.214438539315059));
#19338=CARTESIAN_POINT('Ctrl Pts',(-0.0819904221256615,-0.130825044728502,
0.217085928689319));
#19339=CARTESIAN_POINT('Ctrl Pts',(-0.0307338628262512,-0.151304498698398,
0.21973331806358));
#19340=CARTESIAN_POINT('Ctrl Pts',(0.0173892134168267,-0.145555327884408,
0.22238070743784));
#19341=CARTESIAN_POINT('Ctrl Pts',(0.0655122896599044,-0.139806157070418,
0.2250280968121));
#19342=CARTESIAN_POINT('Ctrl Pts',(0.11050188284665,-0.107828361472542,
0.22767548618636));
#19343=CARTESIAN_POINT('Ctrl Pts',(0.131750448317205,-0.0642694140823833,
0.23032287556062));
#19344=CARTESIAN_POINT('Ctrl Pts',(0.15299901378776,-0.020710466692225,
0.232970264934879));
#19345=CARTESIAN_POINT('Ctrl Pts',(0.150506551542124,0.0344296324902152,
0.23561765430914));
#19346=CARTESIAN_POINT('Ctrl Pts',(0.125414737320077,0.0758938856636754,
0.2382650436834));
#19347=CARTESIAN_POINT('Ctrl Pts',(0.10032292309803,0.117358138837136,0.24091243305766));
#19348=CARTESIAN_POINT('Ctrl Pts',(0.0526317568995709,0.145146546001616,
0.24355982243192));
#19349=CARTESIAN_POINT('Ctrl Pts',(0.00418624259284972,0.146530589268381,
0.24620721180618));
#19350=CARTESIAN_POINT('Ctrl Pts',(-0.0442592717138715,0.147914632535146,
0.24885460118044));
#19351=CARTESIAN_POINT('Ctrl Pts',(-0.0934591341288551,0.122894311904195,
0.2515019905547));
#19352=CARTESIAN_POINT('Ctrl Pts',(-0.120877280418781,0.082930219442967,
0.25414937992896));
#19353=CARTESIAN_POINT('Ctrl Pts',(-0.137396572682769,0.0588520590724165,
0.255744418424543));
#19354=CARTESIAN_POINT('Ctrl Pts',(-0.146009100715185,0.0293493086505574,
0.257339456920127));
#19355=CARTESIAN_POINT('Ctrl Pts',(-0.146150215784492,-7.74481165901552E-5,
0.258934495415711));
#19356=CARTESIAN_POINT('Origin',(0.,0.,0.));
#19357=CARTESIAN_POINT('',(-0.146519404976022,-8.97763884284003E-5,0.316065504584291));
#19358=CARTESIAN_POINT('',(-0.146528765763263,-8.45393868379275E-5,0.30893449541571));
#19359=CARTESIAN_POINT('',(-0.14635,-1.79227059055215E-17,0.));
#19360=CARTESIAN_POINT('Ctrl Pts',(-0.146519404976022,-8.97763884284003E-5,
0.316065504584291));
#19361=CARTESIAN_POINT('Ctrl Pts',(-0.146208092107557,0.043076445171776,
0.313710600118674));
#19362=CARTESIAN_POINT('Ctrl Pts',(-0.125958424314353,0.0864965766126209,
0.311355695653057));
#19363=CARTESIAN_POINT('Ctrl Pts',(-0.0925183485457987,0.1137056160074,
0.309000791187441));
#19364=CARTESIAN_POINT('Ctrl Pts',(-0.0549399784004991,0.144281843189175,
0.306354461308339));
#19365=CARTESIAN_POINT('Ctrl Pts',(-0.00070450021881692,0.154386382754941,
0.303708131429237));
#19366=CARTESIAN_POINT('Ctrl Pts',(0.0453636543616171,0.139394227973128,
0.301061801550135));
#19367=CARTESIAN_POINT('Ctrl Pts',(0.0914318089420511,0.124402073191315,
0.298415471671033));
#19368=CARTESIAN_POINT('Ctrl Pts',(0.129332639921237,0.0843132240619223,
0.295769141791931));
#19369=CARTESIAN_POINT('Ctrl Pts',(0.141718340675246,0.0374769775398043,
0.293122811912829));
#19370=CARTESIAN_POINT('Ctrl Pts',(0.154104041429255,-0.00935926898231351,
0.290476482033727));
#19371=CARTESIAN_POINT('Ctrl Pts',(0.140974611958088,-0.0629429128971569,
0.287830152154626));
#19372=CARTESIAN_POINT('Ctrl Pts',(0.108339598692885,-0.0987478773661917,
0.285183822275524));
#19373=CARTESIAN_POINT('Ctrl Pts',(0.0757045854276824,-0.134552841835227,
0.282537492396422));
#19374=CARTESIAN_POINT('Ctrl Pts',(0.0235639883684441,-0.152579126858453,
0.27989116251732));
#19375=CARTESIAN_POINT('Ctrl Pts',(-0.0242166208952047,-0.144575818177467,
0.277244832638218));
#19376=CARTESIAN_POINT('Ctrl Pts',(-0.0719972301588528,-0.136572509496481,
0.274598502759116));
#19377=CARTESIAN_POINT('Ctrl Pts',(-0.115417851626912,-0.102539607111283,
0.271952172880014));
#19378=CARTESIAN_POINT('Ctrl Pts',(-0.13460418372715,-0.0580545058751705,
0.269305843000912));
#19379=CARTESIAN_POINT('Ctrl Pts',(-0.142435181350113,-0.0398976888130428,
0.268225730195372));
#19380=CARTESIAN_POINT('Ctrl Pts',(-0.146228976240411,-0.0199996345674016,
0.267145617389831));
#19381=CARTESIAN_POINT('Ctrl Pts',(-0.146142672279203,-7.01165389862951E-5,
0.266065504584291));
#19382=CARTESIAN_POINT('Ctrl Pts',(-0.146150215784492,-7.74481165901552E-5,
0.258934495415711));
#19383=CARTESIAN_POINT('Ctrl Pts',(-0.146243318595233,-0.0194921979337541,
0.259986846294387));
#19384=CARTESIAN_POINT('Ctrl Pts',(-0.142648899141753,-0.0388738684647463,
0.261039197173063));
#19385=CARTESIAN_POINT('Ctrl Pts',(-0.135204796371803,-0.0566427511368837,
0.26209154805174));
#19386=CARTESIAN_POINT('Ctrl Pts',(-0.116477735870028,-0.101343764964001,
0.264738937426));
#19387=CARTESIAN_POINT('Ctrl Pts',(-0.0733871847016099,-0.135837928326728,
0.26738632680026));
#19388=CARTESIAN_POINT('Ctrl Pts',(-0.0256708287318585,-0.144325142544676,
0.27003371617452));
#19389=CARTESIAN_POINT('Ctrl Pts',(0.0220455272378925,-0.152812356762624,
0.27268110554878));
#19390=CARTESIAN_POINT('Ctrl Pts',(0.0743876880089763,-0.135292621835792,
0.27532849492304));
#19391=CARTESIAN_POINT('Ctrl Pts',(0.10738025529095,-0.0997908762961729,
0.2779758842973));
#19392=CARTESIAN_POINT('Ctrl Pts',(0.140372822572925,-0.0642891307565533,
0.280623273671559));
#19393=CARTESIAN_POINT('Ctrl Pts',(0.154015796365789,-0.010805374604146,
0.283270663045819));
#19394=CARTESIAN_POINT('Ctrl Pts',(0.142059993874458,0.0361620845457957,
0.285918052420079));
#19395=CARTESIAN_POINT('Ctrl Pts',(0.130104191383128,0.0831295436957373,
0.288565441794339));
#19396=CARTESIAN_POINT('Ctrl Pts',(0.0925496126076039,0.123580705843213,
0.291212831168599));
#19397=CARTESIAN_POINT('Ctrl Pts',(0.0465981836912963,0.138986860871753,
0.29386022054286));
#19398=CARTESIAN_POINT('Ctrl Pts',(0.000646754774988913,0.154393015900293,
0.296507609917119));
#19399=CARTESIAN_POINT('Ctrl Pts',(-0.0537015242821025,0.144754163809898,
0.29915499929138));
#19400=CARTESIAN_POINT('Ctrl Pts',(-0.0915523499663989,0.114485393976436,
0.30180238866564));
#19401=CARTESIAN_POINT('Ctrl Pts',(-0.125542580994678,0.0873038870745135,
0.30417975758233));
#19402=CARTESIAN_POINT('Ctrl Pts',(-0.146229051243382,0.0434861464246214,
0.30655712649902));
#19403=CARTESIAN_POINT('Ctrl Pts',(-0.146528765763263,-8.45393868379275E-5,
0.30893449541571));
#19404=CARTESIAN_POINT('Origin',(0.,0.,0.));
#19405=CARTESIAN_POINT('',(-0.146416087288192,0.000126442170093593,0.366065504584291));
#19406=CARTESIAN_POINT('',(-0.146408012399712,0.000128195943346294,0.358934495415711));
#19407=CARTESIAN_POINT('',(-0.14635,-1.79227059055215E-17,0.));
#19408=CARTESIAN_POINT('Ctrl Pts',(-0.146416087288192,0.000126442170093593,
0.366065504584291));
#19409=CARTESIAN_POINT('Ctrl Pts',(-0.146499294961499,0.00925816812376314,
0.365568242605721));
#19410=CARTESIAN_POINT('Ctrl Pts',(-0.145718277739785,0.0183757049974218,
0.365070980627151));
#19411=CARTESIAN_POINT('Ctrl Pts',(-0.144021710151773,0.0273195705351122,
0.364573718648581));
#19412=CARTESIAN_POINT('Ctrl Pts',(-0.134992913071845,0.0749170536065741,
0.361927388769479));
#19413=CARTESIAN_POINT('Ctrl Pts',(-0.100034284522917,0.117595890322328,
0.359281058890377));
#19414=CARTESIAN_POINT('Ctrl Pts',(-0.0551469387876206,0.135821305661589,
0.356634729011275));
#19415=CARTESIAN_POINT('Ctrl Pts',(-0.0102595930523245,0.15404672100085,
0.353988399132173));
#19416=CARTESIAN_POINT('Ctrl Pts',(0.0445564698693406,0.147818714963618,
0.351342069253072));
#19417=CARTESIAN_POINT('Ctrl Pts',(0.0842110755700531,0.119987943896873,
0.34869573937397));
#19418=CARTESIAN_POINT('Ctrl Pts',(0.123865681270766,0.0921571728301272,
0.346049409494868));
#19419=CARTESIAN_POINT('Ctrl Pts',(0.148358829750526,0.0427236367338667,
0.343403079615766));
#19420=CARTESIAN_POINT('Ctrl Pts',(0.146479621605269,-0.00568615719458776,
0.340756749736664));
#19421=CARTESIAN_POINT('Ctrl Pts',(0.144600413460012,-0.0540959511230416,
0.338110419857562));
#19422=CARTESIAN_POINT('Ctrl Pts',(0.116348848689739,-0.101482002883689,
0.33546408997846));
#19423=CARTESIAN_POINT('Ctrl Pts',(0.0746561129649502,-0.126154971072205,
0.332817760099358));
#19424=CARTESIAN_POINT('Ctrl Pts',(0.0329633772401616,-0.150827939260721,
0.330171430220256));
#19425=CARTESIAN_POINT('Ctrl Pts',(-0.0221705294391424,-0.152787823877104,
0.327525100341154));
#19426=CARTESIAN_POINT('Ctrl Pts',(-0.0655099505772086,-0.131137554898038,
0.324878770462052));
#19427=CARTESIAN_POINT('Ctrl Pts',(-0.108849371715275,-0.109487285918972,
0.322232440582951));
#19428=CARTESIAN_POINT('Ctrl Pts',(-0.140394307312104,-0.0642268633444555,
0.319586110703849));
#19429=CARTESIAN_POINT('Ctrl Pts',(-0.14570614405606,-0.0160726946583056,
0.316939780824747));
#19430=CARTESIAN_POINT('Ctrl Pts',(-0.146291106736525,-0.0107697471190636,
0.316648355411261));
#19431=CARTESIAN_POINT('Ctrl Pts',(-0.146557930734812,-0.0054317060295066,
0.316356929997776));
#19432=CARTESIAN_POINT('Ctrl Pts',(-0.146519404976022,-8.97763884284003E-5,
0.316065504584291));
#19433=CARTESIAN_POINT('Ctrl Pts',(-0.146528765763263,-8.45393868379275E-5,
0.30893449541571));
#19434=CARTESIAN_POINT('Ctrl Pts',(-0.146562807199252,-0.00503327764821679,
0.30920451587328));
#19435=CARTESIAN_POINT('Ctrl Pts',(-0.14633385314783,-0.00997882882536714,
0.30947453633085));
#19436=CARTESIAN_POINT('Ctrl Pts',(-0.145831525524598,-0.0148964553326841,
0.309744556788419));
#19437=CARTESIAN_POINT('Ctrl Pts',(-0.140906503086998,-0.0631108472318147,
0.312391946162679));
#19438=CARTESIAN_POINT('Ctrl Pts',(-0.109703085900295,-0.108640943453547,
0.31503933553694));
#19439=CARTESIAN_POINT('Ctrl Pts',(-0.0665140418604196,-0.13063162118607,
0.3176867249112));
#19440=CARTESIAN_POINT('Ctrl Pts',(-0.0233249978205455,-0.152622298918592,
0.32033411428546));
#19441=CARTESIAN_POINT('Ctrl Pts',(0.0318496730725009,-0.151073558161906,
0.322981503659719));
#19442=CARTESIAN_POINT('Ctrl Pts',(0.0737371373950496,-0.126694801736668,
0.325628893033979));
#19443=CARTESIAN_POINT('Ctrl Pts',(0.115624601717599,-0.10231604531143,
0.328276282408239));
#19444=CARTESIAN_POINT('Ctrl Pts',(0.144224859469651,-0.0551072732176397,
0.3309236717825));
#19445=CARTESIAN_POINT('Ctrl Pts',(0.146437523492708,-0.0066925280449658,
0.33357106115676));
#19446=CARTESIAN_POINT('Ctrl Pts',(0.148650187515766,0.0417222171277085,
0.33621845053102));
#19447=CARTESIAN_POINT('Ctrl Pts',(0.124475257809829,0.0913429353792657,
0.33886583990528));
#19448=CARTESIAN_POINT('Ctrl Pts',(0.0849860939726622,0.119440788885456,
0.34151322927954));
#19449=CARTESIAN_POINT('Ctrl Pts',(0.0454969301354961,0.147538642391646,
0.344160618653799));
#19450=CARTESIAN_POINT('Ctrl Pts',(-0.00930646783289898,0.154113631152469,
0.346808008028059));
#19451=CARTESIAN_POINT('Ctrl Pts',(-0.0543213285795041,0.136154072578339,
0.349455397402319));
#19452=CARTESIAN_POINT('Ctrl Pts',(-0.0993361893261098,0.11819451400421,
0.352102786776579));
#19453=CARTESIAN_POINT('Ctrl Pts',(-0.134562512850926,0.0757004080951257,
0.35475017615084));
#19454=CARTESIAN_POINT('Ctrl Pts',(-0.143864833510727,0.0281362381501331,
0.3573975655251));
#19455=CARTESIAN_POINT('Ctrl Pts',(-0.145664973529558,0.0189318504589563,
0.357909875488637));
#19456=CARTESIAN_POINT('Ctrl Pts',(-0.146494308508217,0.00953759842677947,
0.358422185452174));
#19457=CARTESIAN_POINT('Ctrl Pts',(-0.146408012399712,0.000128195943346294,
0.358934495415711));
#19458=CARTESIAN_POINT('Origin',(0.,0.,0.));
#19459=CARTESIAN_POINT('',(-0.146110491840834,1.12683595067248E-5,0.416065504584291));
#19460=CARTESIAN_POINT('',(-0.146109756335714,8.81622270207575E-6,0.40893449541571));
#19461=CARTESIAN_POINT('',(-0.14635,-1.79227059055215E-17,0.));
#19462=CARTESIAN_POINT('Ctrl Pts',(-0.146110491840834,1.12683595067248E-5,
0.416065504584291));
#19463=CARTESIAN_POINT('Ctrl Pts',(-0.146126798292857,0.0237518011834032,
0.414779555213666));
#19464=CARTESIAN_POINT('Ctrl Pts',(-0.140669750958991,0.0474852665485293,
0.413493605843041));
#19465=CARTESIAN_POINT('Ctrl Pts',(-0.129698698951591,0.0683144158983218,
0.412207656472415));
#19466=CARTESIAN_POINT('Ctrl Pts',(-0.107121587134001,0.111178312051432,
0.409561326593314));
#19467=CARTESIAN_POINT('Ctrl Pts',(-0.0611933749717542,0.141742803557285,
0.406914996714211));
#19468=CARTESIAN_POINT('Ctrl Pts',(-0.0129361277491455,0.146018041789781,
0.40426866683511));
#19469=CARTESIAN_POINT('Ctrl Pts',(0.0353211194734639,0.150293280022276,
0.401622336956008));
#19470=CARTESIAN_POINT('Ctrl Pts',(0.0859074017564354,0.128279264981412,
0.398976007076906));
#19471=CARTESIAN_POINT('Ctrl Pts',(0.115668581836909,0.0900521576926538,
0.396329677197804));
#19472=CARTESIAN_POINT('Ctrl Pts',(0.145429761917382,0.0518250504038959,
0.393683347318702));
#19473=CARTESIAN_POINT('Ctrl Pts',(0.154365839795359,-0.0026151491327561,
0.3910370174396));
#19474=CARTESIAN_POINT('Ctrl Pts',(0.138386632036901,-0.0483503050946702,
0.388390687560498));
#19475=CARTESIAN_POINT('Ctrl Pts',(0.122407424278443,-0.094085461056585,
0.385744357681396));
#19476=CARTESIAN_POINT('Ctrl Pts',(0.0815129308835505,-0.131115573443762,
0.383098027802294));
#19477=CARTESIAN_POINT('Ctrl Pts',(0.0344212048624006,-0.142491377230642,
0.380451697923192));
#19478=CARTESIAN_POINT('Ctrl Pts',(-0.0126705211587486,-0.153867181017521,
0.37780536804409));
#19479=CARTESIAN_POINT('Ctrl Pts',(-0.0659594798061549,-0.139588676204105,
0.375159038164988));
#19480=CARTESIAN_POINT('Ctrl Pts',(-0.101054476324393,-0.106191359083811,
0.372512708285887));
#19481=CARTESIAN_POINT('Ctrl Pts',(-0.129554902927378,-0.0790696072742943,
0.370363640385355));
#19482=CARTESIAN_POINT('Ctrl Pts',(-0.146056480184715,-0.0393390709180539,
0.368214572484823));
#19483=CARTESIAN_POINT('Ctrl Pts',(-0.146416087288192,0.000126442170093593,
0.366065504584291));
#19484=CARTESIAN_POINT('Ctrl Pts',(-0.146408012399712,0.000128195943346294,
0.358934495415711));
#19485=CARTESIAN_POINT('Ctrl Pts',(-0.146048368712081,-0.0390859965171687,
0.361069574826434));
#19486=CARTESIAN_POINT('Ctrl Pts',(-0.1297855810823,-0.0785633296797545,
0.363204654237157));
#19487=CARTESIAN_POINT('Ctrl Pts',(-0.101613371150224,-0.105657280969165,
0.36533973364788));
#19488=CARTESIAN_POINT('Ctrl Pts',(-0.066681270335132,-0.139252396162569,
0.36798712302214));
#19489=CARTESIAN_POINT('Ctrl Pts',(-0.0134387509101597,-0.153808392568477,
0.370634512396399));
#19490=CARTESIAN_POINT('Ctrl Pts',(0.0337263783221333,-0.142657876135818,
0.373281901770659));
#19491=CARTESIAN_POINT('Ctrl Pts',(0.0808915075544263,-0.13150735970316,
0.375929291144919));
#19492=CARTESIAN_POINT('Ctrl Pts',(0.12197924659404,-0.0946503304319347,
0.378576680519179));
#19493=CARTESIAN_POINT('Ctrl Pts',(0.138169300408926,-0.0489692009616054,
0.38122406989344));
#19494=CARTESIAN_POINT('Ctrl Pts',(0.154359354223812,-0.00328807149127619,
0.3838714592677));
#19495=CARTESIAN_POINT('Ctrl Pts',(0.14565172281397,0.0512171581781573,
0.38651884864196));
#19496=CARTESIAN_POINT('Ctrl Pts',(0.11603494864959,0.0895802930905963,
0.38916623801622));
#19497=CARTESIAN_POINT('Ctrl Pts',(0.0864181744852101,0.127943428003035,
0.39181362739048));
#19498=CARTESIAN_POINT('Ctrl Pts',(0.0358922575662923,0.15016446815848,
0.394461016764739));
#19499=CARTESIAN_POINT('Ctrl Pts',(-0.0123993367959677,0.146065035738641,
0.397108406138999));
#19500=CARTESIAN_POINT('Ctrl Pts',(-0.0606909311582276,0.141965603318802,
0.399755795513259));
#19501=CARTESIAN_POINT('Ctrl Pts',(-0.106748202963829,0.111545698323679,
0.40240318488752));
#19502=CARTESIAN_POINT('Ctrl Pts',(-0.129474555904152,0.0687391998188283,
0.40505057426178));
#19503=CARTESIAN_POINT('Ctrl Pts',(-0.140588317483115,0.0478057390183907,
0.406345214646423));
#19504=CARTESIAN_POINT('Ctrl Pts',(-0.146122589096428,0.0239100770892618,
0.407639855031067));
#19505=CARTESIAN_POINT('Ctrl Pts',(-0.146109756335714,8.81622270207575E-6,
0.40893449541571));
#19506=CARTESIAN_POINT('Origin',(0.,0.,0.));
#19507=CARTESIAN_POINT('',(-0.146374718215768,-0.000132229735885947,0.466065504584291));
#19508=CARTESIAN_POINT('',(-0.146375609273197,-0.000132432188538665,0.458934495415711));
#19509=CARTESIAN_POINT('',(-0.14635,-1.79227059055215E-17,0.));
#19510=CARTESIAN_POINT('Ctrl Pts',(-0.146374718215768,-0.000132229735885947,
0.466065504584291));
#19511=CARTESIAN_POINT('Ctrl Pts',(-0.146022504084922,0.0379941335185874,
0.46399086782161));
#19512=CARTESIAN_POINT('Ctrl Pts',(-0.130761950520226,0.0763703265456945,
0.46191623105893));
#19513=CARTESIAN_POINT('Ctrl Pts',(-0.103994021541854,0.103314352404769,
0.45984159429625));
#19514=CARTESIAN_POINT('Ctrl Pts',(-0.0698498419286355,0.137683154682254,
0.457195264417148));
#19515=CARTESIAN_POINT('Ctrl Pts',(-0.0169824611430249,0.153451124186949,
0.454548934538046));
#19516=CARTESIAN_POINT('Ctrl Pts',(0.030409888879481,0.143401013202843,
0.451902604658944));
#19517=CARTESIAN_POINT('Ctrl Pts',(0.0778022389019875,0.133350902218736,
0.449256274779842));
#19518=CARTESIAN_POINT('Ctrl Pts',(0.119719558161389,0.0974827107458278,
0.44660994490074));
#19519=CARTESIAN_POINT('Ctrl Pts',(0.136975630157447,0.0522138743269898,
0.443963615021638));
#19520=CARTESIAN_POINT('Ctrl Pts',(0.154231702153504,0.00694503790815254,
0.441317285142536));
#19521=CARTESIAN_POINT('Ctrl Pts',(0.146826526886218,-0.0477244434566137,
0.438670955263434));
#19522=CARTESIAN_POINT('Ctrl Pts',(0.118149569579287,-0.0867714880447125,
0.436024625384332));
#19523=CARTESIAN_POINT('Ctrl Pts',(0.0894726122723542,-0.125818532632812,
0.43337829550523));
#19524=CARTESIAN_POINT('Ctrl Pts',(0.0395238729257754,-0.149243140444243,
0.430731965626129));
#19525=CARTESIAN_POINT('Ctrl Pts',(-0.00883432462988853,-0.146323499949933,
0.428085635747027));
#19526=CARTESIAN_POINT('Ctrl Pts',(-0.0571925221855517,-0.143403859455623,
0.425439305867925));
#19527=CARTESIAN_POINT('Ctrl Pts',(-0.1039601779503,-0.114139970655572,
0.422792975988823));
#19528=CARTESIAN_POINT('Ctrl Pts',(-0.127731000096207,-0.0719263758553634,
0.420146646109721));
#19529=CARTESIAN_POINT('Ctrl Pts',(-0.139950702323481,-0.0502259249733931,
0.418786265601244));
#19530=CARTESIAN_POINT('Ctrl Pts',(-0.146093241566443,-0.0251033736724598,
0.417425885092767));
#19531=CARTESIAN_POINT('Ctrl Pts',(-0.146110491840834,1.12683595067248E-5,
0.416065504584291));
#19532=CARTESIAN_POINT('Ctrl Pts',(-0.146109756335714,8.81622270207575E-6,
0.40893449541571));
#19533=CARTESIAN_POINT('Ctrl Pts',(-0.146096347589706,-0.0249652282079418,
0.410287244405327));
#19534=CARTESIAN_POINT('Ctrl Pts',(-0.140026707259891,-0.049945385460595,
0.411639993394943));
#19535=CARTESIAN_POINT('Ctrl Pts',(-0.127937780377622,-0.0715588049813403,
0.412992742384559));
#19536=CARTESIAN_POINT('Ctrl Pts',(-0.104279217835726,-0.113857219262079,
0.415640131758819));
#19537=CARTESIAN_POINT('Ctrl Pts',(-0.0575666586768896,-0.14326095580898,
0.41828752113308));
#19538=CARTESIAN_POINT('Ctrl Pts',(-0.00919685447762893,-0.146301592903247,
0.42093491050734));
#19539=CARTESIAN_POINT('Ctrl Pts',(0.039172949721632,-0.149342229997515,
0.4235822998816));
#19540=CARTESIAN_POINT('Ctrl Pts',(0.089199998961318,-0.126019767639148,
0.426229689255859));
#19541=CARTESIAN_POINT('Ctrl Pts',(0.117969334952632,-0.0870170915920772,
0.428877078630119));
#19542=CARTESIAN_POINT('Ctrl Pts',(0.146738670943946,-0.0480144155450057,
0.431524468004379));
#19543=CARTESIAN_POINT('Ctrl Pts',(0.154250293686888,0.00666847419077017,
0.43417185737864));
#19544=CARTESIAN_POINT('Ctrl Pts',(0.137063494116028,0.051984005222912,
0.4368192467529));
#19545=CARTESIAN_POINT('Ctrl Pts',(0.119876694545168,0.0972995362550541,
0.43946663612716));
#19546=CARTESIAN_POINT('Ctrl Pts',(0.0779914726605056,0.133247708583562,
0.442114025501419));
#19547=CARTESIAN_POINT('Ctrl Pts',(0.0305934116013849,0.143362412733947,
0.444761414875679));
#19548=CARTESIAN_POINT('Ctrl Pts',(-0.0168046494577345,0.153477116884331,
0.447408804249939));
#19549=CARTESIAN_POINT('Ctrl Pts',(-0.0697155496913122,0.137758352856595,
0.4500561936242));
#19550=CARTESIAN_POINT('Ctrl Pts',(-0.103903378920715,0.103406122000434,
0.45270358299846));
#19551=CARTESIAN_POINT('Ctrl Pts',(-0.130724942802416,0.0764555792150183,
0.45478055380421));
#19552=CARTESIAN_POINT('Ctrl Pts',(-0.146022533856355,0.0380362146017157,
0.45685752460996));
#19553=CARTESIAN_POINT('Ctrl Pts',(-0.146375609273197,-0.000132432188538665,
0.458934495415711));
#19554=CARTESIAN_POINT('Origin',(0.,0.,0.));
#19555=CARTESIAN_POINT('',(-0.146548608312775,6.99729089778146E-5,0.516065504584291));
#19556=CARTESIAN_POINT('',(-0.146550766805835,6.86360251013434E-5,0.508934495415711));
#19557=CARTESIAN_POINT('',(-0.14635,-1.79227059055215E-17,0.));
#19558=CARTESIAN_POINT('Ctrl Pts',(-0.146548608312775,6.99729089778146E-5,
0.516065504584291));
#19559=CARTESIAN_POINT('Ctrl Pts',(-0.146572081366671,0.00404546554386884,
0.515848510308657));
#19560=CARTESIAN_POINT('Ctrl Pts',(-0.146424333269732,0.00801918670503405,
0.515631516033023));
#19561=CARTESIAN_POINT('Ctrl Pts',(-0.146099725131082,0.0119784074854107,
0.51541452175739));
#19562=CARTESIAN_POINT('Ctrl Pts',(-0.142141002193345,0.06026265009261,
0.512768191878288));
#19563=CARTESIAN_POINT('Ctrl Pts',(-0.111878319621163,0.106390286678145,
0.510121861999186));
#19564=CARTESIAN_POINT('Ctrl Pts',(-0.069163383343408,0.129247972261684,
0.507475532120084));
#19565=CARTESIAN_POINT('Ctrl Pts',(-0.0264484470656534,0.152105657845224,
0.504829202240982));
#19566=CARTESIAN_POINT('Ctrl Pts',(0.0287187429176733,0.151693392426768,
0.50218287236188));
#19567=CARTESIAN_POINT('Ctrl Pts',(0.07108729581893,0.128199876374419,0.499536542482778));
#19568=CARTESIAN_POINT('Ctrl Pts',(0.113455848720186,0.10470636032207,0.496890212603677));
#19569=CARTESIAN_POINT('Ctrl Pts',(0.143025764539373,0.0581315936358261,
0.494243882724575));
#19570=CARTESIAN_POINT('Ctrl Pts',(0.146262427589597,0.00979357977770552,
0.491597552845473));
#19571=CARTESIAN_POINT('Ctrl Pts',(0.149499090639821,-0.0385444340804161,
0.488951222966371));
#19572=CARTESIAN_POINT('Ctrl Pts',(0.126402500921083,-0.0886456951104151,
0.486304893087269));
#19573=CARTESIAN_POINT('Ctrl Pts',(0.087544330920799,-0.117578067907642,
0.483658563208167));
#19574=CARTESIAN_POINT('Ctrl Pts',(0.0486861609205161,-0.146510440704867,
0.481012233329065));
#19575=CARTESIAN_POINT('Ctrl Pts',(-0.00593358936131212,-0.154273925269321,
0.478365903449963));
#19576=CARTESIAN_POINT('Ctrl Pts',(-0.0513146009011563,-0.137315052574797,
0.475719573570861));
#19577=CARTESIAN_POINT('Ctrl Pts',(-0.0966956124410008,-0.120356179880273,
0.473073243691759));
#19578=CARTESIAN_POINT('Ctrl Pts',(-0.132837885238862,-0.078674949926771,
0.470426913812657));
#19579=CARTESIAN_POINT('Ctrl Pts',(-0.14319853241738,-0.0313495174248821,
0.467780583933555));
#19580=CARTESIAN_POINT('Ctrl Pts',(-0.145436768368387,-0.0211256884885646,
0.467208890817134));
#19581=CARTESIAN_POINT('Ctrl Pts',(-0.146471775395962,-0.0106384445195334,
0.466637197700712));
#19582=CARTESIAN_POINT('Ctrl Pts',(-0.146374718215768,-0.000132229735885947,
0.466065504584291));
#19583=CARTESIAN_POINT('Ctrl Pts',(-0.146375609273197,-0.000132432188538665,
0.458934495415711));
#19584=CARTESIAN_POINT('Ctrl Pts',(-0.146472577787773,-0.0106150565970108,
0.45950491398422));
#19585=CARTESIAN_POINT('Ctrl Pts',(-0.145442327125792,-0.021078770125739,
0.46007533255273));
#19586=CARTESIAN_POINT('Ctrl Pts',(-0.143213999951756,-0.0312807998000163,
0.460645751121239));
#19587=CARTESIAN_POINT('Ctrl Pts',(-0.132872033528166,-0.0786297930597184,
0.463293140495499));
#19588=CARTESIAN_POINT('Ctrl Pts',(-0.0967233424557573,-0.120342081894533,
0.465940529869759));
#19589=CARTESIAN_POINT('Ctrl Pts',(-0.0513258840937604,-0.13731129538499,
0.46858791924402));
#19590=CARTESIAN_POINT('Ctrl Pts',(-0.00592842573176499,-0.154280508875447,
0.47123530861828));
#19591=CARTESIAN_POINT('Ctrl Pts',(0.0487177999198187,-0.146506647021548,
0.47388269799254));
#19592=CARTESIAN_POINT('Ctrl Pts',(0.0875820145025328,-0.117550537871965,
0.476530087366799));
#19593=CARTESIAN_POINT('Ctrl Pts',(0.126446229085248,-0.0885944287223814,
0.47917747674106));
#19594=CARTESIAN_POINT('Ctrl Pts',(0.149528432599094,-0.0384560722771122,
0.481824866115319));
#19595=CARTESIAN_POINT('Ctrl Pts',(0.146255790172295,0.0098985887573764,
0.484472255489579));
#19596=CARTESIAN_POINT('Ctrl Pts',(0.142983147745498,0.0582532497918637,
0.487119644863839));
#19597=CARTESIAN_POINT('Ctrl Pts',(0.113355659378058,0.10482421541557,0.4897670342381));
#19598=CARTESIAN_POINT('Ctrl Pts',(0.0709442366160257,0.128279591164298,
0.49241442361236));
#19599=CARTESIAN_POINT('Ctrl Pts',(0.0285328138539934,0.151734966913027,
0.49506181298662));
#19600=CARTESIAN_POINT('Ctrl Pts',(-0.0266625433026316,0.152074752786777,
0.497709202360879));
#19601=CARTESIAN_POINT('Ctrl Pts',(-0.0693595260588707,0.129143309401606,
0.500356591735139));
#19602=CARTESIAN_POINT('Ctrl Pts',(-0.11205650881511,0.106211866016435,
0.503003981109399));
#19603=CARTESIAN_POINT('Ctrl Pts',(-0.142255117170964,0.060009193372344,
0.505651370483659));
#19604=CARTESIAN_POINT('Ctrl Pts',(-0.146122837288996,0.0116984888307781,
0.50829875985792));
#19605=CARTESIAN_POINT('Ctrl Pts',(-0.146432431239741,0.00783142983325791,
0.508510671710517));
#19606=CARTESIAN_POINT('Ctrl Pts',(-0.14657331536999,0.00395086404934249,
0.508722583563114));
#19607=CARTESIAN_POINT('Ctrl Pts',(-0.146550766805835,6.86360251013434E-5,
0.508934495415711));
#19608=CARTESIAN_POINT('Origin',(0.,0.,0.));
#19609=CARTESIAN_POINT('',(-0.146165204287215,8.83645032875094E-5,0.566065504584291));
#19610=CARTESIAN_POINT('',(-0.146168951232552,9.12430751481418E-5,0.558934495415711));
#19611=CARTESIAN_POINT('',(-0.14635,-1.79227059055215E-17,0.));
#19612=CARTESIAN_POINT('Ctrl Pts',(-0.146165204287215,8.83645032875094E-5,
0.566065504584291));
#19613=CARTESIAN_POINT('Ctrl Pts',(-0.146267412293664,0.0186373661349918,
0.565059822916602));
#19614=CARTESIAN_POINT('Ctrl Pts',(-0.142994166834961,0.0371516370495788,
0.564054141248913));
#19615=CARTESIAN_POINT('Ctrl Pts',(-0.136179985035193,0.0542551712289143,
0.563048459581224));
#19616=CARTESIAN_POINT('Ctrl Pts',(-0.118249288396568,0.0992610562830057,
0.560402129702122));
#19617=CARTESIAN_POINT('Ctrl Pts',(-0.0758005933416487,0.134498778989873,
0.55775579982302));
#19618=CARTESIAN_POINT('Ctrl Pts',(-0.0282633354322908,0.143839479279877,
0.555109469943918));
#19619=CARTESIAN_POINT('Ctrl Pts',(0.0192739224770691,0.153180179569881,
0.552463140064816));
#19620=CARTESIAN_POINT('Ctrl Pts',(0.0718997432408687,0.136623857443018,
0.549816810185715));
#19621=CARTESIAN_POINT('Ctrl Pts',(0.105526460745998,0.101748602013432,
0.547170480306613));
#19622=CARTESIAN_POINT('Ctrl Pts',(0.139153178251127,0.0668733465838454,
0.544524150427511));
#19623=CARTESIAN_POINT('Ctrl Pts',(0.153780792497586,0.0136791578515372,
0.541877820548409));
#19624=CARTESIAN_POINT('Ctrl Pts',(0.142714014311998,-0.0334861471092027,
0.539231490669307));
#19625=CARTESIAN_POINT('Ctrl Pts',(0.13164723612641,-0.0806514520699426,
0.536585160790205));
#19626=CARTESIAN_POINT('Ctrl Pts',(0.0948860655087725,-0.121787873259113,
0.533938830911103));
#19627=CARTESIAN_POINT('Ctrl Pts',(0.0492566686055307,-0.138066623508903,
0.531292501032001));
#19628=CARTESIAN_POINT('Ctrl Pts',(0.00362727170228945,-0.154345373758693,
0.528646171152899));
#19629=CARTESIAN_POINT('Ctrl Pts',(-0.050870351486557,-0.145766453069103,
0.525999841273797));
#19630=CARTESIAN_POINT('Ctrl Pts',(-0.089291781429334,-0.116256568409877,
0.523353511394695));
#19631=CARTESIAN_POINT('Ctrl Pts',(-0.124562723435938,-0.0891664410515947,
0.520924175791227));
#19632=CARTESIAN_POINT('Ctrl Pts',(-0.146285818313441,-0.0444372186796531,
0.518494840187759));
#19633=CARTESIAN_POINT('Ctrl Pts',(-0.146548608312775,6.99729089778146E-5,
0.516065504584291));
#19634=CARTESIAN_POINT('Ctrl Pts',(-0.146550766805835,6.86360251013434E-5,
0.508934495415711));
#19635=CARTESIAN_POINT('Ctrl Pts',(-0.146291618860727,-0.0445493453248537,
0.511369972937373));
#19636=CARTESIAN_POINT('Ctrl Pts',(-0.124445252016267,-0.0893868858389474,
0.513805450459036));
#19637=CARTESIAN_POINT('Ctrl Pts',(-0.0890226177929609,-0.116463349340462,
0.516240927980699));
#19638=CARTESIAN_POINT('Ctrl Pts',(-0.0505178462986829,-0.145895746531099,
0.518888317354959));
#19639=CARTESIAN_POINT('Ctrl Pts',(0.00402852857008221,-0.154341804473332,
0.52153570672922));
#19640=CARTESIAN_POINT('Ctrl Pts',(0.0496314652424392,-0.137932794781367,
0.52418309610348));
#19641=CARTESIAN_POINT('Ctrl Pts',(0.0952344019147948,-0.121523785089403,
0.52683048547774));
#19642=CARTESIAN_POINT('Ctrl Pts',(0.131893900390741,-0.0802597077632436,
0.529477874851999));
#19643=CARTESIAN_POINT('Ctrl Pts',(0.14281802728161,-0.0330416298281342,
0.532125264226259));
#19644=CARTESIAN_POINT('Ctrl Pts',(0.153742154172479,0.0141764481069759,
0.53477265360052));
#19645=CARTESIAN_POINT('Ctrl Pts',(0.138930909478268,0.0673485266510362,
0.53742004297478));
#19646=CARTESIAN_POINT('Ctrl Pts',(0.105168604077417,0.102119062543277,
0.54006743234904));
#19647=CARTESIAN_POINT('Ctrl Pts',(0.0714062986765666,0.136889598435517,
0.5427148217233));
#19648=CARTESIAN_POINT('Ctrl Pts',(0.018692932569077,0.153258591675938,
0.545362211097559));
#19649=CARTESIAN_POINT('Ctrl Pts',(-0.0288260648428939,0.143728202535144,
0.548009600471819));
#19650=CARTESIAN_POINT('Ctrl Pts',(-0.0763450622548654,0.13419781339435,
0.550656989846079));
#19651=CARTESIAN_POINT('Ctrl Pts',(-0.118669690971318,0.0987680418723385,
0.55330437922034));
#19652=CARTESIAN_POINT('Ctrl Pts',(-0.136413096952957,0.0536675432455532,
0.5559517685946));
#19653=CARTESIAN_POINT('Ctrl Pts',(-0.143076734904351,0.036729792140314,
0.556946010868304));
#19654=CARTESIAN_POINT('Ctrl Pts',(-0.146273385252938,0.0184280612467595,
0.557940253142007));
#19655=CARTESIAN_POINT('Ctrl Pts',(-0.146168951232552,9.12430751481418E-5,
0.558934495415711));
#19656=CARTESIAN_POINT('Origin',(0.,0.,0.));
#19657=CARTESIAN_POINT('',(-0.146227179098081,-0.000117664897458569,0.616065504584291));
#19658=CARTESIAN_POINT('',(-0.146218520919543,-0.000115076211918358,0.608934495415711));
#19659=CARTESIAN_POINT('',(-0.14635,-1.79227059055215E-17,0.));
#19660=CARTESIAN_POINT('Ctrl Pts',(-0.146227179098081,-0.000117664897458569,
0.616065504584291));
#19661=CARTESIAN_POINT('Ctrl Pts',(-0.145977603365176,0.0329427899635141,
0.614271135524546));
#19662=CARTESIAN_POINT('Ctrl Pts',(-0.134874795495675,0.0661550248562671,
0.612476766464802));
#19663=CARTESIAN_POINT('Ctrl Pts',(-0.114309815624116,0.091770790457776,
0.610682397405058));
#19664=CARTESIAN_POINT('Ctrl Pts',(-0.0839806476072558,0.129548841477563,
0.608036067525956));
#19665=CARTESIAN_POINT('Ctrl Pts',(-0.0330710111925292,0.150804375664025,
0.605389737646855));
#19666=CARTESIAN_POINT('Ctrl Pts',(0.0151169520838501,0.145808400611758,
0.602743407767753));
#19667=CARTESIAN_POINT('Ctrl Pts',(0.0633049153602295,0.140812425559491,
0.600097077888651));
#19668=CARTESIAN_POINT('Ctrl Pts',(0.108771205498262,0.109564941268491,
0.597450748009549));
#19669=CARTESIAN_POINT('Ctrl Pts',(0.130705186191441,0.0663684129079872,
0.594804418130447));
#19670=CARTESIAN_POINT('Ctrl Pts',(0.152639166884621,0.023171884547483,
0.592158088251345));
#19671=CARTESIAN_POINT('Ctrl Pts',(0.151040838132949,-0.0319736878825246,
0.589511758372243));
#19672=CARTESIAN_POINT('Ctrl Pts',(0.126641780152193,-0.0738273082886534,
0.586865428493141));
#19673=CARTESIAN_POINT('Ctrl Pts',(0.102242722171437,-0.115680928694782,
0.584219098614039));
#19674=CARTESIAN_POINT('Ctrl Pts',(0.0550429349615966,-0.14424259707703,
0.581572768734937));
#19675=CARTESIAN_POINT('Ctrl Pts',(0.00664650371163741,-0.14643918846291,
0.578926438855836));
#19676=CARTESIAN_POINT('Ctrl Pts',(-0.0417499275383225,-0.148635779848789,
0.576280108976733));
#19677=CARTESIAN_POINT('Ctrl Pts',(-0.0913430028284016,-0.1244672942383,
0.573633779097631));
#19678=CARTESIAN_POINT('Ctrl Pts',(-0.119433191362276,-0.0849960277323969,
0.570987449218529));
#19679=CARTESIAN_POINT('Ctrl Pts',(-0.136848298201485,-0.0605249807527623,
0.569346801007117));
#19680=CARTESIAN_POINT('Ctrl Pts',(-0.145998464265635,-0.0301720919893573,
0.567706152795704));
#19681=CARTESIAN_POINT('Ctrl Pts',(-0.146165204287215,8.83645032875094E-5,
0.566065504584291));
#19682=CARTESIAN_POINT('Ctrl Pts',(-0.146168951232552,9.12430751481418E-5,
0.558934495415711));
#19683=CARTESIAN_POINT('Ctrl Pts',(-0.145995306636495,-0.0303977620653178,
0.560587642516267));
#19684=CARTESIAN_POINT('Ctrl Pts',(-0.136695352934655,-0.0609837708898569,
0.562240789616823));
#19685=CARTESIAN_POINT('Ctrl Pts',(-0.119031718004195,-0.0855580991331628,
0.563893936717379));
#19686=CARTESIAN_POINT('Ctrl Pts',(-0.090744749826965,-0.124912017153538,
0.566541326091639));
#19687=CARTESIAN_POINT('Ctrl Pts',(-0.0410086302256792,-0.148848627462727,
0.5691887154659));
#19688=CARTESIAN_POINT('Ctrl Pts',(0.00739494322942312,-0.146403732988417,
0.57183610484016));
#19689=CARTESIAN_POINT('Ctrl Pts',(0.0557985166845234,-0.143958838514108,
0.57448349421442));
#19690=CARTESIAN_POINT('Ctrl Pts',(0.10286954399344,-0.1151324392563,0.57713088358868));
#19691=CARTESIAN_POINT('Ctrl Pts',(0.127047076753504,-0.0731285067993286,
0.579778272962939));
#19692=CARTESIAN_POINT('Ctrl Pts',(0.151224609513568,-0.031124574342357,
0.5824256623372));
#19693=CARTESIAN_POINT('Ctrl Pts',(0.15250864772478,0.0240568913137802,
0.58507305171146));
#19694=CARTESIAN_POINT('Ctrl Pts',(0.130311035929276,0.0671399443948921,
0.58772044108572));
#19695=CARTESIAN_POINT('Ctrl Pts',(0.108113424133771,0.110222997476006,
0.59036783045998));
#19696=CARTESIAN_POINT('Ctrl Pts',(0.0624341623315493,0.141207637982093,
0.593015219834239));
#19697=CARTESIAN_POINT('Ctrl Pts',(0.0141966988324609,0.145901308974836,
0.595662609208499));
#19698=CARTESIAN_POINT('Ctrl Pts',(-0.0340407646666261,0.150594979967579,
0.598309998582759));
#19699=CARTESIAN_POINT('Ctrl Pts',(-0.0848364298625779,0.128997681446978,
0.60095738795702));
#19700=CARTESIAN_POINT('Ctrl Pts',(-0.114923272877171,0.091002085522857,
0.60360477733128));
#19701=CARTESIAN_POINT('Ctrl Pts',(-0.135113526827902,0.0655045372973676,
0.60538135002609));
#19702=CARTESIAN_POINT('Ctrl Pts',(-0.14597798884013,0.0326223532682757,
0.6071579227209));
#19703=CARTESIAN_POINT('Ctrl Pts',(-0.146218520919543,-0.000115076211918358,
0.608934495415711));
#19704=CARTESIAN_POINT('Origin',(0.,0.,0.));
#19705=CARTESIAN_POINT('',(-0.146586033401767,-2.15382961294558E-5,0.66606550458429));
#19706=CARTESIAN_POINT('',(-0.146582846697157,-3.00215943766004E-5,0.65893449541571));
#19707=CARTESIAN_POINT('',(-0.14635,-1.79227059055215E-17,0.));
#19708=CARTESIAN_POINT('Ctrl Pts',(-0.146586033401767,-2.15382961294558E-5,
0.66606550458429));
#19709=CARTESIAN_POINT('Ctrl Pts',(-0.146488810225965,0.0472697707580183,
0.663482448132491));
#19710=CARTESIAN_POINT('Ctrl Pts',(-0.121516563758978,0.0946492637554097,
0.660899391680692));
#19711=CARTESIAN_POINT('Ctrl Pts',(-0.0824084263440199,0.121233094478226,
0.658316335228893));
#19712=CARTESIAN_POINT('Ctrl Pts',(-0.0423423130056393,0.148468111155377,
0.655670005349791));
#19713=CARTESIAN_POINT('Ctrl Pts',(0.0125607065496858,0.153876184485078,
0.653023675470689));
#19714=CARTESIAN_POINT('Ctrl Pts',(0.0571706564953393,0.134981954220393,
0.650377345591587));
#19715=CARTESIAN_POINT('Ctrl Pts',(0.101780606440992,0.116087723955709,
0.647731015712485));
#19716=CARTESIAN_POINT('Ctrl Pts',(0.136097486776972,0.0728911900966409,
0.645084685833384));
#19717=CARTESIAN_POINT('Ctrl Pts',(0.144413921474191,0.0251640857912735,
0.642438355954282));
#19718=CARTESIAN_POINT('Ctrl Pts',(0.152730356171409,-0.0225630185140953,
0.63979202607518));
#19719=CARTESIAN_POINT('Ctrl Pts',(0.135046345229863,-0.0748206932657649,
0.637145696196077));
#19720=CARTESIAN_POINT('Ctrl Pts',(0.0994561386758346,-0.10768977857233,
0.634499366316975));
#19721=CARTESIAN_POINT('Ctrl Pts',(0.0638659321218069,-0.140558863878895,
0.631853036437873));
#19722=CARTESIAN_POINT('Ctrl Pts',(0.0103695299552984,-0.154039359740357,
0.629206706558772));
#19723=CARTESIAN_POINT('Ctrl Pts',(-0.0365469229059137,-0.141961031115491,
0.62656037667967));
#19724=CARTESIAN_POINT('Ctrl Pts',(-0.0834633757671259,-0.129882702490626,
0.623914046800568));
#19725=CARTESIAN_POINT('Ctrl Pts',(-0.123799879323041,-0.0922455493794331,
0.621267716921466));
#19726=CARTESIAN_POINT('Ctrl Pts',(-0.139093781291504,-0.0462766888972804,
0.618621387042364));
#19727=CARTESIAN_POINT('Ctrl Pts',(-0.14401750805555,-0.0314774500153124,
0.617769426223006));
#19728=CARTESIAN_POINT('Ctrl Pts',(-0.14634567687575,-0.0158146654998378,
0.616917465403648));
#19729=CARTESIAN_POINT('Ctrl Pts',(-0.146227179098081,-0.000117664897458569,
0.616065504584291));
#19730=CARTESIAN_POINT('Ctrl Pts',(-0.146218520919543,-0.000115076211918358,
0.608934495415711));
#19731=CARTESIAN_POINT('Ctrl Pts',(-0.1463364217222,-0.0161618722236638,
0.60980531209516));
#19732=CARTESIAN_POINT('Ctrl Pts',(-0.143901781624712,-0.032173889023867,
0.61067612877461));
#19733=CARTESIAN_POINT('Ctrl Pts',(-0.138761720114909,-0.0472643972675185,
0.611546945454059));
#19734=CARTESIAN_POINT('Ctrl Pts',(-0.123135303504819,-0.0931413908061287,
0.614194334828319));
#19735=CARTESIAN_POINT('Ctrl Pts',(-0.0825044494514074,-0.130501484555709,
0.616841724202579));
#19736=CARTESIAN_POINT('Ctrl Pts',(-0.0354801761942514,-0.142231836504824,
0.619489113576839));
#19737=CARTESIAN_POINT('Ctrl Pts',(0.0115440970629072,-0.15396218845394,
0.6221365029511));
#19738=CARTESIAN_POINT('Ctrl Pts',(0.0649617895238099,-0.140062798602586,
0.624783892325359));
#19739=CARTESIAN_POINT('Ctrl Pts',(0.100304854137336,-0.106900301471969,
0.627431281699619));
#19740=CARTESIAN_POINT('Ctrl Pts',(0.135647918750861,-0.0737378043413545,
0.630078671073879));
#19741=CARTESIAN_POINT('Ctrl Pts',(0.15291635551701,-0.0213121999314781,
0.63272606044814));
#19742=CARTESIAN_POINT('Ctrl Pts',(0.144200333369931,0.026362891994447,
0.6353734498224));
#19743=CARTESIAN_POINT('Ctrl Pts',(0.135484311222852,0.0740379839203748,
0.63802083919666));
#19744=CARTESIAN_POINT('Ctrl Pts',(0.100783830162543,0.11696256336235,0.640668228570919));
#19745=CARTESIAN_POINT('Ctrl Pts',(0.055993492972559,0.135474968031154,
0.643315617945179));
#19746=CARTESIAN_POINT('Ctrl Pts',(0.0112031557825773,0.153987372699956,
0.64596300731944));
#19747=CARTESIAN_POINT('Ctrl Pts',(-0.04367703753708,0.148087602595587,
0.6486103966937));
#19748=CARTESIAN_POINT('Ctrl Pts',(-0.0835091394177698,0.120478055479053,
0.65125778606796));
#19749=CARTESIAN_POINT('Ctrl Pts',(-0.122009894390588,0.0937913289882395,
0.653816689183877));
#19750=CARTESIAN_POINT('Ctrl Pts',(-0.146451680634158,0.0468218259492564,
0.656375592299793));
#19751=CARTESIAN_POINT('Ctrl Pts',(-0.146582846697157,-3.00215943766004E-5,
0.65893449541571));
#19752=CARTESIAN_POINT('Origin',(0.,0.,0.));
#19753=CARTESIAN_POINT('',(-0.146290249280603,0.000131112932912382,0.716065504584291));
#19754=CARTESIAN_POINT('',(-0.146307221518699,0.000133045872591754,0.708934495415711));
#19755=CARTESIAN_POINT('',(-0.14635,-1.79227059055215E-17,0.));
#19756=CARTESIAN_POINT('Ctrl Pts',(-0.146290249280603,0.000131112932912382,
0.716065504584291));
#19757=CARTESIAN_POINT('Ctrl Pts',(-0.146406294125046,0.0134819654399978,
0.715340090619538));
#19758=CARTESIAN_POINT('Ctrl Pts',(-0.144729088574721,0.0268041890186768,
0.714614676654786));
#19759=CARTESIAN_POINT('Ctrl Pts',(-0.141142411757643,0.0395908011096033,
0.713889262690033));
#19760=CARTESIAN_POINT('Ctrl Pts',(-0.128058117149462,0.0862367098911347,
0.711242932810931));
#19761=CARTESIAN_POINT('Ctrl Pts',(-0.0895623832093418,0.125754646095387,
0.708596602931829));
#19762=CARTESIAN_POINT('Ctrl Pts',(-0.0432753130058998,0.140056628595385,
0.705950273052727));
#19763=CARTESIAN_POINT('Ctrl Pts',(0.00301175719754219,0.154358611095384,
0.703303943173625));
#19764=CARTESIAN_POINT('Ctrl Pts',(0.0570901636643063,0.143444639891129,
0.700657613294523));
#19765=CARTESIAN_POINT('Ctrl Pts',(0.0942073689518517,0.11231021130972,
0.698011283415421));
#19766=CARTESIAN_POINT('Ctrl Pts',(0.131324574239397,0.0811757827283121,
0.695364953536319));
#19767=CARTESIAN_POINT('Ctrl Pts',(0.151480578347723,0.0298208967697505,
0.692718623657217));
#19768=CARTESIAN_POINT('Ctrl Pts',(0.145449661086834,-0.0182485073085286,
0.690072293778115));
#19769=CARTESIAN_POINT('Ctrl Pts',(0.139418743825945,-0.0663179113868083,
0.687425963899014));
#19770=CARTESIAN_POINT('Ctrl Pts',(0.107200905195838,-0.111101833584806,
0.684779634019911));
#19771=CARTESIAN_POINT('Ctrl Pts',(0.0635427568131047,-0.132101968137704,
0.68213330414081));
#19772=CARTESIAN_POINT('Ctrl Pts',(0.0198846084303716,-0.153102102690602,
0.679486974261708));
#19773=CARTESIAN_POINT('Ctrl Pts',(-0.0352138497049885,-0.150318449598402,
0.676840644382606));
#19774=CARTESIAN_POINT('Ctrl Pts',(-0.0765331864534889,-0.125025130675956,
0.674194314503504));
#19775=CARTESIAN_POINT('Ctrl Pts',(-0.117852523201989,-0.0997318117535095,
0.671547984624402));
#19776=CARTESIAN_POINT('Ctrl Pts',(-0.14539273856363,-0.0519288270008166,
0.6689016547453));
#19777=CARTESIAN_POINT('Ctrl Pts',(-0.146548242683733,-0.00349635461217019,
0.666255324866198));
#19778=CARTESIAN_POINT('Ctrl Pts',(-0.146575870647472,-0.00233834005587287,
0.666192051438896));
#19779=CARTESIAN_POINT('Ctrl Pts',(-0.146588414938392,-0.00117996563262623,
0.666128778011593));
#19780=CARTESIAN_POINT('Ctrl Pts',(-0.146586033401767,-2.15382961294558E-5,
0.66606550458429));
#19781=CARTESIAN_POINT('Ctrl Pts',(-0.146582846697157,-3.00215943766004E-5,
0.65893449541571));
#19782=CARTESIAN_POINT('Ctrl Pts',(-0.146587382388275,-0.00165014728799839,
0.659022981674053));
#19783=CARTESIAN_POINT('Ctrl Pts',(-0.146562848415234,-0.00327013229389975,
0.659111467932396));
#19784=CARTESIAN_POINT('Ctrl Pts',(-0.146508820881567,-0.00488913307276392,
0.659199954190739));
#19785=CARTESIAN_POINT('Ctrl Pts',(-0.144892390022949,-0.0533274503793473,
0.661847343564999));
#19786=CARTESIAN_POINT('Ctrl Pts',(-0.116875517863988,-0.100884760863813,
0.66449473293926));
#19787=CARTESIAN_POINT('Ctrl Pts',(-0.0752913709948059,-0.125777373450206,
0.66714212231352));
#19788=CARTESIAN_POINT('Ctrl Pts',(-0.0337072241256252,-0.150669986036599,
0.66978951168778));
#19789=CARTESIAN_POINT('Ctrl Pts',(0.021444197453776,-0.15289790072492,
0.672436901062039));
#19790=CARTESIAN_POINT('Ctrl Pts',(0.0649007096996251,-0.131440618146733,
0.675084290436299));
#19791=CARTESIAN_POINT('Ctrl Pts',(0.108357221945475,-0.109983335568545,
0.677731679810559));
#19792=CARTESIAN_POINT('Ctrl Pts',(0.140118824857774,-0.0648408557238465,
0.68037906918482));
#19793=CARTESIAN_POINT('Ctrl Pts',(0.145637072805965,-0.0166907532130915,
0.68302645855908));
#19794=CARTESIAN_POINT('Ctrl Pts',(0.151155320754156,0.031459349297663,
0.68567384793334));
#19795=CARTESIAN_POINT('Ctrl Pts',(0.130430213738242,0.0826170744744734,
0.688321237307599));
#19796=CARTESIAN_POINT('Ctrl Pts',(0.0929549153570804,0.113349556369966,
0.690968626681859));
#19797=CARTESIAN_POINT('Ctrl Pts',(0.0554796169759186,0.14408203826546,
0.693616016056119));
#19798=CARTESIAN_POINT('Ctrl Pts',(0.00125412722950909,0.154389276879634,
0.69626340543038));
#19799=CARTESIAN_POINT('Ctrl Pts',(-0.0448834941801804,0.139550027475769,
0.69891079480464));
#19800=CARTESIAN_POINT('Ctrl Pts',(-0.0910211155898686,0.124710778071904,
0.7015581841789));
#19801=CARTESIAN_POINT('Ctrl Pts',(-0.129070868662838,0.0847250406500019,
0.704205573553159));
#19802=CARTESIAN_POINT('Ctrl Pts',(-0.141604011991841,0.0379083368947344,
0.706852962927419));
#19803=CARTESIAN_POINT('Ctrl Pts',(-0.144888775625201,0.0256383259412015,
0.707546807090183));
#19804=CARTESIAN_POINT('Ctrl Pts',(-0.146420824649375,0.0128991016161637,
0.708240651252947));
#19805=CARTESIAN_POINT('Ctrl Pts',(-0.146307221518699,0.000133045872591754,
0.708934495415711));
#19806=CARTESIAN_POINT('Origin',(0.,0.,0.));
#19807=CARTESIAN_POINT('',(-0.1461301977291,-5.61458017395017E-5,0.766065504584291));
#19808=CARTESIAN_POINT('',(-0.14612241379348,-4.54149644099216E-5,0.758934495415711));
#19809=CARTESIAN_POINT('',(-0.14635,-1.79227059055215E-17,0.));
#19810=CARTESIAN_POINT('Ctrl Pts',(-0.1461301977291,-5.61458017395017E-5,
0.766065504584291));
#19811=CARTESIAN_POINT('Ctrl Pts',(-0.14603380141711,0.0278870014676159,
0.764551403227483));
#19812=CARTESIAN_POINT('Ctrl Pts',(-0.138327245009168,0.0558793842949389,
0.763037301870675));
#19813=CARTESIAN_POINT('Ctrl Pts',(-0.123350675409043,0.079203679241543,
0.761523200513867));
#19814=CARTESIAN_POINT('Ctrl Pts',(-0.0971747899961838,0.119969628197767,
0.758876870634766));
#19815=CARTESIAN_POINT('Ctrl Pts',(-0.048790709571801,0.146475657227381,
0.756230540755664));
#19816=CARTESIAN_POINT('Ctrl Pts',(-0.000344588961360588,0.146589539830481,
0.753584210876561));
#19817=CARTESIAN_POINT('Ctrl Pts',(0.0481015316490792,0.14670342243358,
0.750937880997459));
#19818=CARTESIAN_POINT('Ctrl Pts',(0.0966096924455767,0.120425158610167,
0.748291551118357));
#19819=CARTESIAN_POINT('Ctrl Pts',(0.122976945064223,0.0797827231418903,
0.745645221239255));
#19820=CARTESIAN_POINT('Ctrl Pts',(0.149344197682869,0.0391402876736125,
0.742998891360154));
#19821=CARTESIAN_POINT('Ctrl Pts',(0.153570542123663,-0.01586631943953,
0.740352561481052));
#19822=CARTESIAN_POINT('Ctrl Pts',(0.133721514043982,-0.0600597087159893,
0.73770623160195));
#19823=CARTESIAN_POINT('Ctrl Pts',(0.113872485964301,-0.104253097992448,
0.735059901722848));
#19824=CARTESIAN_POINT('Ctrl Pts',(0.0699480853641458,-0.137633269432224,
0.732413571843746));
#19825=CARTESIAN_POINT('Ctrl Pts',(0.0220532014503509,-0.144921593405036,
0.729767241964644));
#19826=CARTESIAN_POINT('Ctrl Pts',(-0.0258416824634434,-0.152209917377848,
0.727120912085542));
#19827=CARTESIAN_POINT('Ctrl Pts',(-0.0777070496908773,-0.133406393883698,
0.724474582206441));
#19828=CARTESIAN_POINT('Ctrl Pts',(-0.109803305666473,-0.0971176914572187,
0.721828252327339));
#19829=CARTESIAN_POINT('Ctrl Pts',(-0.133101311474982,-0.0707764758164216,
0.71990733641299));
#19830=CARTESIAN_POINT('Ctrl Pts',(-0.14598295937539,-0.0352223077304616,
0.71798642049864));
#19831=CARTESIAN_POINT('Ctrl Pts',(-0.146290249280603,0.000131112932912382,
0.716065504584291));
#19832=CARTESIAN_POINT('Ctrl Pts',(-0.146307221518699,0.000133045872591754,
0.708934495415711));
#19833=CARTESIAN_POINT('Ctrl Pts',(-0.145987367488279,-0.0358102803178394,
0.710888040627207));
#19834=CARTESIAN_POINT('Ctrl Pts',(-0.132622002370819,-0.0719663061161047,
0.712841585838703));
#19835=CARTESIAN_POINT('Ctrl Pts',(-0.1086007072861,-0.0984612847532928,
0.7147951310502));
#19836=CARTESIAN_POINT('Ctrl Pts',(-0.0760477256663158,-0.134366532557423,
0.71744252042446));
#19837=CARTESIAN_POINT('Ctrl Pts',(-0.0239252288417074,-0.152529358077047,
0.720089909798719));
#19838=CARTESIAN_POINT('Ctrl Pts',(0.0238920022682765,-0.144630254255197,
0.722737299172979));
#19839=CARTESIAN_POINT('Ctrl Pts',(0.071709233378259,-0.136731150433346,
0.725384688547239));
#19840=CARTESIAN_POINT('Ctrl Pts',(0.115221198773618,-0.102770117270024,
0.7280320779215));
#19841=CARTESIAN_POINT('Ctrl Pts',(0.134497183226257,-0.058303052428779,
0.730679467295759));
#19842=CARTESIAN_POINT('Ctrl Pts',(0.153773167678896,-0.0138359875875333,
0.733326856670019));
#19843=CARTESIAN_POINT('Ctrl Pts',(0.148813171188813,0.0411371089316358,
0.735974246044279));
#19844=CARTESIAN_POINT('Ctrl Pts',(0.121889126928366,0.0814357351225549,
0.738621635418539));
#19845=CARTESIAN_POINT('Ctrl Pts',(0.0949650826679194,0.121734361313473,
0.741269024792799));
#19846=CARTESIAN_POINT('Ctrl Pts',(0.0460769906371109,0.147358517176143,
0.74391641416706));
#19847=CARTESIAN_POINT('Ctrl Pts',(-0.00238189178169058,0.146571023090686,
0.74656380354132));
#19848=CARTESIAN_POINT('Ctrl Pts',(-0.0508407742004934,0.14578352900523,
0.74921119291558));
#19849=CARTESIAN_POINT('Ctrl Pts',(-0.0988704470072894,0.118584384971644,
0.751858582289839));
#19850=CARTESIAN_POINT('Ctrl Pts',(-0.124470852918682,0.0774321960944291,
0.754505971664099));
#19851=CARTESIAN_POINT('Ctrl Pts',(-0.138745545153454,0.0544858868428234,
0.75598214624797));
#19852=CARTESIAN_POINT('Ctrl Pts',(-0.146046671909043,0.027201385339783,
0.757458320831841));
#19853=CARTESIAN_POINT('Ctrl Pts',(-0.14612241379348,-4.54149644099216E-5,
0.758934495415711));
#19854=CARTESIAN_POINT('Origin',(0.,0.,0.));
#19855=CARTESIAN_POINT('',(-0.146495788566881,-0.000101744904923998,0.816065504584291));
#19856=CARTESIAN_POINT('',(-0.146473871348434,-0.000110945968026819,0.808934495415711));
#19857=CARTESIAN_POINT('',(-0.14635,-1.79227059055215E-17,0.));
#19858=CARTESIAN_POINT('Ctrl Pts',(-0.146495788566881,-0.000101744904923998,
0.816065504584291));
#19859=CARTESIAN_POINT('Ctrl Pts',(-0.14616118452328,0.0421270051992108,
0.813762715835428));
#19860=CARTESIAN_POINT('Ctrl Pts',(-0.126905337350145,0.0846218946815527,
0.811459927086565));
#19861=CARTESIAN_POINT('Ctrl Pts',(-0.0947343415465314,0.111866064832055,
0.809157138337701));
#19862=CARTESIAN_POINT('Ctrl Pts',(-0.0577639214515077,0.143174651664521,
0.806510808458599));
#19863=CARTESIAN_POINT('Ctrl Pts',(-0.00373742343573488,0.154342745753647,
0.803864478579497));
#19864=CARTESIAN_POINT('Ctrl Pts',(0.0426163743729279,0.140258534729872,
0.801218148700395));
#19865=CARTESIAN_POINT('Ctrl Pts',(0.0889701721815907,0.126174323706097,
0.798571818821294));
#19866=CARTESIAN_POINT('Ctrl Pts',(0.127651269783143,0.0868378075694234,
0.795925488942192));
#19867=CARTESIAN_POINT('Ctrl Pts',(0.140954720244851,0.040253928627653,
0.79327915906309));
#19868=CARTESIAN_POINT('Ctrl Pts',(0.154258170706558,-0.00632995031411615,
0.790632829183988));
#19869=CARTESIAN_POINT('Ctrl Pts',(0.14218397402842,-0.060161192060982,
0.787986499304886));
#19870=CARTESIAN_POINT('Ctrl Pts',(0.110258679990485,-0.0966003903512828,
0.785340169425784));
#19871=CARTESIAN_POINT('Ctrl Pts',(0.0783333859525485,-0.133039588641585,
0.782693839546682));
#19872=CARTESIAN_POINT('Ctrl Pts',(0.0265569945548152,-0.152086743475322,
0.780047509667581));
#19873=CARTESIAN_POINT('Ctrl Pts',(-0.021371625274328,-0.14502367242074,
0.777401179788479));
#19874=CARTESIAN_POINT('Ctrl Pts',(-0.0693002451034712,-0.137960601366157,
0.774754849909377));
#19875=CARTESIAN_POINT('Ctrl Pts',(-0.113381093364023,-0.104787304423254,
0.772108520030274));
#19876=CARTESIAN_POINT('Ctrl Pts',(-0.133437672293631,-0.0606877215103841,
0.769462190151172));
#19877=CARTESIAN_POINT('Ctrl Pts',(-0.1420188514214,-0.0418197768941368,
0.768329961628878));
#19878=CARTESIAN_POINT('Ctrl Pts',(-0.146202281842484,-0.0209517273285418,
0.767197733106584));
#19879=CARTESIAN_POINT('Ctrl Pts',(-0.1461301977291,-5.61458017395017E-5,
0.766065504584291));
#19880=CARTESIAN_POINT('Ctrl Pts',(-0.14612241379348,-4.54149644099216E-5,
0.758934495415711));
#19881=CARTESIAN_POINT('Ctrl Pts',(-0.146182508321779,-0.0216633562673834,
0.760105710206101));
#19882=CARTESIAN_POINT('Ctrl Pts',(-0.141694203021096,-0.0432575645610501,
0.76127692499649));
#19883=CARTESIAN_POINT('Ctrl Pts',(-0.132531725405586,-0.0626424774360703,
0.76244813978688));
#19884=CARTESIAN_POINT('Ctrl Pts',(-0.111821052965107,-0.106459728368519,
0.76509552916114));
#19885=CARTESIAN_POINT('Ctrl Pts',(-0.067228569068158,-0.138988996512573,
0.767742918535399));
#19886=CARTESIAN_POINT('Ctrl Pts',(-0.0191799219195066,-0.145330206128911,
0.770390307909659));
#19887=CARTESIAN_POINT('Ctrl Pts',(0.0288687252291434,-0.151671415745249,
0.773037697283919));
#19888=CARTESIAN_POINT('Ctrl Pts',(0.080373535629496,-0.131824566833873,
0.77568508665818));
#19889=CARTESIAN_POINT('Ctrl Pts',(0.111742660473083,-0.0948805356683208,
0.77833247603244));
#19890=CARTESIAN_POINT('Ctrl Pts',(0.14311178531667,-0.0579365045027684,
0.7809798654067));
#19891=CARTESIAN_POINT('Ctrl Pts',(0.154345224603492,-0.00389529108304171,
0.783627254780959));
#19892=CARTESIAN_POINT('Ctrl Pts',(0.140297486112651,0.0424894529122293,
0.786274644155219));
#19893=CARTESIAN_POINT('Ctrl Pts',(0.126249747621811,0.0888741969075009,
0.788922033529479));
#19894=CARTESIAN_POINT('Ctrl Pts',(0.0869208313533056,0.127602471478316,
0.79156942290374));
#19895=CARTESIAN_POINT('Ctrl Pts',(0.0403254011646538,0.140934737517831,
0.794216812278));
#19896=CARTESIAN_POINT('Ctrl Pts',(-0.00627002902399674,0.154267003557346,
0.79686420165226));
#19897=CARTESIAN_POINT('Ctrl Pts',(-0.0601319731327944,0.142203261065564,
0.799511591026519));
#19898=CARTESIAN_POINT('Ctrl Pts',(-0.0965888940360299,0.110269323781398,
0.802158980400779));
#19899=CARTESIAN_POINT('Ctrl Pts',(-0.127690529151203,0.0830262752573849,
0.804417485405756));
#19900=CARTESIAN_POINT('Ctrl Pts',(-0.146124951115714,0.0413218847513699,
0.806675990410734));
#19901=CARTESIAN_POINT('Ctrl Pts',(-0.146473871348434,-0.000110945968026819,
0.808934495415711));
#19902=CARTESIAN_POINT('Origin',(0.,0.,0.));
#19903=CARTESIAN_POINT('',(-0.146444331750498,0.000119944961782359,0.866065504584291));
#19904=CARTESIAN_POINT('',(-0.146471560192382,0.00011177640072981,0.858934495415711));
#19905=CARTESIAN_POINT('',(-0.14635,-1.79227059055215E-17,0.));
#19906=CARTESIAN_POINT('Ctrl Pts',(-0.146444331750498,0.000119944961782359,
0.866065504584291));
#19907=CARTESIAN_POINT('Ctrl Pts',(-0.146516681599632,0.00829054204730037,
0.865620358322474));
#19908=CARTESIAN_POINT('Ctrl Pts',(-0.145891801779796,0.0164500693154795,
0.865175212060658));
#19909=CARTESIAN_POINT('Ctrl Pts',(-0.14453063157077,0.0244848619971339,
0.864730065798841));
#19910=CARTESIAN_POINT('Ctrl Pts',(-0.136438672357208,0.0722505376181754,
0.862083735919739));
#19911=CARTESIAN_POINT('Ctrl Pts',(-0.102325254887189,0.115607931012472,
0.859437406040638));
#19912=CARTESIAN_POINT('Ctrl Pts',(-0.0578046270350215,0.134711681091902,
0.856791076161536));
#19913=CARTESIAN_POINT('Ctrl Pts',(-0.0132839991828526,0.153815431171333,
0.854144746282434));
#19914=CARTESIAN_POINT('Ctrl Pts',(0.0416438390514653,0.148665537935894,
0.851498416403331));
#19915=CARTESIAN_POINT('Ctrl Pts',(0.081837551941475,0.121619188541491,
0.848852086524229));
#19916=CARTESIAN_POINT('Ctrl Pts',(0.122031264831484,0.0945728391470885,
0.846205756645128));
#19917=CARTESIAN_POINT('Ctrl Pts',(0.147490852377186,0.0456300335937214,
0.843559426766026));
#19918=CARTESIAN_POINT('Ctrl Pts',(0.146563060809277,-0.0028073360113171,
0.840913096886925));
#19919=CARTESIAN_POINT('Ctrl Pts',(0.145635269241369,-0.0512447056163556,
0.838266767007823));
#19920=CARTESIAN_POINT('Ctrl Pts',(0.118320098559852,-0.0991766392730661,
0.835620437128721));
#19921=CARTESIAN_POINT('Ctrl Pts',(0.0771201321287374,-0.124663936845065,
0.832974107249619));
#19922=CARTESIAN_POINT('Ctrl Pts',(0.035920165697623,-0.150151234417064,
0.830327777370517));
#19923=CARTESIAN_POINT('Ctrl Pts',(-0.0191645964830881,-0.153193895904352,
0.827681447491415));
#19924=CARTESIAN_POINT('Ctrl Pts',(-0.0629209921278279,-0.132399247274726,
0.825035117612313));
#19925=CARTESIAN_POINT('Ctrl Pts',(-0.106677387772568,-0.111604598645101,
0.822388787733211));
#19926=CARTESIAN_POINT('Ctrl Pts',(-0.139105416881337,-0.0669726398985626,
0.819742457854109));
#19927=CARTESIAN_POINT('Ctrl Pts',(-0.145362260348583,-0.0189321207373897,
0.817096127975007));
#19928=CARTESIAN_POINT('Ctrl Pts',(-0.146174510965348,-0.0126955988357878,
0.816752586844768));
#19929=CARTESIAN_POINT('Ctrl Pts',(-0.146545706411658,-0.00640163348415362,
0.81640904571453));
#19930=CARTESIAN_POINT('Ctrl Pts',(-0.146495788566881,-0.000101744904923998,
0.816065504584291));
#19931=CARTESIAN_POINT('Ctrl Pts',(-0.146473871348434,-0.000110945968026819,
0.808934495415711));
#19932=CARTESIAN_POINT('Ctrl Pts',(-0.146533950748007,-0.00724512552769256,
0.809323379784994));
#19933=CARTESIAN_POINT('Ctrl Pts',(-0.146057826922151,-0.0143712538186879,
0.809712264154277));
#19934=CARTESIAN_POINT('Ctrl Pts',(-0.145017839345608,-0.0214141189368497,
0.81010114852356));
#19935=CARTESIAN_POINT('Ctrl Pts',(-0.137937966054276,-0.0693594922943736,
0.81274853789782));
#19936=CARTESIAN_POINT('Ctrl Pts',(-0.104726321773939,-0.113446106932874,
0.81539592727208));
#19937=CARTESIAN_POINT('Ctrl Pts',(-0.0605955455659204,-0.133480028752914,
0.818043316646339));
#19938=CARTESIAN_POINT('Ctrl Pts',(-0.0164647693578984,-0.153513950572954,
0.820690706020599));
#19939=CARTESIAN_POINT('Ctrl Pts',(0.0385851387778066,-0.149495179574532,
0.823338095394859));
#19940=CARTESIAN_POINT('Ctrl Pts',(0.0793384931690736,-0.12326451930694,
0.825985484769119));
#19941=CARTESIAN_POINT('Ctrl Pts',(0.120091847560339,-0.0970338590393495,
0.828632874143379));
#19942=CARTESIAN_POINT('Ctrl Pts',(0.146548648207165,-0.0485913095025905,
0.83128026351764));
#19943=CARTESIAN_POINT('Ctrl Pts',(0.146590321408106,-0.000126046730599388,
0.833927652891899));
#19944=CARTESIAN_POINT('Ctrl Pts',(0.146631994609047,0.0483392160413931,
0.836575042266159));
#19945=CARTESIAN_POINT('Ctrl Pts',(0.120258540364101,0.0968271920486179,
0.839222431640419));
#19946=CARTESIAN_POINT('Ctrl Pts',(0.0795503554414038,0.123127897600245,
0.841869821014679));
#19947=CARTESIAN_POINT('Ctrl Pts',(0.0388421705187073,0.149428603151872,
0.844517210388939));
#19948=CARTESIAN_POINT('Ctrl Pts',(-0.0162007450817403,0.153542038247903,
0.8471645997632));
#19949=CARTESIAN_POINT('Ctrl Pts',(-0.0603659086281491,0.133584038319734,
0.84981198913746));
#19950=CARTESIAN_POINT('Ctrl Pts',(-0.104531072174558,0.113626038391565,
0.85245937851172));
#19951=CARTESIAN_POINT('Ctrl Pts',(-0.137818483666928,0.0695966034391962,
0.855106767885979));
#19952=CARTESIAN_POINT('Ctrl Pts',(-0.144980798768897,0.0216634763286692,
0.857754157260239));
#19953=CARTESIAN_POINT('Ctrl Pts',(-0.146045237806912,0.0145398171508471,
0.858147603312063));
#19954=CARTESIAN_POINT('Ctrl Pts',(-0.146532654486068,0.00732993751956911,
0.858541049363887));
#19955=CARTESIAN_POINT('Ctrl Pts',(-0.146471560192382,0.00011177640072981,
0.858934495415711));
#19956=CARTESIAN_POINT('Origin',(0.,0.,0.));
#19957=CARTESIAN_POINT('',(-0.146114231148477,2.69008449349656E-5,0.916065504584291));
#19958=CARTESIAN_POINT('',(-0.146121644853617,4.41067432152685E-5,0.908934495415711));
#19959=CARTESIAN_POINT('',(-0.14635,-1.79227059055215E-17,0.));
#19960=CARTESIAN_POINT('Ctrl Pts',(-0.146114231148477,2.69008449349656E-5,
0.916065504584291));
#19961=CARTESIAN_POINT('Ctrl Pts',(-0.146151635159142,0.0228038459942234,
0.914831670930419));
#19962=CARTESIAN_POINT('Ctrl Pts',(-0.141147538069067,0.0455652341090756,
0.913597837276548));
#19963=CARTESIAN_POINT('Ctrl Pts',(-0.131015765267123,0.0657531838068269,
0.912364003622676));
#19964=CARTESIAN_POINT('Ctrl Pts',(-0.109285110563454,0.109052354902802,
0.909717673743574));
#19965=CARTESIAN_POINT('Ctrl Pts',(-0.0639662294071284,0.140513248471977,
0.907071343864472));
#19966=CARTESIAN_POINT('Ctrl Pts',(-0.015802286694576,0.145735718560985,
0.90442501398537));
#19967=CARTESIAN_POINT('Ctrl Pts',(0.0323616560179757,0.150958188649994,
0.901778684106268));
#19968=CARTESIAN_POINT('Ctrl Pts',(0.0833706602867547,0.129942235258839,
0.899132354227166));
#19969=CARTESIAN_POINT('Ctrl Pts',(0.113877102345416,0.0923071908936453,
0.896486024348064));
#19970=CARTESIAN_POINT('Ctrl Pts',(0.144383544404078,0.0546721465284523,
0.893839694468962));
#19971=CARTESIAN_POINT('Ctrl Pts',(0.15438742425262,0.000418011189221586,
0.891193364589861));
#19972=CARTESIAN_POINT('Ctrl Pts',(0.139309808695705,-0.0456222438118789,
0.888547034710759));
#19973=CARTESIAN_POINT('Ctrl Pts',(0.124232193138789,-0.0916624988129813,
0.885900704831657));
#19974=CARTESIAN_POINT('Ctrl Pts',(0.0840730821764119,-0.129488873475953,
0.883254374952555));
#19975=CARTESIAN_POINT('Ctrl Pts',(0.0372139327097935,-0.141787641004198,
0.880608045073453));
#19976=CARTESIAN_POINT('Ctrl Pts',(-0.00964521675682358,-0.154086408532443,
0.877961715194351));
#19977=CARTESIAN_POINT('Ctrl Pts',(-0.0632044047276821,-0.140857568925962,
0.875315385315249));
#19978=CARTESIAN_POINT('Ctrl Pts',(-0.0989487482345592,-0.108156170198829,
0.872669055436147));
#19979=CARTESIAN_POINT('Ctrl Pts',(-0.128680439645858,-0.0809555616469925,
0.870467871818862));
#19980=CARTESIAN_POINT('Ctrl Pts',(-0.146086572253705,-0.0402824710322022,
0.868266688201576));
#19981=CARTESIAN_POINT('Ctrl Pts',(-0.146444331750498,0.000119944961782359,
0.866065504584291));
#19982=CARTESIAN_POINT('Ctrl Pts',(-0.146471560192382,0.00011177640072981,
0.858934495415711));
#19983=CARTESIAN_POINT('Ctrl Pts',(-0.146121567926216,-0.0412390669452651,
0.861188438738147));
#19984=CARTESIAN_POINT('Ctrl Pts',(-0.127770397964496,-0.0828616943330661,
0.863442382060584));
#19985=CARTESIAN_POINT('Ctrl Pts',(-0.096778382793969,-0.110103055552942,
0.86569632538302));
#19986=CARTESIAN_POINT('Ctrl Pts',(-0.0603764330055066,-0.142099641055337,
0.86834371475728));
#19987=CARTESIAN_POINT('Ctrl Pts',(-0.00653531471701479,-0.154255992791443,
0.870991104131539));
#19988=CARTESIAN_POINT('Ctrl Pts',(0.040082974241256,-0.14100387723139,
0.873638493505799));
#19989=CARTESIAN_POINT('Ctrl Pts',(0.0867012631995282,-0.127751761671338,
0.876285882880059));
#19990=CARTESIAN_POINT('Ctrl Pts',(0.12609672282758,-0.0890911788151255,
0.878933272254319));
#19991=CARTESIAN_POINT('Ctrl Pts',(0.140224208991091,-0.042730661487191,
0.88158066162858));
#19992=CARTESIAN_POINT('Ctrl Pts',(0.154351695154603,0.00362985584074295,
0.88422805100284));
#19993=CARTESIAN_POINT('Ctrl Pts',(0.143211207853577,0.057690307640398,
0.886875440377099));
#19994=CARTESIAN_POINT('Ctrl Pts',(0.111905662524754,0.09468823006692,0.889522829751359));
#19995=CARTESIAN_POINT('Ctrl Pts',(0.0806001171959318,0.131686152493442,
0.892170219125619));
#19996=CARTESIAN_POINT('Ctrl Pts',(0.0291295138393125,0.15162154554683,
0.894817608499879));
#19997=CARTESIAN_POINT('Ctrl Pts',(-0.0189299673197759,0.145362975188259,
0.897464997874139));
#19998=CARTESIAN_POINT('Ctrl Pts',(-0.0669894484788628,0.139104404829688,
0.9001123872484));
#19999=CARTESIAN_POINT('Ctrl Pts',(-0.11163780744042,0.10665187105916,0.902759776622659));
#20000=CARTESIAN_POINT('Ctrl Pts',(-0.132423802349956,0.0628703013313112,
0.905407165996919));
#20001=CARTESIAN_POINT('Ctrl Pts',(-0.141655418982822,0.043425734493323,
0.90658294246985));
#20002=CARTESIAN_POINT('Ctrl Pts',(-0.146180218154578,0.0217465313827003,
0.907758718942781));
#20003=CARTESIAN_POINT('Ctrl Pts',(-0.146121644853617,4.41067432152685E-5,
0.908934495415711));
#20004=CARTESIAN_POINT('Origin',(0.,0.,0.));
#20005=CARTESIAN_POINT('',(-0.146345621585321,-0.000133809880645736,0.966065504584291));
#20006=CARTESIAN_POINT('',(-0.146309694201085,-0.000133223314395004,0.958934495415711));
#20007=CARTESIAN_POINT('',(-0.14635,-1.79227059055215E-17,0.));
#20008=CARTESIAN_POINT('Ctrl Pts',(-0.146345621585321,-0.000133809880645736,
0.966065504584291));
#20009=CARTESIAN_POINT('Ctrl Pts',(-0.146004672532387,0.0370537288701324,
0.964042983538364));
#20010=CARTESIAN_POINT('Ctrl Pts',(-0.131578083002406,0.0744765756810296,
0.962020462492437));
#20011=CARTESIAN_POINT('Ctrl Pts',(-0.106003654037246,0.101251356830495,
0.959997941446511));
#20012=CARTESIAN_POINT('Ctrl Pts',(-0.0725412702228666,0.136284319036219,
0.957351611567409));
#20013=CARTESIAN_POINT('Ctrl Pts',(-0.0199938687303381,0.153087872523943,
0.954705281688306));
#20014=CARTESIAN_POINT('Ctrl Pts',(0.0275867780614433,0.143970766496025,
0.952058951809204));
#20015=CARTESIAN_POINT('Ctrl Pts',(0.0751674248532248,0.134853660468108,
0.949412621930102));
#20016=CARTESIAN_POINT('Ctrl Pts',(0.11778131694426,0.0998158949245492,
0.946766292051));
#20017=CARTESIAN_POINT('Ctrl Pts',(0.135923405490256,0.0548948063954655,
0.944119962171899));
#20018=CARTESIAN_POINT('Ctrl Pts',(0.154065494036253,0.0099737178663825,
0.941473632292797));
#20019=CARTESIAN_POINT('Ctrl Pts',(0.147735779037212,-0.0448306936482241,
0.938827302413695));
#20020=CARTESIAN_POINT('Ctrl Pts',(0.119831470632095,-0.0844335867733556,
0.936180972534593));
#20021=CARTESIAN_POINT('Ctrl Pts',(0.0919271622269763,-0.124036479898489,
0.933534642655491));
#20022=CARTESIAN_POINT('Ctrl Pts',(0.0424482604157787,-0.148437854634144,
0.93088831277639));
#20023=CARTESIAN_POINT('Ctrl Pts',(-0.00595796300272124,-0.146468817862788,
0.928241982897288));
#20024=CARTESIAN_POINT('Ctrl Pts',(-0.0543641864212212,-0.144499781091432,
0.925595653018186));
#20025=CARTESIAN_POINT('Ctrl Pts',(-0.101697731447024,-0.116160332813065,
0.922949323139084));
#20026=CARTESIAN_POINT('Ctrl Pts',(-0.126293289834417,-0.0744218843624929,
0.920302993259982));
#20027=CARTESIAN_POINT('Ctrl Pts',(-0.139421333187579,-0.052143709087005,
0.918890497034752));
#20028=CARTESIAN_POINT('Ctrl Pts',(-0.146071410932229,-0.0260482098028304,
0.917478000809521));
#20029=CARTESIAN_POINT('Ctrl Pts',(-0.146114231148477,2.69008449349656E-5,
0.916065504584291));
#20030=CARTESIAN_POINT('Ctrl Pts',(-0.146121644853617,4.41067432152685E-5,
0.908934495415711));
#20031=CARTESIAN_POINT('Ctrl Pts',(-0.146048333958771,-0.027118852224649,
0.910406108317041));
#20032=CARTESIAN_POINT('Ctrl Pts',(-0.138795050353101,-0.0543181883240968,
0.91187772121837));
#20033=CARTESIAN_POINT('Ctrl Pts',(-0.124603830013468,-0.0772180274565794,
0.9133493341197));
#20034=CARTESIAN_POINT('Ctrl Pts',(-0.0990742319099257,-0.118414180831446,
0.91599672349396));
#20035=CARTESIAN_POINT('Ctrl Pts',(-0.0510914048453256,-0.145695881896007,
0.91864411286822));
#20036=CARTESIAN_POINT('Ctrl Pts',(-0.00263394834681351,-0.146566710184873,
0.92129150224248));
#20037=CARTESIAN_POINT('Ctrl Pts',(0.0458235081516972,-0.147437538473739,
0.92393889161674));
#20038=CARTESIAN_POINT('Ctrl Pts',(0.0947555940841207,-0.121897493986912,
0.926586280990999));
#20039=CARTESIAN_POINT('Ctrl Pts',(0.121748900601314,-0.0816452290135895,
0.929233670365259));
#20040=CARTESIAN_POINT('Ctrl Pts',(0.148742207118509,-0.0413929640402651,
0.931881059739519));
#20041=CARTESIAN_POINT('Ctrl Pts',(0.153796734220472,0.0135715214195569,
0.93452844911378));
#20042=CARTESIAN_POINT('Ctrl Pts',(0.134597248858856,0.0580716696672091,
0.93717583848804));
#20043=CARTESIAN_POINT('Ctrl Pts',(0.115397763497239,0.102571817914861,
0.9398232278623));
#20044=CARTESIAN_POINT('Ctrl Pts',(0.0719442656720451,0.136607628950342,
0.942470617236559));
#20045=CARTESIAN_POINT('Ctrl Pts',(0.0241406894609324,0.144588953003544,
0.945118006610819));
#20046=CARTESIAN_POINT('Ctrl Pts',(-0.023662886750181,0.152570277056746,
0.947765395985079));
#20047=CARTESIAN_POINT('Ctrl Pts',(-0.0758165413472122,0.134497114127667,
0.950412785359339));
#20048=CARTESIAN_POINT('Ctrl Pts',(-0.108431221550465,0.0986479012011113,
0.953060174733599));
#20049=CARTESIAN_POINT('Ctrl Pts',(-0.132554242808212,0.0721325001574252,
0.955018281627637));
#20050=CARTESIAN_POINT('Ctrl Pts',(-0.145988218858404,0.0358924841874147,
0.956976388521674));
#20051=CARTESIAN_POINT('Ctrl Pts',(-0.146309694201085,-0.000133223314395004,
0.958934495415711));
#20052=CARTESIAN_POINT('Origin',(0.,0.,0.));
#20053=CARTESIAN_POINT('',(-0.146565171121453,5.44893591410845E-5,1.01606550458429));
#20054=CARTESIAN_POINT('',(-0.146582076026177,3.15354312248815E-5,1.00893449541571));
#20055=CARTESIAN_POINT('',(-0.14635,-1.79227059055215E-17,0.));
#20056=CARTESIAN_POINT('Ctrl Pts',(-0.146565171121453,5.44893591410845E-5,
1.01606550458429));
#20057=CARTESIAN_POINT('Ctrl Pts',(-0.146579596851449,0.00307427920823236,
1.01590062602541));
#20058=CARTESIAN_POINT('Ctrl Pts',(-0.146494352296349,0.00609323927190738,
1.01573574746653));
#20059=CARTESIAN_POINT('Ctrl Pts',(-0.146306854564556,0.00910583530985269,
1.01557086890765));
#20060=CARTESIAN_POINT('Ctrl Pts',(-0.143297482980539,0.0574585317612167,
1.01292453902855));
#20061=CARTESIAN_POINT('Ctrl Pts',(-0.11394685994478,0.104171803331984,
1.01027820914945));
#20062=CARTESIAN_POINT('Ctrl Pts',(-0.0716892273871119,0.127864250695428,
1.00763187927034));
#20063=CARTESIAN_POINT('Ctrl Pts',(-0.0294315948294418,0.151556698058874,
1.00498554939124));
#20064=CARTESIAN_POINT('Ctrl Pts',(0.0257330472501378,0.152228321214993,
1.00233921951214));
#20065=CARTESIAN_POINT('Ctrl Pts',(0.0685549742796134,0.129571707678744,
0.999692889633039));
#20066=CARTESIAN_POINT('Ctrl Pts',(0.111376901309088,0.106915094142495,
0.997046559753937));
#20067=CARTESIAN_POINT('Ctrl Pts',(0.141856113288459,0.0609302439138786,
0.994400229874835));
#20068=CARTESIAN_POINT('Ctrl Pts',(0.146041795372579,0.0126651464112397,
0.991753899995733));
#20069=CARTESIAN_POINT('Ctrl Pts',(0.150227477456699,-0.0355999510913994,
0.989107570116631));
#20070=CARTESIAN_POINT('Ctrl Pts',(0.128119629645567,-0.0861452958680607,
0.986461240237529));
#20071=CARTESIAN_POINT('Ctrl Pts',(0.0898373616998479,-0.115835488396583,
0.983814910358427));
#20072=CARTESIAN_POINT('Ctrl Pts',(0.051555093754129,-0.145525680925106,
0.981168580479325));
#20073=CARTESIAN_POINT('Ctrl Pts',(-0.00290159432617693,-0.154360721205491,
0.978522250600224));
#20074=CARTESIAN_POINT('Ctrl Pts',(-0.0486070196525971,-0.138296672301818,
0.975875920721122));
#20075=CARTESIAN_POINT('Ctrl Pts',(-0.0943124449790173,-0.122232623398145,
0.97322959084202));
#20076=CARTESIAN_POINT('Ctrl Pts',(-0.131266607551552,-0.081269485310415,
0.970583260962917));
#20077=CARTESIAN_POINT('Ctrl Pts',(-0.142555005769704,-0.0341567308046872,
0.967936931083816));
#20078=CARTESIAN_POINT('Ctrl Pts',(-0.145215975052668,-0.0230510282813687,
0.967313122250641));
#20079=CARTESIAN_POINT('Ctrl Pts',(-0.146450780951306,-0.0116036114945705,
0.966689313417466));
#20080=CARTESIAN_POINT('Ctrl Pts',(-0.146345621585321,-0.000133809880645736,
0.966065504584291));
#20081=CARTESIAN_POINT('Ctrl Pts',(-0.146309694201085,-0.000133223314395004,
0.958934495415711));
#20082=CARTESIAN_POINT('Ctrl Pts',(-0.146422858258782,-0.0128148032088542,
0.959623777895933));
#20083=CARTESIAN_POINT('Ctrl Pts',(-0.14491119500038,-0.0254698272036438,
0.960313060376156));
#20084=CARTESIAN_POINT('Ctrl Pts',(-0.141668994059001,-0.037664762585484,
0.961002342856379));
#20085=CARTESIAN_POINT('Ctrl Pts',(-0.129216380554811,-0.0845029505214961,
0.963649732230639));
#20086=CARTESIAN_POINT('Ctrl Pts',(-0.0912354477369537,-0.12455406346949,
0.966297121604899));
#20087=CARTESIAN_POINT('Ctrl Pts',(-0.0451234138007503,-0.1394726343957,
0.968944510979159));
#20088=CARTESIAN_POINT('Ctrl Pts',(0.00098862013545236,-0.154391205321909,
0.97159190035342));
#20089=CARTESIAN_POINT('Ctrl Pts',(0.055231755190001,-0.144177234226336,
0.974239289727679));
#20090=CARTESIAN_POINT('Ctrl Pts',(0.0927598492034174,-0.113509244531313,
0.976886679101939));
#20091=CARTESIAN_POINT('Ctrl Pts',(0.130287943216833,-0.0828412548362905,
0.979534068476199));
#20092=CARTESIAN_POINT('Ctrl Pts',(0.151100996189117,-0.0317192465418168,
0.982181457850459));
#20093=CARTESIAN_POINT('Ctrl Pts',(0.145665560755875,0.0164402745715088,
0.984828847224719));
#20094=CARTESIAN_POINT('Ctrl Pts',(0.140230125322634,0.0645997956848379,
0.987476236598979));
#20095=CARTESIAN_POINT('Ctrl Pts',(0.108546201483865,0.109796829617019,
0.990123625973239));
#20096=CARTESIAN_POINT('Ctrl Pts',(0.0651266538643092,0.131328813193254,
0.992771015347499));
#20097=CARTESIAN_POINT('Ctrl Pts',(0.0217071062447581,0.152860796769488,
0.995418404721759));
#20098=CARTESIAN_POINT('Ctrl Pts',(-0.0334480651555777,0.15072772998978,
0.998065794096019));
#20099=CARTESIAN_POINT('Ctrl Pts',(-0.0750749586823209,0.125906667008376,
1.00071318347028));
#20100=CARTESIAN_POINT('Ctrl Pts',(-0.116701852209067,0.101085604026969,
1.00336057284454));
#20101=CARTESIAN_POINT('Ctrl Pts',(-0.144800467862219,0.053576544843864,
1.0060079622188));
#20102=CARTESIAN_POINT('Ctrl Pts',(-0.146500196332402,0.00514107896046776,
1.00865535159306));
#20103=CARTESIAN_POINT('Ctrl Pts',(-0.146559936783033,0.00343871495990628,
1.00874839953394));
#20104=CARTESIAN_POINT('Ctrl Pts',(-0.146587066279139,0.00173520655478852,
1.00884144747483));
#20105=CARTESIAN_POINT('Ctrl Pts',(-0.146582076026177,3.15354312248815E-5,
1.00893449541571));
#20106=CARTESIAN_POINT('Origin',(0.,0.,0.));
#20107=CARTESIAN_POINT('',(-0.146184049129756,9.96948043307314E-5,1.06606550458429));
#20108=CARTESIAN_POINT('',(-0.146216477546812,0.000114345603752017,1.05893449541571));
#20109=CARTESIAN_POINT('',(-0.14635,-1.79227059055215E-17,0.));
#20110=CARTESIAN_POINT('Ctrl Pts',(-0.146184049129756,9.96948043307314E-5,
1.06606550458429));
#20111=CARTESIAN_POINT('Ctrl Pts',(-0.146294264763128,0.0176817746259609,
1.06511193863336));
#20112=CARTESIAN_POINT('Ctrl Pts',(-0.143360807533043,0.0352283113603788,
1.06415837268242));
#20113=CARTESIAN_POINT('Ctrl Pts',(-0.13721959397524,0.0515693218739058,
1.06320480673148));
#20114=CARTESIAN_POINT('Ctrl Pts',(-0.120176538991979,0.0969187854681546,
1.06055847685238));
#20115=CARTESIAN_POINT('Ctrl Pts',(-0.0784283132238915,0.132983650068601,
1.05791214697328));
#20116=CARTESIAN_POINT('Ctrl Pts',(-0.0310837364199337,0.143256459747686,
1.05526581709418));
#20117=CARTESIAN_POINT('Ctrl Pts',(0.0162608403840241,0.153529269426771,
1.05261948721508));
#20118=CARTESIAN_POINT('Ctrl Pts',(0.0692017682238519,0.138010024184496,
1.04997315733597));
#20119=CARTESIAN_POINT('Ctrl Pts',(0.103507151520239,0.103802126728842,
1.04732682745687));
#20120=CARTESIAN_POINT('Ctrl Pts',(0.137812534816628,0.0695942292731864,
1.04468049757777));
#20121=CARTESIAN_POINT('Ctrl Pts',(0.153482373569574,0.01669767960415,1.04203416769867));
#20122=CARTESIAN_POINT('Ctrl Pts',(0.143344336052008,-0.0306759392859165,
1.03938783781957));
#20123=CARTESIAN_POINT('Ctrl Pts',(0.133206298534443,-0.0780495581759789,
1.03674150794047));
#20124=CARTESIAN_POINT('Ctrl Pts',(0.0972603847463712,-0.119900246287072,
1.03409517806136));
#20125=CARTESIAN_POINT('Ctrl Pts',(0.0519596049571008,-0.137072285243832,
1.03144884818226));
#20126=CARTESIAN_POINT('Ctrl Pts',(0.00665882516783032,-0.154244324200591,
1.02880251830316));
#20127=CARTESIAN_POINT('Ctrl Pts',(-0.0479968206226384,-0.146737714003016,
1.02615618842406));
#20128=CARTESIAN_POINT('Ctrl Pts',(-0.0869905834517384,-0.11798834823825,
1.02350985854496));
#20129=CARTESIAN_POINT('Ctrl Pts',(-0.123554854979944,-0.0910302005802824,
1.02102840722473));
#20130=CARTESIAN_POINT('Ctrl Pts',(-0.146348061346918,-0.0453938791777224,
1.01854695590451));
#20131=CARTESIAN_POINT('Ctrl Pts',(-0.146565171121453,5.44893591410845E-5,
1.01606550458429));
#20132=CARTESIAN_POINT('Ctrl Pts',(-0.146582076026177,3.15354312248815E-5,
1.00893449541571));
#20133=CARTESIAN_POINT('Ctrl Pts',(-0.146445084172466,-0.0467374494427972,
1.01148883684909));
#20134=CARTESIAN_POINT('Ctrl Pts',(-0.122102455869861,-0.0936290599181376,
1.01404317828246));
#20135=CARTESIAN_POINT('Ctrl Pts',(-0.0837162036049941,-0.120334265578335,
1.01659751971584));
#20136=CARTESIAN_POINT('Ctrl Pts',(-0.0439316411201867,-0.14801227165006,
1.0192449090901));
#20137=CARTESIAN_POINT('Ctrl Pts',(0.0109383251366414,-0.154006411209824,
1.02189229846436));
#20138=CARTESIAN_POINT('Ctrl Pts',(0.0557604321169594,-0.135571060438576,
1.02453968783862));
#20139=CARTESIAN_POINT('Ctrl Pts',(0.100582539097277,-0.11713570966733,
1.02718707721288));
#20140=CARTESIAN_POINT('Ctrl Pts',(0.135356786801084,-0.0742708685650716,
1.02983446658714));
#20141=CARTESIAN_POINT('Ctrl Pts',(0.144154783532934,-0.0266108361928598,
1.0324818559614));
#20142=CARTESIAN_POINT('Ctrl Pts',(0.152952780264784,0.0210491961793507,
1.03512924533566));
#20143=CARTESIAN_POINT('Ctrl Pts',(0.135774526024679,0.0735044198215165,
1.03777663470992));
#20144=CARTESIAN_POINT('Ctrl Pts',(0.100488543649143,0.106727647840587,
1.04042402408418));
#20145=CARTESIAN_POINT('Ctrl Pts',(0.0652025612736062,0.139950875859659,
1.04307141345844));
#20146=CARTESIAN_POINT('Ctrl Pts',(0.0118088507626404,0.153942108255635,
1.0457188028327));
#20147=CARTESIAN_POINT('Ctrl Pts',(-0.0352355257975899,0.142292641904202,
1.04836619220696));
#20148=CARTESIAN_POINT('Ctrl Pts',(-0.0822799023578202,0.130643175552769,
1.05101358158122));
#20149=CARTESIAN_POINT('Ctrl Pts',(-0.122974944967313,0.0933530104539243,
1.05366097095548));
#20150=CARTESIAN_POINT('Ctrl Pts',(-0.138680233730631,0.0475029577050484,
1.05630836032974));
#20151=CARTESIAN_POINT('Ctrl Pts',(-0.143873300563147,0.0323423075707214,
1.05718373869173));
#20152=CARTESIAN_POINT('Ctrl Pts',(-0.146334133026589,0.0162457690968458,
1.05805911705372));
#20153=CARTESIAN_POINT('Ctrl Pts',(-0.146216477546812,0.000114345603752017,
1.05893449541571));
#20154=CARTESIAN_POINT('Origin',(0.,0.,0.));
#20155=CARTESIAN_POINT('',(-0.146204073634541,-0.000109175101205505,1.11606550458429));
#20156=CARTESIAN_POINT('',(-0.146170555016798,-9.22629125885076E-5,1.10893449541571));
#20157=CARTESIAN_POINT('',(-0.14635,-1.79227059055215E-17,0.));
#20158=CARTESIAN_POINT('Ctrl Pts',(-0.146204073634541,-0.000109175101205505,
1.11606550458429));
#20159=CARTESIAN_POINT('Ctrl Pts',(-0.145981599624502,0.032003853555373,
1.1143232512413));
#20160=CARTESIAN_POINT('Ctrl Pts',(-0.135565881201595,0.0642480963468658,
1.11258099789831));
#20161=CARTESIAN_POINT('Ctrl Pts',(-0.11609067353381,0.0895073597405865,
1.11083874455532));
#20162=CARTESIAN_POINT('Ctrl Pts',(-0.0865095427755784,0.127873963375947,
1.10819241467622));
#20163=CARTESIAN_POINT('Ctrl Pts',(-0.0360273159486943,0.150125560802435,
1.10554608479712));
#20164=CARTESIAN_POINT('Ctrl Pts',(0.0122494975033169,0.14607724579886,
1.10289975491801));
#20165=CARTESIAN_POINT('Ctrl Pts',(0.0605263109553308,0.142028930795284,
1.10025342503891));
#20166=CARTESIAN_POINT('Ctrl Pts',(0.10659771103247,0.111680703361642,1.09760709515981));
#20167=CARTESIAN_POINT('Ctrl Pts',(0.129376093089052,0.0689234246557527,
1.09496076528071));
#20168=CARTESIAN_POINT('Ctrl Pts',(0.152154475145634,0.0261661459498645,
1.09231443540161));
#20169=CARTESIAN_POINT('Ctrl Pts',(0.151639839181659,-0.0290001840282729,
1.0896681055225));
#20170=CARTESIAN_POINT('Ctrl Pts',(0.128067742174483,-0.0713250681289163,
1.0870217756434));
#20171=CARTESIAN_POINT('Ctrl Pts',(0.104495645167307,-0.11364995222956,
1.0843754457643));
#20172=CARTESIAN_POINT('Ctrl Pts',(0.0578660871169326,-0.143133390452712,
1.0817291158852));
#20173=CARTESIAN_POINT('Ctrl Pts',(0.00952215035475689,-0.146280349267719,
1.0790827860061));
#20174=CARTESIAN_POINT('Ctrl Pts',(-0.0388217864074202,-0.149427308082725,
1.07643645612699));
#20175=CARTESIAN_POINT('Ctrl Pts',(-0.0888801018813974,-0.126237787489585,
1.07379012624789));
#20176=CARTESIAN_POINT('Ctrl Pts',(-0.117740317519168,-0.0873259958989869,
1.07114379636879));
#20177=CARTESIAN_POINT('Ctrl Pts',(-0.136201180005177,-0.0624354946409797,
1.06945103244062));
#20178=CARTESIAN_POINT('Ctrl Pts',(-0.145988395071105,-0.0311118962502767,
1.06775826851246));
#20179=CARTESIAN_POINT('Ctrl Pts',(-0.146184049129756,9.96948043307314E-5,
1.06606550458429));
#20180=CARTESIAN_POINT('Ctrl Pts',(-0.146216477546812,0.000114345603752017,
1.05893449541571));
#20181=CARTESIAN_POINT('Ctrl Pts',(-0.145978309898544,-0.0325401742182177,
1.06070650642798));
#20182=CARTESIAN_POINT('Ctrl Pts',(-0.135174246449945,-0.06533764273189,
1.06247851744025));
#20183=CARTESIAN_POINT('Ctrl Pts',(-0.115079600404687,-0.0908043159161929,
1.06425052845252));
#20184=CARTESIAN_POINT('Ctrl Pts',(-0.0850581433982766,-0.128851596389654,
1.06689791782678));
#20185=CARTESIAN_POINT('Ctrl Pts',(-0.0342996944683099,-0.150536216937668,
1.06954530720104));
#20186=CARTESIAN_POINT('Ctrl Pts',(0.0139457694684962,-0.145925507476389,
1.0721926965753));
#20187=CARTESIAN_POINT('Ctrl Pts',(0.0621912334052997,-0.14131479801511,
1.07484008594956));
#20188=CARTESIAN_POINT('Ctrl Pts',(0.107923712348941,-0.110408758544542,
1.07748747532382));
#20189=CARTESIAN_POINT('Ctrl Pts',(0.1301953818052,-0.0673639426912374,
1.08013486469808));
#20190=CARTESIAN_POINT('Ctrl Pts',(0.15246705126146,-0.024319126837932,
1.08278225407234));
#20191=CARTESIAN_POINT('Ctrl Pts',(0.151277911230334,0.0308644653981125,
1.0854296434466));
#20192=CARTESIAN_POINT('Ctrl Pts',(0.127172648928576,0.0729099141598672,
1.08807703282086));
#20193=CARTESIAN_POINT('Ctrl Pts',(0.103067386626818,0.114955362921624,
1.09072442219512));
#20194=CARTESIAN_POINT('Ctrl Pts',(0.0560460020544268,0.143862668209093,
1.09337181156938));
#20195=CARTESIAN_POINT('Ctrl Pts',(0.00764670469074742,0.146390799320458,
1.09601920094364));
#20196=CARTESIAN_POINT('Ctrl Pts',(-0.0407525926729279,0.148918930431823,
1.0986665903179));
#20197=CARTESIAN_POINT('Ctrl Pts',(-0.0905298028278899,0.125067887367091,
1.10131397969216));
#20198=CARTESIAN_POINT('Ctrl Pts',(-0.11888440661962,0.0857626730052823,
1.10396136906642));
#20199=CARTESIAN_POINT('Ctrl Pts',(-0.136639133674055,0.0611510311732957,
1.10561907784952));
#20200=CARTESIAN_POINT('Ctrl Pts',(-0.145994366384503,0.0304800321277272,
1.10727678663261));
#20201=CARTESIAN_POINT('Ctrl Pts',(-0.146170555016798,-9.22629125885076E-5,
1.10893449541571));
#20202=CARTESIAN_POINT('Origin',(0.,0.,0.));
#20203=CARTESIAN_POINT('',(-0.146577386142569,-3.88073511912723E-5,1.16606550458429));
#20204=CARTESIAN_POINT('',(-0.146552328192774,-6.73160170860698E-5,1.15893449541571));
#20205=CARTESIAN_POINT('',(-0.14635,-1.79227059055215E-17,0.));
#20206=CARTESIAN_POINT('Ctrl Pts',(-0.146577386142569,-3.88073511912723E-5,
1.16606550458429));
#20207=CARTESIAN_POINT('Ctrl Pts',(-0.146413350709018,0.0463056768050285,
1.16353456384924));
#20208=CARTESIAN_POINT('Ctrl Pts',(-0.122574225104448,0.0927954474992645,
1.1610036231142));
#20209=CARTESIAN_POINT('Ctrl Pts',(-0.0847742546295189,0.119590709008994,
1.15847268237915));
#20210=CARTESIAN_POINT('Ctrl Pts',(-0.0452509303920754,0.147607604138013,
1.15582635250005));
#20211=CARTESIAN_POINT('Ctrl Pts',(0.00953524646069181,0.154093252855687,
1.15318002262095));
#20212=CARTESIAN_POINT('Ctrl Pts',(0.0545077808453859,0.136079071706768,
1.15053369274185));
#20213=CARTESIAN_POINT('Ctrl Pts',(0.0994803152300801,0.118064890557849,
1.14788736286275));
#20214=CARTESIAN_POINT('Ctrl Pts',(0.134639207146701,0.0755508795423365,
1.14524103298364));
#20215=CARTESIAN_POINT('Ctrl Pts',(0.14389167861853,0.027996370364851,1.14259470310454));
#20216=CARTESIAN_POINT('Ctrl Pts',(0.15314415009036,-0.0195581388126345,
1.13994837322544));
#20217=CARTESIAN_POINT('Ctrl Pts',(0.136490201117397,-0.0721531461520931,
1.13730204334634));
#20218=CARTESIAN_POINT('Ctrl Pts',(0.101552606157185,-0.105715089329518,
1.13465571346724));
#20219=CARTESIAN_POINT('Ctrl Pts',(0.0666150111969725,-0.139277032506943,
1.13200938358813));
#20220=CARTESIAN_POINT('Ctrl Pts',(0.0133937702495101,-0.153805911522335,
1.12936305370903));
#20221=CARTESIAN_POINT('Ctrl Pts',(-0.033750917386428,-0.142651629870951,
1.12671672382993));
#20222=CARTESIAN_POINT('Ctrl Pts',(-0.0808956050223675,-0.131497348219567,
1.12407039395083));
#20223=CARTESIAN_POINT('Ctrl Pts',(-0.121963739346782,-0.094659905901407,
1.12142406407173));
#20224=CARTESIAN_POINT('Ctrl Pts',(-0.1381577891642,-0.0490003798202082,
1.11877773419262));
#20225=CARTESIAN_POINT('Ctrl Pts',(-0.143690228857438,-0.0334015285560649,
1.11787365765651));
#20226=CARTESIAN_POINT('Ctrl Pts',(-0.146319518115206,-0.0167730178360648,
1.1169695811204));
#20227=CARTESIAN_POINT('Ctrl Pts',(-0.146204073634541,-0.000109175101205505,
1.11606550458429));
#20228=CARTESIAN_POINT('Ctrl Pts',(-0.146170555016798,-9.22629125885076E-5,
1.10893449541571));
#20229=CARTESIAN_POINT('Ctrl Pts',(-0.146275742653821,-0.0183444476975235,
1.10992417600687));
#20230=CARTESIAN_POINT('Ctrl Pts',(-0.143109248288425,-0.0365614514641733,
1.11091385659804));
#20231=CARTESIAN_POINT('Ctrl Pts',(-0.136505188007283,-0.0534328725168923,
1.1119035371892));
#20232=CARTESIAN_POINT('Ctrl Pts',(-0.118839368174718,-0.0985638180183679,
1.11455092656346));
#20233=CARTESIAN_POINT('Ctrl Pts',(-0.0765757310810901,-0.134066323362434,
1.11719831593772));
#20234=CARTESIAN_POINT('Ctrl Pts',(-0.0290731934694857,-0.143678417446031,
1.11984570531198));
#20235=CARTESIAN_POINT('Ctrl Pts',(0.01842934414212,-0.153290511529629,
1.12249309468624));
#20236=CARTESIAN_POINT('Ctrl Pts',(0.071170782271703,-0.137012194352758,
1.1251404840605));
#20237=CARTESIAN_POINT('Ctrl Pts',(0.10499283308901,-0.102299771349957,
1.12778787343476));
#20238=CARTESIAN_POINT('Ctrl Pts',(0.138814883906317,-0.0675873483471558,
1.13043526280902));
#20239=CARTESIAN_POINT('Ctrl Pts',(0.153717547411349,-0.0144408195184256,
1.13308265218328));
#20240=CARTESIAN_POINT('Ctrl Pts',(0.142874638214406,0.0327959749574983,
1.13573004155754));
#20241=CARTESIAN_POINT('Ctrl Pts',(0.132031729017462,0.0800327694334235,
1.1383774309318));
#20242=CARTESIAN_POINT('Ctrl Pts',(0.0954432471185425,0.121359829556542,
1.14102482030606));
#20243=CARTESIAN_POINT('Ctrl Pts',(0.0498685966661331,0.137847238945365,
1.14367220968032));
#20244=CARTESIAN_POINT('Ctrl Pts',(0.00429394621372511,0.154334648334189,
1.14631959905458));
#20245=CARTESIAN_POINT('Ctrl Pts',(-0.0502668727921719,0.145982406988718,
1.14896698842884));
#20246=CARTESIAN_POINT('Ctrl Pts',(-0.0888222026239048,0.116616270474356,
1.1516143778031));
#20247=CARTESIAN_POINT('Ctrl Pts',(-0.124357782404925,0.0895501633622979,
1.1540544170073));
#20248=CARTESIAN_POINT('Ctrl Pts',(-0.146296868742479,0.0446329749882746,
1.15649445621151));
#20249=CARTESIAN_POINT('Ctrl Pts',(-0.146552328192774,-6.73160170860698E-5,
1.15893449541571));
#20250=CARTESIAN_POINT('Origin',(0.,0.,0.));
#20251=CARTESIAN_POINT('',(-0.146318311025392,0.000133437649768732,1.21606550458429));
#20252=CARTESIAN_POINT('',(-0.146373054956946,0.000132657382717961,1.20893449541571));
#20253=CARTESIAN_POINT('',(-0.14635,-1.79227059055215E-17,0.));
#20254=CARTESIAN_POINT('Ctrl Pts',(-0.146318311025392,0.000133437649768732,
1.21606550458429));
#20255=CARTESIAN_POINT('Ctrl Pts',(-0.146429658069886,0.0125190846592594,
1.21539220633629));
#20256=CARTESIAN_POINT('Ctrl Pts',(-0.144988168643405,0.0248791929292086,
1.21471890808829));
#20257=CARTESIAN_POINT('Ctrl Pts',(-0.141892968227885,0.0368102906365087,
1.21404560984029));
#20258=CARTESIAN_POINT('Ctrl Pts',(-0.129727599662405,0.083704249513052,
1.21139927996119));
#20259=CARTESIAN_POINT('Ctrl Pts',(-0.0920156607298113,0.123970842060419,
1.20875295008209));
#20260=CARTESIAN_POINT('Ctrl Pts',(-0.0460184991925076,0.139179415364965,
1.20610662020299));
#20261=CARTESIAN_POINT('Ctrl Pts',(-2.13376552038805E-5,0.15438798866951,
1.20346029032389));
#20262=CARTESIAN_POINT('Ctrl Pts',(0.0542610464868107,0.144538542731236,
1.20081396044478));
#20263=CARTESIAN_POINT('Ctrl Pts',(0.091982751999895,0.114139323915075,
1.19816763056568));
#20264=CARTESIAN_POINT('Ctrl Pts',(0.129704457512977,0.0837401050989159,
1.19552130068658));
#20265=CARTESIAN_POINT('Ctrl Pts',(0.150865484397133,0.0327911134048729,
1.19287497080748));
#20266=CARTESIAN_POINT('Ctrl Pts',(0.145780097726084,-0.0153874961003253,
1.19022864092838));
#20267=CARTESIAN_POINT('Ctrl Pts',(0.140694711055036,-0.063566105605525,
1.18758231104927));
#20268=CARTESIAN_POINT('Ctrl Pts',(0.109362910828785,-0.108974332921877,
1.18493598117017));
#20269=CARTESIAN_POINT('Ctrl Pts',(0.0661257549466402,-0.130828118009858,
1.18228965129107));
#20270=CARTESIAN_POINT('Ctrl Pts',(0.0228885990644955,-0.152681903097838,
1.17964332141197));
#20271=CARTESIAN_POINT('Ctrl Pts',(-0.0322539124735426,-0.150981245957443,
1.17699699153287));
#20272=CARTESIAN_POINT('Ctrl Pts',(-0.0740621845924981,-0.126504564117865,
1.17435066165376));
#20273=CARTESIAN_POINT('Ctrl Pts',(-0.115870456711455,-0.102027882278287,
1.17170433177466));
#20274=CARTESIAN_POINT('Ctrl Pts',(-0.144344489411329,-0.0547751757395235,
1.16905800189556));
#20275=CARTESIAN_POINT('Ctrl Pts',(-0.146451269950206,-0.00637475169995868,
1.16641167201646));
#20276=CARTESIAN_POINT('Ctrl Pts',(-0.146543132875163,-0.00426432565444621,
1.1662962828724));
#20277=CARTESIAN_POINT('Ctrl Pts',(-0.146584864748453,-0.00215171749738942,
1.16618089372835));
#20278=CARTESIAN_POINT('Ctrl Pts',(-0.146577386142569,-3.88073511912723E-5,
1.16606550458429));
#20279=CARTESIAN_POINT('Ctrl Pts',(-0.146552328192774,-6.73160170860698E-5,
1.15893449541571));
#20280=CARTESIAN_POINT('Ctrl Pts',(-0.146574036680232,-0.00386586684592084,
1.15914184558577));
#20281=CARTESIAN_POINT('Ctrl Pts',(-0.1464391612665,-0.00766285139452399,
1.15934919575582));
#20282=CARTESIAN_POINT('Ctrl Pts',(-0.146142739258869,-0.0114471821958193,
1.15955654592588));
#20283=CARTESIAN_POINT('Ctrl Pts',(-0.142358105404532,-0.0597644666683822,
1.16220393530014));
#20284=CARTESIAN_POINT('Ctrl Pts',(-0.112238997038288,-0.106019003930254,
1.1648513246744));
#20285=CARTESIAN_POINT('Ctrl Pts',(-0.0695815129186611,-0.129023839960917,
1.16749871404866));
#20286=CARTESIAN_POINT('Ctrl Pts',(-0.026924028799035,-0.15202867599158,
1.17014610342292));
#20287=CARTESIAN_POINT('Ctrl Pts',(0.0282718310739737,-0.151783810791035,
1.17279349279718));
#20288=CARTESIAN_POINT('Ctrl Pts',(0.0707235276354612,-0.128401405199111,
1.17544088217144));
#20289=CARTESIAN_POINT('Ctrl Pts',(0.11317522419695,-0.105018999607187,
1.1780882715457));
#20290=CARTESIAN_POINT('Ctrl Pts',(0.142882757446916,-0.0584990536238821,
1.18073566091996));
#20291=CARTESIAN_POINT('Ctrl Pts',(0.146238551171451,-0.0101500920973681,
1.18338305029422));
#20292=CARTESIAN_POINT('Ctrl Pts',(0.149594344895986,0.0381988694291446,
1.18603043966848));
#20293=CARTESIAN_POINT('Ctrl Pts',(0.12659839909509,0.0883768464988665,
1.18867782904274));
#20294=CARTESIAN_POINT('Ctrl Pts',(0.0877840381772113,0.117399748124142,
1.191325218417));
#20295=CARTESIAN_POINT('Ctrl Pts',(0.0489696772593311,0.146422649749419,
1.19397260779126));
#20296=CARTESIAN_POINT('Ctrl Pts',(-0.00566309877553352,0.154290475930249,
1.19661999716552));
#20297=CARTESIAN_POINT('Ctrl Pts',(-0.0510896721842483,0.137399358129564,
1.19926738653978));
#20298=CARTESIAN_POINT('Ctrl Pts',(-0.0965162455929618,0.12050824032888,
1.20191477591404));
#20299=CARTESIAN_POINT('Ctrl Pts',(-0.132736616375526,0.0788581785466829,
1.2045621652883));
#20300=CARTESIAN_POINT('Ctrl Pts',(-0.143159994183491,0.0315270405159292,
1.20720955466256));
#20301=CARTESIAN_POINT('Ctrl Pts',(-0.145423823013163,0.021247302336111,
1.20778453491361));
#20302=CARTESIAN_POINT('Ctrl Pts',(-0.146470795531708,0.0106995851133921,
1.20835951516466));
#20303=CARTESIAN_POINT('Ctrl Pts',(-0.146373054956946,0.000132657382717961,
1.20893449541571));
#20304=CARTESIAN_POINT('Origin',(0.,0.,0.));
#20305=CARTESIAN_POINT('',(-0.146120596765396,-4.14129048147555E-5,1.26606550458429));
#20306=CARTESIAN_POINT('',(-0.146109918970638,-1.0198006988139E-5,1.25893449541571));
#20307=CARTESIAN_POINT('',(-0.14635,-1.79227059055215E-17,0.));
#20308=CARTESIAN_POINT('Ctrl Pts',(-0.146120596765396,-4.14129048147555E-5,
1.26606550458429));
#20309=CARTESIAN_POINT('Ctrl Pts',(-0.14605219935785,0.0269443530192317,
1.26460351894424));
#20310=CARTESIAN_POINT('Ctrl Pts',(-0.138898723445843,0.053963836666407,
1.26314153330418));
#20311=CARTESIAN_POINT('Ctrl Pts',(-0.124882896249422,0.0767650581554474,
1.26167954766413));
#20312=CARTESIAN_POINT('Ctrl Pts',(-0.0995129464537159,0.118037388097231,
1.25903321778503));
#20313=CARTESIAN_POINT('Ctrl Pts',(-0.051658938874944,0.145488850208621,
1.25638688790592));
#20314=CARTESIAN_POINT('Ctrl Pts',(-0.00322440565727106,0.146554478394238,
1.25374055802682));
#20315=CARTESIAN_POINT('Ctrl Pts',(0.0452101275604033,0.147620106579856,
1.25109422814772));
#20316=CARTESIAN_POINT('Ctrl Pts',(0.0942251864169787,0.122299900839699,
1.24844789826862));
#20317=CARTESIAN_POINT('Ctrl Pts',(0.121385807331354,0.0821833176976391,
1.24580156838952));
#20318=CARTESIAN_POINT('Ctrl Pts',(0.148546428245729,0.0420667345555804,
1.24315523851041));
#20319=CARTESIAN_POINT('Ctrl Pts',(0.153852611217905,-0.0128462259883804,
1.24050890863131));
#20320=CARTESIAN_POINT('Ctrl Pts',(0.134875632820701,-0.0574210379606392,
1.23786257875221));
#20321=CARTESIAN_POINT('Ctrl Pts',(0.115898654423498,-0.101995849932898,
1.23521624887311));
#20322=CARTESIAN_POINT('Ctrl Pts',(0.0726385146569148,-0.136232513333455,
1.23256991899401));
#20323=CARTESIAN_POINT('Ctrl Pts',(0.0248960600935515,-0.144460368686643,
1.2299235891149));
#20324=CARTESIAN_POINT('Ctrl Pts',(-0.0228463944698117,-0.152688224039831,
1.2272772592358));
#20325=CARTESIAN_POINT('Ctrl Pts',(-0.0750711638299551,-0.134907271345651,
1.2246309293567));
#20326=CARTESIAN_POINT('Ctrl Pts',(-0.107874149410843,-0.0992561323957017,
1.2219845994776));
#20327=CARTESIAN_POINT('Ctrl Pts',(-0.132331163880887,-0.072675612185966,
1.2200115678465));
#20328=CARTESIAN_POINT('Ctrl Pts',(-0.145992019903337,-0.0361614337449312,
1.21803853621539));
#20329=CARTESIAN_POINT('Ctrl Pts',(-0.146318311025392,0.000133437649768732,
1.21606550458429));
#20330=CARTESIAN_POINT('Ctrl Pts',(-0.146373054956946,0.000132657382717961,
1.20893449541571));
#20331=CARTESIAN_POINT('Ctrl Pts',(-0.146020767276673,-0.0379538636644633,
1.21100690453892));
#20332=CARTESIAN_POINT('Ctrl Pts',(-0.130797424420382,-0.0762899498869128,
1.21307931366213));
#20333=CARTESIAN_POINT('Ctrl Pts',(-0.104081054125652,-0.103227285106232,
1.21515172278534));
#20334=CARTESIAN_POINT('Ctrl Pts',(-0.0699523514264828,-0.137638258418326,
1.2177991121596));
#20335=CARTESIAN_POINT('Ctrl Pts',(-0.0170685611947798,-0.153447990763203,
1.22044650153386));
#20336=CARTESIAN_POINT('Ctrl Pts',(0.0303468241642401,-0.143414812629152,
1.22309389090812));
#20337=CARTESIAN_POINT('Ctrl Pts',(0.0777622095232573,-0.133381634495101,
1.22574128028238));
#20338=CARTESIAN_POINT('Ctrl Pts',(0.119709190009594,-0.0975055458821257,
1.22838866965664));
#20339=CARTESIAN_POINT('Ctrl Pts',(0.136973893871985,-0.052219638220276,
1.2310360590309));
#20340=CARTESIAN_POINT('Ctrl Pts',(0.154238597734379,-0.00693373055842239,
1.23368344840516));
#20341=CARTESIAN_POINT('Ctrl Pts',(0.146821024972825,0.0477619961523044,
1.23633083777942));
#20342=CARTESIAN_POINT('Ctrl Pts',(0.118118804930222,0.0868140895256425,
1.23897822715368));
#20343=CARTESIAN_POINT('Ctrl Pts',(0.0894165848876198,0.125866182898978,
1.24162561652794));
#20344=CARTESIAN_POINT('Ctrl Pts',(0.0394297175639698,0.149274642934924,
1.2442730059022));
#20345=CARTESIAN_POINT('Ctrl Pts',(-0.00894524413350711,0.146317192515786,
1.24692039527646));
#20346=CARTESIAN_POINT('Ctrl Pts',(-0.0573202058309854,0.143359742096648,
1.24956778465072));
#20347=CARTESIAN_POINT('Ctrl Pts',(-0.104083261902292,0.114036381222425,
1.25221517402498));
#20348=CARTESIAN_POINT('Ctrl Pts',(-0.127814530591109,0.0717787154251623,
1.25486256339924));
#20349=CARTESIAN_POINT('Ctrl Pts',(-0.139981499518435,0.0501133037087236,
1.2562198740714));
#20350=CARTESIAN_POINT('Ctrl Pts',(-0.146094355379323,0.0250479932723348,
1.25757718474355));
#20351=CARTESIAN_POINT('Ctrl Pts',(-0.146109918970638,-1.0198006988139E-5,
1.25893449541571));
#20352=CARTESIAN_POINT('Origin',(0.,0.,0.));
#20353=CARTESIAN_POINT('',(-0.146470135615938,-0.000111966546850736,1.31606550458429));
#20354=CARTESIAN_POINT('',(-0.146410535958061,-0.000127756381200432,1.30893449541571));
#20355=CARTESIAN_POINT('',(-0.14635,-1.79227059055215E-17,0.));
#20356=CARTESIAN_POINT('Ctrl Pts',(-0.146470135615938,-0.000111966546850736,
1.31606550458429));
#20357=CARTESIAN_POINT('Ctrl Pts',(-0.146120207411574,0.0411799307449602,
1.31381483155218));
#20358=CARTESIAN_POINT('Ctrl Pts',(-0.127827491572984,0.0827431563937987,
1.31156415852007));
#20359=CARTESIAN_POINT('Ctrl Pts',(-0.0969137672218927,0.10998333351997,
1.30931348548796));
#20360=CARTESIAN_POINT('Ctrl Pts',(-0.0605655677022408,0.142012194937238,
1.30666715560886));
#20361=CARTESIAN_POINT('Ctrl Pts',(-0.00676890401288169,0.154239532672684,
1.30402082572976));
#20362=CARTESIAN_POINT('Ctrl Pts',(0.0398526445220406,0.14106870189023,
1.30137449585066));
#20363=CARTESIAN_POINT('Ctrl Pts',(0.0864741930569617,0.127897871107775,
1.29872816597155));
#20364=CARTESIAN_POINT('Ctrl Pts',(0.125920626437448,0.0893288718074177,
1.29608183609245));
#20365=CARTESIAN_POINT('Ctrl Pts',(0.14013669149516,0.0430153417578024,
1.29343550621335));
#20366=CARTESIAN_POINT('Ctrl Pts',(0.154352756552873,-0.00329818829181684,
1.29078917633425));
#20367=CARTESIAN_POINT('Ctrl Pts',(0.143338453287813,-0.0573562490906975,
1.28814284645515));
#20368=CARTESIAN_POINT('Ctrl Pts',(0.112135201594409,-0.0944156157243562,
1.28549651657604));
#20369=CARTESIAN_POINT('Ctrl Pts',(0.0809319499010078,-0.131474982358013,
1.28285018669694));
#20370=CARTESIAN_POINT('Ctrl Pts',(0.0295397497792676,-0.151535654826449,
1.28020385681784));
#20371=CARTESIAN_POINT('Ctrl Pts',(-0.0185183802362589,-0.1454155477333,
1.27755752693874));
#20372=CARTESIAN_POINT('Ctrl Pts',(-0.066576510251784,-0.139295440640151,
1.27491119705964));
#20373=CARTESIAN_POINT('Ctrl Pts',(-0.111300570161094,-0.106994553985419,
1.27226486718053));
#20374=CARTESIAN_POINT('Ctrl Pts',(-0.13221965410943,-0.0632975117719662,
1.26961853730143));
#20375=CARTESIAN_POINT('Ctrl Pts',(-0.141581826511298,-0.0437412423069929,
1.26843419306239));
#20376=CARTESIAN_POINT('Ctrl Pts',(-0.146176005022067,-0.0219023912433209,
1.26724984882334));
#20377=CARTESIAN_POINT('Ctrl Pts',(-0.146120596765396,-4.14129048147555E-5,
1.26606550458429));
#20378=CARTESIAN_POINT('Ctrl Pts',(-0.146109918970638,-1.0198006988139E-5,
1.25893449541571));
#20379=CARTESIAN_POINT('Ctrl Pts',(-0.146124711647138,-0.0238271763493914,
1.26022457411781));
#20380=CARTESIAN_POINT('Ctrl Pts',(-0.140631289159497,-0.0476377233371588,
1.26151465281992));
#20381=CARTESIAN_POINT('Ctrl Pts',(-0.129592576141605,-0.0685164391025303,
1.26280473152202));
#20382=CARTESIAN_POINT('Ctrl Pts',(-0.106939871696956,-0.111361957112663,
1.26545212089628));
#20383=CARTESIAN_POINT('Ctrl Pts',(-0.0609349815013302,-0.141861022412626,
1.26809951027054));
#20384=CARTESIAN_POINT('Ctrl Pts',(-0.0126505083952331,-0.146043496451057,
1.2707468996448));
#20385=CARTESIAN_POINT('Ctrl Pts',(0.0356339647108625,-0.150225970489488,
1.27339428901906));
#20386=CARTESIAN_POINT('Ctrl Pts',(0.0861980207274291,-0.128091853266388,
1.27604167839332));
#20387=CARTESIAN_POINT('Ctrl Pts',(0.11588072467734,-0.0897797074320025,
1.27868906776758));
#20388=CARTESIAN_POINT('Ctrl Pts',(0.145563428627253,-0.0514675615976161,
1.28133645714184));
#20389=CARTESIAN_POINT('Ctrl Pts',(0.154364780510509,0.00302261284805656,
1.2839838465161));
#20390=CARTESIAN_POINT('Ctrl Pts',(0.138253309066183,0.0487315170146188,
1.28663123589036));
#20391=CARTESIAN_POINT('Ctrl Pts',(0.122141837621857,0.0944404211811797,
1.28927862526462));
#20392=CARTESIAN_POINT('Ctrl Pts',(0.0811175428499519,0.131368055068631,
1.29192601463888));
#20393=CARTESIAN_POINT('Ctrl Pts',(0.0339716590485425,0.142599665496764,
1.29457340401314));
#20394=CARTESIAN_POINT('Ctrl Pts',(-0.013174224752867,0.153831275924897,
1.2972207933874));
#20395=CARTESIAN_POINT('Ctrl Pts',(-0.0664416975837803,0.139366862893713,
1.29986818276166));
#20396=CARTESIAN_POINT('Ctrl Pts',(-0.101431520699135,0.105831870563862,
1.30251557213592));
#20397=CARTESIAN_POINT('Ctrl Pts',(-0.129710573305276,0.0787286237393239,
1.30465521322918));
#20398=CARTESIAN_POINT('Ctrl Pts',(-0.146050663974784,0.0391684733249047,
1.30679485432245));
#20399=CARTESIAN_POINT('Ctrl Pts',(-0.146410535958061,-0.000127756381200432,
1.30893449541571));
#20400=CARTESIAN_POINT('Origin',(0.,0.,0.));
#20401=CARTESIAN_POINT('',(-0.146471469669193,0.000111495080380188,1.36606550458429));
#20402=CARTESIAN_POINT('',(-0.146526884620975,8.5711493927648E-5,1.35893449541571));
#20403=CARTESIAN_POINT('',(-0.14635,-1.79227059055215E-17,0.));
#20404=CARTESIAN_POINT('Ctrl Pts',(-0.146471469669193,0.000111495080380188,
1.36606550458429));
#20405=CARTESIAN_POINT('Ctrl Pts',(-0.146532402405025,0.0073220458586883,
1.36567247403923));
#20406=CARTESIAN_POINT('Ctrl Pts',(-0.146045973070864,0.0145243451116175,
1.36527944349416));
#20407=CARTESIAN_POINT('Ctrl Pts',(-0.144983764805735,0.0216407019395156,
1.3648864129491));
#20408=CARTESIAN_POINT('Ctrl Pts',(-0.137831767320671,0.0695561322809842,
1.36224008307));
#20409=CARTESIAN_POINT('Ctrl Pts',(-0.104576727819841,0.113575347233418,
1.3595937531909));
#20410=CARTESIAN_POINT('Ctrl Pts',(-0.060440002550743,0.133550058215342,
1.3569474233118));
#20411=CARTESIAN_POINT('Ctrl Pts',(-0.0163032772816473,0.153524769197265,
1.35430109343269));
#20412=CARTESIAN_POINT('Ctrl Pts',(0.0387151337557165,0.149454976208681,
1.35165476355359));
#20413=CARTESIAN_POINT('Ctrl Pts',(0.0794324390145508,0.123203488242689,
1.34900843367449));
#20414=CARTESIAN_POINT('Ctrl Pts',(0.120149744273387,0.0969520002766962,
1.34636210379539));
#20415=CARTESIAN_POINT('Ctrl Pts',(0.146565943753694,0.048518817333291,
1.34371577391629));
#20416=CARTESIAN_POINT('Ctrl Pts',(0.14658992694451,7.25688577880009E-5,
1.34106944403718));
#20417=CARTESIAN_POINT('Ctrl Pts',(0.146613910135327,-0.0483736796177136,
1.33842311415808));
#20418=CARTESIAN_POINT('Ctrl Pts',(0.120245677036657,-0.0968329936253116,
1.33577678427898));
#20419=CARTESIAN_POINT('Ctrl Pts',(0.0795543829983497,-0.123124782547022,
1.33313045439988));
#20420=CARTESIAN_POINT('Ctrl Pts',(0.0388630889600415,-0.149416571468734,
1.33048412452078));
#20421=CARTESIAN_POINT('Ctrl Pts',(-0.0161512660179049,-0.153540835304554,
1.32783779464168));
#20422=CARTESIAN_POINT('Ctrl Pts',(-0.0603077462478081,-0.133609833714981,
1.32519146476257));
#20423=CARTESIAN_POINT('Ctrl Pts',(-0.10446422647771,-0.113678832125408,
1.32254513488347));
#20424=CARTESIAN_POINT('Ctrl Pts',(-0.137762831959571,-0.0696925651104417,
1.31989880500437));
#20425=CARTESIAN_POINT('Ctrl Pts',(-0.144962267025529,-0.0217842390534145,
1.31725247512527));
#20426=CARTESIAN_POINT('Ctrl Pts',(-0.146038665626028,-0.0146213916011371,
1.31685681827827));
#20427=CARTESIAN_POINT('Ctrl Pts',(-0.146531651210624,-0.00737087161912708,
1.31646116143128));
#20428=CARTESIAN_POINT('Ctrl Pts',(-0.146470135615938,-0.000111966546850736,
1.31606550458429));
#20429=CARTESIAN_POINT('Ctrl Pts',(-0.146410535958061,-0.000127756381200432,
1.30893449541571));
#20430=CARTESIAN_POINT('Ctrl Pts',(-0.146495935505426,-0.00945296197092968,
1.30944224369671));
#20431=CARTESIAN_POINT('Ctrl Pts',(-0.145681427739287,-0.018763305174839,
1.3099499919777));
#20432=CARTESIAN_POINT('Ctrl Pts',(-0.143913007029536,-0.0278887903271487,
1.3104577402587));
#20433=CARTESIAN_POINT('Ctrl Pts',(-0.134692496844786,-0.0754688872597875,
1.31310512963296));
#20434=CARTESIAN_POINT('Ctrl Pts',(-0.0995393030754929,-0.118023509496548,
1.31575251900722));
#20435=CARTESIAN_POINT('Ctrl Pts',(-0.0545553941775042,-0.136060454153345,
1.31839990838148));
#20436=CARTESIAN_POINT('Ctrl Pts',(-0.00957148527951295,-0.154097398810142,
1.32104729775574));
#20437=CARTESIAN_POINT('Ctrl Pts',(0.0452431387471776,-0.14761666588697,
1.32369468713));
#20438=CARTESIAN_POINT('Ctrl Pts',(0.0847805644327026,-0.119586763955155,
1.32634207650426));
#20439=CARTESIAN_POINT('Ctrl Pts',(0.124317990118227,-0.09155686202334,
1.32898946587852));
#20440=CARTESIAN_POINT('Ctrl Pts',(0.148578217462589,-0.041977791082884,
1.33163685525278));
#20441=CARTESIAN_POINT('Ctrl Pts',(0.146448816178573,0.00644068764408242,
1.33428424462704));
#20442=CARTESIAN_POINT('Ctrl Pts',(0.144319414894557,0.0548591663710502,
1.3369316340013));
#20443=CARTESIAN_POINT('Ctrl Pts',(0.115800384982161,0.102117052884526,
1.33957902337556));
#20444=CARTESIAN_POINT('Ctrl Pts',(0.0739549070570988,0.126567807678519,
1.34222641274982));
#20445=CARTESIAN_POINT('Ctrl Pts',(0.0321094291320376,0.151018562472512,
1.34487380212408));
#20446=CARTESIAN_POINT('Ctrl Pts',(-0.0230624968056921,0.152662185547021,
1.34752119149834));
#20447=CARTESIAN_POINT('Ctrl Pts',(-0.0662892946253695,0.1307458130856,
1.3501685808726));
#20448=CARTESIAN_POINT('Ctrl Pts',(-0.109516092445046,0.10882944062418,
1.35281597024686));
#20449=CARTESIAN_POINT('Ctrl Pts',(-0.140797762146673,0.0633530726268328,
1.35546335962112));
#20450=CARTESIAN_POINT('Ctrl Pts',(-0.145805692234247,0.0151472216574969,
1.35811074899538));
#20451=CARTESIAN_POINT('Ctrl Pts',(-0.146325105122407,0.0101474034011793,
1.35838533113549));
#20452=CARTESIAN_POINT('Ctrl Pts',(-0.146561879835735,0.00511822289583405,
1.3586599132756));
#20453=CARTESIAN_POINT('Ctrl Pts',(-0.146526884620975,8.5711493927648E-5,
1.35893449541571));
#20454=CARTESIAN_POINT('Origin',(0.,0.,0.));
#20455=CARTESIAN_POINT('',(-0.146120987371435,4.2191387702159E-5,1.41606550458429));
#20456=CARTESIAN_POINT('',(-0.146148882937928,7.6306569664006E-5,1.40893449541571));
#20457=CARTESIAN_POINT('',(-0.14635,-1.79227059055215E-17,0.));
#20458=CARTESIAN_POINT('Ctrl Pts',(-0.146120987371435,4.2191387702159E-5,
1.41606550458429));
#20459=CARTESIAN_POINT('Ctrl Pts',(-0.146177309023295,0.021854523983563,
1.41488378664717));
#20460=CARTESIAN_POINT('Ctrl Pts',(-0.141604359564088,0.0436444172696427,
1.41370206871005));
#20461=CARTESIAN_POINT('Ctrl Pts',(-0.132282279973341,0.0631665524487371,
1.41252035077294));
#20462=CARTESIAN_POINT('Ctrl Pts',(-0.1114064880593,0.106884268839086,1.40987402089383));
#20463=CARTESIAN_POINT('Ctrl Pts',(-0.0667143915920224,0.139229456738304,
1.40722769101473));
#20464=CARTESIAN_POINT('Ctrl Pts',(-0.0186623352932378,0.145397151366753,
1.40458136113563));
#20465=CARTESIAN_POINT('Ctrl Pts',(0.0293897210055454,0.151564845995202,
1.40193503125653));
#20466=CARTESIAN_POINT('Ctrl Pts',(0.0808017371358351,0.131555047352884,
1.39928870137743));
#20467=CARTESIAN_POINT('Ctrl Pts',(0.112041660826149,0.0945265884816804,
1.39664237149832));
#20468=CARTESIAN_POINT('Ctrl Pts',(0.143281584516463,0.0574981296104763,
1.39399604161922));
#20469=CARTESIAN_POINT('Ctrl Pts',(0.154349415766802,0.00345101051038574,
1.39134971174012));
#20470=CARTESIAN_POINT('Ctrl Pts',(0.140179214932283,-0.0428765696854336,
1.38870338186102));
#20471=CARTESIAN_POINT('Ctrl Pts',(0.126009014097764,-0.089204149881253,
1.38605705198192));
#20472=CARTESIAN_POINT('Ctrl Pts',(0.0866007811783877,-0.127812191172801,
1.38341072210282));
#20473=CARTESIAN_POINT('Ctrl Pts',(0.0399922944706322,-0.14102917638501,
1.38076439222371));
#20474=CARTESIAN_POINT('Ctrl Pts',(-0.00661619223712474,-0.15424616159722,
1.37811806234461));
#20475=CARTESIAN_POINT('Ctrl Pts',(-0.060424932733261,-0.142072090730089,
1.37547173246551));
#20476=CARTESIAN_POINT('Ctrl Pts',(-0.0968048252466797,-0.110079232431271,
1.37282540258641));
#20477=CARTESIAN_POINT('Ctrl Pts',(-0.127781608685608,-0.08283792481198,
1.37057210325237));
#20478=CARTESIAN_POINT('Ctrl Pts',(-0.146122133733866,-0.0412276055847571,
1.36831880391833));
#20479=CARTESIAN_POINT('Ctrl Pts',(-0.146471469669193,0.000111495080380188,
1.36606550458429));
#20480=CARTESIAN_POINT('Ctrl Pts',(-0.146526884620975,8.5711493927648E-5,
1.35893449541571));
#20481=CARTESIAN_POINT('Ctrl Pts',(-0.146224472749943,-0.0434028397118431,
1.36130730264986));
#20482=CARTESIAN_POINT('Ctrl Pts',(-0.125627402569456,-0.0871401285467012,
1.36368010988401));
#20483=CARTESIAN_POINT('Ctrl Pts',(-0.0917490966422633,-0.114327780902106,
1.36605291711816));
#20484=CARTESIAN_POINT('Ctrl Pts',(-0.0539503804891888,-0.144661598551044,
1.36870030649242));
#20485=CARTESIAN_POINT('Ctrl Pts',(0.00038124229047478,-0.154393899907594,
1.37134769586668));
#20486=CARTESIAN_POINT('Ctrl Pts',(0.0463590973565905,-0.139066790892088,
1.37399508524094));
#20487=CARTESIAN_POINT('Ctrl Pts',(0.0923369524227062,-0.123739681876581,
1.3766424746152));
#20488=CARTESIAN_POINT('Ctrl Pts',(0.129961039775272,-0.083353162489017,
1.37928986398946));
#20489=CARTESIAN_POINT('Ctrl Pts',(0.141997595260484,-0.0364063334065561,
1.38193725336372));
#20490=CARTESIAN_POINT('Ctrl Pts',(0.154034150745695,0.0105404956759021,
1.38458464273798));
#20491=CARTESIAN_POINT('Ctrl Pts',(0.140483174363557,0.0640476344532581,
1.38723203211224));
#20492=CARTESIAN_POINT('Ctrl Pts',(0.10755170844225,0.0996060653705087,
1.3898794214865));
#20493=CARTESIAN_POINT('Ctrl Pts',(0.0746202425209409,0.135164496287762,
1.39252681086076));
#20494=CARTESIAN_POINT('Ctrl Pts',(0.0223082870604623,0.152774219344908,
1.39517420023502));
#20495=CARTESIAN_POINT('Ctrl Pts',(-0.025422593472234,0.144369075867769,
1.39782158960928));
#20496=CARTESIAN_POINT('Ctrl Pts',(-0.073153474004929,0.135963932390631,
1.40046897898354));
#20497=CARTESIAN_POINT('Ctrl Pts',(-0.11630327960984,0.101543922379208,
1.4031163683578));
#20498=CARTESIAN_POINT('Ctrl Pts',(-0.135107186188192,0.0568751802851974,
1.40576375773206));
#20499=CARTESIAN_POINT('Ctrl Pts',(-0.142614236437708,0.0390421576584788,
1.40682067029328));
#20500=CARTESIAN_POINT('Ctrl Pts',(-0.14624095998336,0.0195756595648056,
1.40787758285449));
#20501=CARTESIAN_POINT('Ctrl Pts',(-0.146148882937928,7.6306569664006E-5,
1.40893449541571));
#20502=CARTESIAN_POINT('Origin',(0.,0.,0.));
#20503=CARTESIAN_POINT('',(-0.14631473222987,-0.000131398079681141,1.46606550458429));
#20504=CARTESIAN_POINT('',(-0.146248097568756,-0.000123763188177425,1.45893449541571));
#20505=CARTESIAN_POINT('',(-0.14635,-1.79227059055215E-17,0.));
#20506=CARTESIAN_POINT('Ctrl Pts',(-0.14631473222987,-0.000131398079681141,
1.46606550458429));
#20507=CARTESIAN_POINT('Ctrl Pts',(-0.145989697979493,0.0361157155227289,
1.46409509925512));
#20508=CARTESIAN_POINT('Ctrl Pts',(-0.132370868650209,0.0725796635271419,
1.46212469392594));
#20509=CARTESIAN_POINT('Ctrl Pts',(-0.107973319296019,0.0991484059484618,
1.46015428859677));
#20510=CARTESIAN_POINT('Ctrl Pts',(-0.0752064754000165,0.134831245351468,
1.45750795871767));
#20511=CARTESIAN_POINT('Ctrl Pts',(-0.0229974942306327,0.152665588379184,
1.45486162883857));
#20512=CARTESIAN_POINT('Ctrl Pts',(0.0247535192036911,0.144485406820094,
1.45221529895946));
#20513=CARTESIAN_POINT('Ctrl Pts',(0.0725045326380122,0.136305225261004,
1.44956896908036));
#20514=CARTESIAN_POINT('Ctrl Pts',(0.115797578337275,0.102110519115111,
1.44692263920126));
#20515=CARTESIAN_POINT('Ctrl Pts',(0.134818450998255,0.0575543070937695,
1.44427630932216));
#20516=CARTESIAN_POINT('Ctrl Pts',(0.153839323659235,0.0129980950724284,
1.44162997944306));
#20517=CARTESIAN_POINT('Ctrl Pts',(0.148588023281934,-0.0419196228243577,
1.43898364956396));
#20518=CARTESIAN_POINT('Ctrl Pts',(0.121467255745355,-0.082062966762292,
1.43633731968485));
#20519=CARTESIAN_POINT('Ctrl Pts',(0.0943464882087764,-0.122206310700226,
1.43369098980575));
#20520=CARTESIAN_POINT('Ctrl Pts',(0.0453562535129183,-0.147575280679306,
1.43104465992665));
#20521=CARTESIAN_POINT('Ctrl Pts',(-0.00307937473935208,-0.146557666176543,
1.42839833004755));
#20522=CARTESIAN_POINT('Ctrl Pts',(-0.0515150029916225,-0.14554005167378,
1.42575200016845));
#20523=CARTESIAN_POINT('Ctrl Pts',(-0.0993960248003067,-0.118135852689175,
1.42310567028934));
#20524=CARTESIAN_POINT('Ctrl Pts',(-0.124806792024246,-0.0768886307561326,
1.42045934041024));
#20525=CARTESIAN_POINT('Ctrl Pts',(-0.138870387581649,-0.0540603453281256,
1.41899472846826));
#20526=CARTESIAN_POINT('Ctrl Pts',(-0.146051182757901,-0.0269918425378075,
1.41753011652627));
#20527=CARTESIAN_POINT('Ctrl Pts',(-0.146120987371435,4.2191387702159E-5,
1.41606550458429));
#20528=CARTESIAN_POINT('Ctrl Pts',(-0.146148882937928,7.6306569664006E-5,
1.40893449541571));
#20529=CARTESIAN_POINT('Ctrl Pts',(-0.146010322369016,-0.0292669616874671,
1.41052497222875));
#20530=CARTESIAN_POINT('Ctrl Pts',(-0.137450455640384,-0.0586846305953837,
1.4121154490418));
#20531=CARTESIAN_POINT('Ctrl Pts',(-0.121019719714466,-0.0827222215753489,
1.41370592585484));
#20532=CARTESIAN_POINT('Ctrl Pts',(-0.0936703391105966,-0.122733407165291,
1.4163533152291));
#20533=CARTESIAN_POINT('Ctrl Pts',(-0.0445135703510636,-0.147838304168576,
1.41900070460336));
#20534=CARTESIAN_POINT('Ctrl Pts',(0.00393424939099551,-0.146537573651384,
1.42164809397762));
#20535=CARTESIAN_POINT('Ctrl Pts',(0.0523820691330518,-0.145236843134192,
1.42429548335188));
#20536=CARTESIAN_POINT('Ctrl Pts',(0.100120939857634,-0.117530485096527,
1.42694287272614));
#20537=CARTESIAN_POINT('Ctrl Pts',(0.125284029446909,-0.0761094471358441,
1.4295902621004));
#20538=CARTESIAN_POINT('Ctrl Pts',(0.150447119036187,-0.0346884091751576,
1.43223765147466));
#20539=CARTESIAN_POINT('Ctrl Pts',(0.153034427490153,0.020447308708549,
1.43488504084892));
#20540=CARTESIAN_POINT('Ctrl Pts',(0.13186079120536,0.0640427391611241,
1.43753243022318));
#20541=CARTESIAN_POINT('Ctrl Pts',(0.110687154920568,0.107638169613697,
1.44017981959744));
#20542=CARTESIAN_POINT('Ctrl Pts',(0.0657525738970213,0.139693312635139,
1.4428272089717));
#20543=CARTESIAN_POINT('Ctrl Pts',(0.0176394768514684,0.145525221357757,
1.44547459834596));
#20544=CARTESIAN_POINT('Ctrl Pts',(-0.0304736201940859,0.151357130080375,
1.44812198772022));
#20545=CARTESIAN_POINT('Ctrl Pts',(-0.0817652332616461,0.130965804504167,
1.45076937709448));
#20546=CARTESIAN_POINT('Ctrl Pts',(-0.112741325423428,0.0936916042199666,
1.45341676646874));
#20547=CARTESIAN_POINT('Ctrl Pts',(-0.134261605244105,0.0677957870194472,
1.45525600945106));
#20548=CARTESIAN_POINT('Ctrl Pts',(-0.145976367207401,0.0337512577971725,
1.45709525243339));
#20549=CARTESIAN_POINT('Ctrl Pts',(-0.146248097568756,-0.000123763188177425,
1.45893449541571));
#20550=CARTESIAN_POINT('Origin',(0.,0.,-0.0924367114736175));
#20551=CARTESIAN_POINT('',(-0.117746618301147,-0.000105742458702955,1.48256328852638));
#20552=CARTESIAN_POINT('',(-0.117971241274414,-5.28325160115065E-6,1.49243671147361));
#20553=CARTESIAN_POINT('',(-0.117775,2.85464118895969E-14,-0.0924367114736175));
#20554=CARTESIAN_POINT('',(-0.117668597464313,0.00500517689812599,1.532225));
#20555=CARTESIAN_POINT('Ctrl Pts',(-0.117746618301147,-0.000105742458702949,
1.48256328852638));
#20556=CARTESIAN_POINT('Ctrl Pts',(-0.117836347163251,-0.0101121102621826,
1.48323921307631));
#20557=CARTESIAN_POINT('Ctrl Pts',(-0.112089674709738,-0.0591937430214443,
1.48656146750534));
#20558=CARTESIAN_POINT('Ctrl Pts',(-0.0435804807853106,-0.132222740314769,
1.49253005181348));
#20559=CARTESIAN_POINT('Ctrl Pts',(0.0874774386997331,-0.108286040948335,
1.50046904145078));
#20560=CARTESIAN_POINT('Ctrl Pts',(0.138385550162814,0.0147146982980264,
1.50840803108809));
#20561=CARTESIAN_POINT('Ctrl Pts',(0.0627460642121078,0.124368470664037,
1.51634702072539));
#20562=CARTESIAN_POINT('Ctrl Pts',(-0.0706026869052757,0.119928391791904,
1.5242860103627));
#20563=CARTESIAN_POINT('Ctrl Pts',(-0.116004137797729,0.0441355889673283,
1.5295786701209));
#20564=CARTESIAN_POINT('Ctrl Pts',(-0.117668597464313,0.00500517689812487,
1.532225));
#20565=CARTESIAN_POINT('',(-0.0334019664627544,0.1129391839063,1.53222500000001));
#20566=CARTESIAN_POINT('Origin',(0.,0.,1.532225));
#20567=CARTESIAN_POINT('Ctrl Pts',(-0.117971276761593,-5.28420699491729E-6,
1.49243671147361));
#20568=CARTESIAN_POINT('Ctrl Pts',(-0.117971582784674,-0.000385634193345565,
1.49246252744444));
#20569=CARTESIAN_POINT('Ctrl Pts',(-0.117794795258817,-0.0397700451254522,
1.49513573278954));
#20570=CARTESIAN_POINT('Ctrl Pts',(-0.0742871760264013,-0.117748889605885,
1.50045632750888));
#20571=CARTESIAN_POINT('Ctrl Pts',(0.0586284551779338,-0.126233948370975,
1.50839849563167));
#20572=CARTESIAN_POINT('Ctrl Pts',(0.137995068118234,-0.019163470063063,
1.51634066375444));
#20573=CARTESIAN_POINT('Ctrl Pts',(0.0906261803825392,0.105639137646141,
1.52428283187723));
#20574=CARTESIAN_POINT('Ctrl Pts',(0.00417072711528833,0.124051375507138,
1.52957761062575));
#20575=CARTESIAN_POINT('Ctrl Pts',(-0.0334019664627544,0.1129391839063,
1.53222500000001));
#20576=CARTESIAN_POINT('Origin',(0.,0.,-0.0924367114736175));
#20577=CARTESIAN_POINT('',(-0.117590702341447,3.3953472435133E-5,1.43256328852638));
#20578=CARTESIAN_POINT('',(-0.117692994131604,-9.95982882293356E-5,1.44243671147361));
#20579=CARTESIAN_POINT('',(-0.117775,2.85464118895969E-14,-0.0924367114736175));
#20580=CARTESIAN_POINT('Ctrl Pts',(-0.117590702341447,3.39534724351446E-5,
1.43256328852638));
#20581=CARTESIAN_POINT('Ctrl Pts',(-0.117534527156218,-0.0217216553118358,
1.43402790046837));
#20582=CARTESIAN_POINT('Ctrl Pts',(-0.101314495966545,-0.0828641818343832,
1.43813884228945));
#20583=CARTESIAN_POINT('Ctrl Pts',(-0.00292444232197888,-0.139176693688359,
1.44489611398964));
#20584=CARTESIAN_POINT('Ctrl Pts',(0.115350068603298,-0.0779297424218237,
1.45283510362695));
#20585=CARTESIAN_POINT('Ctrl Pts',(0.128028003046829,0.0546551750765237,
1.46077409326425));
#20586=CARTESIAN_POINT('Ctrl Pts',(0.0235079116789307,0.137209630484779,
1.46871308290156));
#20587=CARTESIAN_POINT('Ctrl Pts',(-0.0918059616614023,0.0978189523496558,
1.47597614798894));
#20588=CARTESIAN_POINT('Ctrl Pts',(-0.117485047349053,0.0290640819657798,
1.48059288319721));
#20589=CARTESIAN_POINT('Ctrl Pts',(-0.117746618301147,-0.000105742458702949,
1.48256328852638));
#20590=CARTESIAN_POINT('Ctrl Pts',(-0.117692994131604,-9.9598288229346E-5,
1.44243671147361));
#20591=CARTESIAN_POINT('Ctrl Pts',(-0.117789077779518,-0.0120777797952868,
1.44324485786555));
#20592=CARTESIAN_POINT('Ctrl Pts',(-0.110597905189529,-0.0631824179582176,
1.44670039363175));
#20593=CARTESIAN_POINT('Ctrl Pts',(-0.0368790902657646,-0.134252921254984,
1.45280331877221));
#20594=CARTESIAN_POINT('Ctrl Pts',(0.0928396680879532,-0.103751556080299,
1.46074548689499));
#20595=CARTESIAN_POINT('Ctrl Pts',(0.137511141307062,0.0217950526079239,
1.46868765501776));
#20596=CARTESIAN_POINT('Ctrl Pts',(0.0562018483347667,0.127378648737854,
1.47662982314055));
#20597=CARTESIAN_POINT('Ctrl Pts',(-0.0761502833827582,0.1162998103107,
1.48454617529249));
#20598=CARTESIAN_POINT('Ctrl Pts',(-0.117940200573233,0.0386186906477724,
1.48981513807018));
#20599=CARTESIAN_POINT('Ctrl Pts',(-0.117971276761593,-5.28420699491729E-6,
1.49243671147361));
#20600=CARTESIAN_POINT('Origin',(0.,0.,-0.0924367114736175));
#20601=CARTESIAN_POINT('',(-0.117872752581409,8.97255421561373E-5,1.38256328852638));
#20602=CARTESIAN_POINT('',(-0.117613151267609,6.14076272390171E-5,1.39243671147361));
#20603=CARTESIAN_POINT('',(-0.117775,2.85464118895969E-14,-0.0924367114736175));
#20604=CARTESIAN_POINT('Ctrl Pts',(-0.117872752581409,8.97255421561322E-5,
1.38256328852638));
#20605=CARTESIAN_POINT('Ctrl Pts',(-0.117591624875346,-0.0331778698171688,
1.38481658786042));
#20606=CARTESIAN_POINT('Ctrl Pts',(-0.0854981695600773,-0.105990339321694,
1.38971621707357));
#20607=CARTESIAN_POINT('Ctrl Pts',(0.0379781508110965,-0.133926497290667,
1.39726217616581));
#20608=CARTESIAN_POINT('Ctrl Pts',(0.133119345865688,-0.0407171622080862,
1.40520116580311));
#20609=CARTESIAN_POINT('Ctrl Pts',(0.106398871137127,0.0897659150453452,
1.41314015544042));
#20610=CARTESIAN_POINT('Ctrl Pts',(-0.0177224175491345,0.138074504763813,
1.42107914507772));
#20611=CARTESIAN_POINT('Ctrl Pts',(-0.105714817800915,0.0743914165933911,
1.42755352277305));
#20612=CARTESIAN_POINT('Ctrl Pts',(-0.11763602712824,0.0175874039095825,
1.43138157058926));
#20613=CARTESIAN_POINT('Ctrl Pts',(-0.117590702341447,3.39534724351446E-5,
1.43256328852638));
#20614=CARTESIAN_POINT('Ctrl Pts',(-0.117613151267609,6.1407627239024E-5,
1.39243671147361));
#20615=CARTESIAN_POINT('Ctrl Pts',(-0.117501644803633,-0.0235525549213426,
1.39402718828666));
#20616=CARTESIAN_POINT('Ctrl Pts',(-0.0991469449676741,-0.0866320980727062,
1.39826505447396));
#20617=CARTESIAN_POINT('Ctrl Pts',(0.00373660876362508,-0.139175849115243,
1.40515031003553));
#20618=CARTESIAN_POINT('Ctrl Pts',(0.118990018389619,-0.0722858665142316,
1.41309247815831));
#20619=CARTESIAN_POINT('Ctrl Pts',(0.125236419206141,0.0608253567263532,
1.42103464628109));
#20620=CARTESIAN_POINT('Ctrl Pts',(0.0167532566496359,0.13821437898841,
1.42897681440387));
#20621=CARTESIAN_POINT('Ctrl Pts',(-0.0944771051913143,0.0939940009069027,
1.43611083613471));
#20622=CARTESIAN_POINT('Ctrl Pts',(-0.117474319425011,0.0271612872365273,
1.44059746849129));
#20623=CARTESIAN_POINT('Ctrl Pts',(-0.117692994131604,-9.9598288229346E-5,
1.44243671147361));
#20624=CARTESIAN_POINT('Origin',(0.,0.,-0.0924367114736175));
#20625=CARTESIAN_POINT('',(-0.117871679003533,-9.01049542302267E-5,1.33256328852638));
#20626=CARTESIAN_POINT('',(-0.117917347702326,6.89762296073142E-5,1.34243671147361));
#20627=CARTESIAN_POINT('',(-0.117775,2.85464118895969E-14,-0.0924367114736175));
#20628=CARTESIAN_POINT('Ctrl Pts',(-0.117871679003533,-9.01049542302501E-5,
1.33256328852638));
#20629=CARTESIAN_POINT('Ctrl Pts',(-0.117921183610054,-0.00593170075121234,
1.33295894537338));
#20630=CARTESIAN_POINT('Ctrl Pts',(-0.114870949065289,-0.0507926200311143,
1.33600093209947));
#20631=CARTESIAN_POINT('Ctrl Pts',(-0.0572704544775333,-0.126880813469472,
1.34168924870467));
#20632=CARTESIAN_POINT('Ctrl Pts',(0.0755477687720905,-0.116923823242002,
1.34962823834197));
#20633=CARTESIAN_POINT('Ctrl Pts',(0.13920718769651,6.89141801743488E-5,
1.35756722797928));
#20634=CARTESIAN_POINT('Ctrl Pts',(0.0754319660950179,0.116998564767658,
1.36550621761658));
#20635=CARTESIAN_POINT('Ctrl Pts',(-0.0573960494825499,0.126824048933643,
1.37344520725389));
#20636=CARTESIAN_POINT('Ctrl Pts',(-0.11489462347839,0.0507140179075799,
1.37913089755716));
#20637=CARTESIAN_POINT('Ctrl Pts',(-0.117921788132912,0.00589240827474643,
1.38217025798132));
#20638=CARTESIAN_POINT('Ctrl Pts',(-0.117872752581409,8.97255421561322E-5,
1.38256328852638));
#20639=CARTESIAN_POINT('Ctrl Pts',(-0.117917347702326,6.89762296073276E-5,
1.34243671147361));
#20640=CARTESIAN_POINT('Ctrl Pts',(-0.117673982084908,-0.0349283870656527,
1.34480951870776));
#20641=CARTESIAN_POINT('Ctrl Pts',(-0.0826049238592893,-0.109396528181867,
1.34982971531618));
#20642=CARTESIAN_POINT('Ctrl Pts',(0.0440301174146577,-0.132080378229483,
1.35749730129884));
#20643=CARTESIAN_POINT('Ctrl Pts',(0.13486394497766,-0.0345773583278084,
1.36543946942163));
#20644=CARTESIAN_POINT('Ctrl Pts',(0.102148545386143,0.0946020732301706,
1.3733816375444));
#20645=CARTESIAN_POINT('Ctrl Pts',(-0.0241454188302812,0.137116288461919,
1.38132380566719));
#20646=CARTESIAN_POINT('Ctrl Pts',(-0.107458038693719,0.07065895059964,
1.38767549697692));
#20647=CARTESIAN_POINT('Ctrl Pts',(-0.117687250167678,0.015753490298928,
1.3913797989124));
#20648=CARTESIAN_POINT('Ctrl Pts',(-0.117613151267609,6.1407627239024E-5,
1.39243671147361));
#20649=CARTESIAN_POINT('Origin',(0.,0.,-0.0924367114736175));
#20650=CARTESIAN_POINT('',(-0.117590388001671,-3.33269891443968E-5,1.28256328852638));
#20651=CARTESIAN_POINT('',(-0.117823716245033,-0.000102811805890834,1.29243671147362));
#20652=CARTESIAN_POINT('',(-0.117775,2.85464118895969E-14,-0.0924367114736175));
#20653=CARTESIAN_POINT('Ctrl Pts',(-0.117590388001671,-3.33269891444124E-5,
1.28256328852638));
#20654=CARTESIAN_POINT('Ctrl Pts',(-0.117634977734708,-0.017625925033684,
1.28374763276543));
#20655=CARTESIAN_POINT('Ctrl Pts',(-0.105676786131388,-0.0744702911817869,
1.28757830688358));
#20656=CARTESIAN_POINT('Ctrl Pts',(-0.0175857351491984,-0.138091953858251,
1.29405531088083));
#20657=CARTESIAN_POINT('Ctrl Pts',(0.106487712804436,-0.089660542174548,
1.30199430051814));
#20658=CARTESIAN_POINT('Ctrl Pts',(0.133078957772855,0.0408489510387311,
1.30993329015544));
#20659=CARTESIAN_POINT('Ctrl Pts',(0.0378455373822902,0.133964029124136,
1.31787227979275));
#20660=CARTESIAN_POINT('Ctrl Pts',(-0.0855601048685178,0.105915403748908,
1.32541561258306));
#20661=CARTESIAN_POINT('Ctrl Pts',(-0.117590074669608,0.0331395035428114,
1.33031261549427));
#20662=CARTESIAN_POINT('Ctrl Pts',(-0.117871679003533,-9.01049542302501E-5,
1.33256328852638));
#20663=CARTESIAN_POINT('Ctrl Pts',(-0.117823716245033,-0.000102811805890825,
1.29243671147362));
#20664=CARTESIAN_POINT('Ctrl Pts',(-0.117892441435953,-0.00760726064997237,
1.29294445975461));
#20665=CARTESIAN_POINT('Ctrl Pts',(-0.113819337750002,-0.0541654333254181,
1.29609959740987));
#20666=CARTESIAN_POINT('Ctrl Pts',(-0.0518146499729274,-0.129225073214149,
1.30190212443939));
#20667=CARTESIAN_POINT('Ctrl Pts',(0.0805213734929343,-0.11357898534207,
1.30984429256217));
#20668=CARTESIAN_POINT('Ctrl Pts',(0.1390915465469,0.0061171215252809,1.31778646068495));
#20669=CARTESIAN_POINT('Ctrl Pts',(0.0702395735793815,0.120209316621791,
1.32572862880773));
#20670=CARTESIAN_POINT('Ctrl Pts',(-0.0629590648350173,0.124177428154433,
1.33367079693051));
#20671=CARTESIAN_POINT('Ctrl Pts',(-0.115917830154768,0.0471875384414626,
1.33924015781913));
#20672=CARTESIAN_POINT('Ctrl Pts',(-0.117945510062545,0.00411888419242175,
1.3421621293335));
#20673=CARTESIAN_POINT('Ctrl Pts',(-0.117917347702326,6.89762296073276E-5,
1.34243671147361));
#20674=CARTESIAN_POINT('Origin',(0.,0.,-0.0924367114736175));
#20675=CARTESIAN_POINT('',(-0.11774949833287,0.000107383800510985,1.23256328852638));
#20676=CARTESIAN_POINT('',(-0.117581795058195,-8.20683476789735E-6,1.24243671147361));
#20677=CARTESIAN_POINT('',(-0.117775,2.85464118895969E-14,-0.0924367114736175));
#20678=CARTESIAN_POINT('Ctrl Pts',(-0.11774949833287,0.000107383800510997,
1.23256328852638));
#20679=CARTESIAN_POINT('Ctrl Pts',(-0.1174869159147,-0.0291008736543001,
1.23453632015749));
#20680=CARTESIAN_POINT('Ctrl Pts',(-0.0917482398636095,-0.0978979247776974,
1.23915568166769));
#20681=CARTESIAN_POINT('Ctrl Pts',(0.0236422145726536,-0.137184880695923,
1.246421373057));
#20682=CARTESIAN_POINT('Ctrl Pts',(0.128082862902196,-0.0545291301253663,
1.2543603626943));
#20683=CARTESIAN_POINT('Ctrl Pts',(0.115272428336817,0.0780443019497631,
1.26229935233161));
#20684=CARTESIAN_POINT('Ctrl Pts',(-0.00306201423577413,0.139173524314926,
1.27023834196891));
#20685=CARTESIAN_POINT('Ctrl Pts',(-0.101358337705897,0.08278581645186,
1.27699298736717));
#20686=CARTESIAN_POINT('Ctrl Pts',(-0.117535345263889,0.02168343817453,
1.28110130288633));
#20687=CARTESIAN_POINT('Ctrl Pts',(-0.117590388001671,-3.33269891444124E-5,
1.28256328852638));
#20688=CARTESIAN_POINT('Ctrl Pts',(-0.117581795058195,-8.20683476789562E-6,
1.24243671147361));
#20689=CARTESIAN_POINT('Ctrl Pts',(-0.117593699448189,-0.0191748937105988,
1.24372679017572));
#20690=CARTESIAN_POINT('Ctrl Pts',(-0.104100832827715,-0.0776580224685839,
1.24766425825208));
#20691=CARTESIAN_POINT('Ctrl Pts',(-0.0120149744006178,-0.138706589206355,
1.25424911570271));
#20692=CARTESIAN_POINT('Ctrl Pts',(0.110059129405696,-0.0852693704304675,
1.26219128382548));
#20693=CARTESIAN_POINT('Ctrl Pts',(0.13130776387206,0.0462833517151888,
1.27013345194827));
#20694=CARTESIAN_POINT('Ctrl Pts',(0.0322649968732001,0.135435768819968,
1.27807562007105));
#20695=CARTESIAN_POINT('Ctrl Pts',(-0.0881142830049797,0.102747609761224,
1.28551003991283));
#20696=CARTESIAN_POINT('Ctrl Pts',(-0.117534109666069,0.0315207854174475,
1.29029707038035));
#20697=CARTESIAN_POINT('Ctrl Pts',(-0.117823716245033,-0.000102811805890825,
1.29243671147362));
#20698=CARTESIAN_POINT('Origin',(0.,0.,-0.0924367114736175));
#20699=CARTESIAN_POINT('',(-0.117957988745754,-3.12301727557783E-5,1.18256328852638));
#20700=CARTESIAN_POINT('',(-0.117793553451004,0.000106755881474893,1.19243671147362));
#20701=CARTESIAN_POINT('',(-0.117775,2.85464118895969E-14,-0.0924367114736175));
#20702=CARTESIAN_POINT('Ctrl Pts',(-0.117957988745754,-3.12301727557569E-5,
1.18256328852638));
#20703=CARTESIAN_POINT('Ctrl Pts',(-0.117964007145535,-0.00173159226684161,
1.18267867767044));
#20704=CARTESIAN_POINT('Ctrl Pts',(-0.117160216762375,-0.0424221720604921,
1.1854403966936));
#20705=CARTESIAN_POINT('Ctrl Pts',(-0.0703321751825429,-0.12013338809653,
1.19084844559586));
#20706=CARTESIAN_POINT('Ctrl Pts',(0.0627954496153871,-0.124239193932754,
1.19878743523316));
#20707=CARTESIAN_POINT('Ctrl Pts',(0.138438143943654,-0.0146125323915816,
1.20672642487047));
#20708=CARTESIAN_POINT('Ctrl Pts',(0.0873502052771435,0.108390901091839,
1.21466541450777));
#20709=CARTESIAN_POINT('Ctrl Pts',(-0.043700859820065,0.132169893139269,
1.22260440414508));
#20710=CARTESIAN_POINT('Ctrl Pts',(-0.112119660921406,0.0591163174148552,
1.22857036215128));
#20711=CARTESIAN_POINT('Ctrl Pts',(-0.117839104743291,0.0100747194789664,
1.23188999027838));
#20712=CARTESIAN_POINT('Ctrl Pts',(-0.11774949833287,0.000107383800510997,
1.23256328852638));
#20713=CARTESIAN_POINT('Ctrl Pts',(-0.117793553451004,0.000106755881474891,
1.19243671147362));
#20714=CARTESIAN_POINT('Ctrl Pts',(-0.117510050331475,-0.0305433296418112,
1.19450912059683));
#20715=CARTESIAN_POINT('Ctrl Pts',(-0.0896091397727994,-0.100804620014092,
1.19922891909429));
#20716=CARTESIAN_POINT('Ctrl Pts',(0.0288222657999454,-0.136209964735594,
1.20659610696603));
#20717=CARTESIAN_POINT('Ctrl Pts',(0.130092623711363,-0.0495962373069701,
1.21453827508881));
#20718=CARTESIAN_POINT('Ctrl Pts',(0.112184773380136,0.082452738709893,
1.22248044321158));
#20719=CARTESIAN_POINT('Ctrl Pts',(-0.00849585454694533,0.138966535376798,
1.23042261133437));
#20720=CARTESIAN_POINT('Ctrl Pts',(-0.103054997843392,0.079672038485689,
1.23707470075504));
#20721=CARTESIAN_POINT('Ctrl Pts',(-0.11756927027536,0.0201573447738481,
1.24107940080146));
#20722=CARTESIAN_POINT('Ctrl Pts',(-0.117581795058195,-8.20683476789562E-6,
1.24243671147361));
#20723=CARTESIAN_POINT('Origin',(0.,0.,-0.0924367114736175));
#20724=CARTESIAN_POINT('',(-0.117657565919426,-8.78585414499747E-5,1.13256328852638));
#20725=CARTESIAN_POINT('',(-0.117937823388479,-5.4172489969917E-5,1.14243671147362));
#20726=CARTESIAN_POINT('',(-0.117775,2.85464118895969E-14,-0.0924367114736175));
#20727=CARTESIAN_POINT('Ctrl Pts',(-0.117657565919426,-8.78585414499974E-5,
1.13256328852638));
#20728=CARTESIAN_POINT('Ctrl Pts',(-0.11775046973706,-0.0134980674796043,
1.13346736506249));
#20729=CARTESIAN_POINT('Ctrl Pts',(-0.109441032251172,-0.0660497484721492,
1.13701777147771));
#20730=CARTESIAN_POINT('Ctrl Pts',(-0.0320511128216771,-0.13546723577438,
1.14321450777202));
#20731=CARTESIAN_POINT('Ctrl Pts',(0.0964380908528195,-0.100390938007982,
1.15115349740933));
#20732=CARTESIAN_POINT('Ctrl Pts',(0.136644831685568,0.0265863832644056,
1.15909248704664));
#20733=CARTESIAN_POINT('Ctrl Pts',(0.0517625939920979,0.129225692742072,
1.16703147668394));
#20734=CARTESIAN_POINT('Ctrl Pts',(-0.0785823129332351,0.113795317289389,
1.17485507717719));
#20735=CARTESIAN_POINT('Ctrl Pts',(-0.117825981412732,0.0372644419932696,
1.18003234779134));
#20736=CARTESIAN_POINT('Ctrl Pts',(-0.117957988745754,-3.12301727557569E-5,
1.18256328852638));
#20737=CARTESIAN_POINT('Ctrl Pts',(-0.117937823388479,-5.41724899699178E-5,
1.14243671147362));
#20738=CARTESIAN_POINT('Ctrl Pts',(-0.117955293269658,-0.0031110520517566,
1.14264406164367));
#20739=CARTESIAN_POINT('Ctrl Pts',(-0.116460933142332,-0.0451799670343263,
1.14549880118799));
#20740=CARTESIAN_POINT('Ctrl Pts',(-0.0660858892268601,-0.122541963197144,
1.15100093010657));
#20741=CARTESIAN_POINT('Ctrl Pts',(0.0671705316110708,-0.121950798202395,
1.15894309822935));
#20742=CARTESIAN_POINT('Ctrl Pts',(0.138891844802359,-0.00964017357273747,
1.16688526635212));
#20743=CARTESIAN_POINT('Ctrl Pts',(0.0833739592533277,0.111501840422208,
1.17482743447491));
#20744=CARTESIAN_POINT('Ctrl Pts',(-0.0485230383040216,0.130496713571114,
1.18276960259768));
#20745=CARTESIAN_POINT('Ctrl Pts',(-0.113150295826959,0.0561813708375219,
1.18863936159726));
#20746=CARTESIAN_POINT('Ctrl Pts',(-0.117872210070015,0.00861047923971886,
1.19186173122257));
#20747=CARTESIAN_POINT('Ctrl Pts',(-0.117793553451004,0.000106755881474891,
1.19243671147362));
#20748=CARTESIAN_POINT('Origin',(0.,0.,-0.0924367114736175));
#20749=CARTESIAN_POINT('',(-0.117641451221435,8.0229283111194E-5,1.08256328852638));
#20750=CARTESIAN_POINT('',(-0.117630591849015,-7.42484764288953E-5,1.09243671147362));
#20751=CARTESIAN_POINT('',(-0.117775,2.85464118895969E-14,-0.0924367114736175));
#20752=CARTESIAN_POINT('Ctrl Pts',(-0.117641451221435,8.02292831111745E-5,
1.08256328852638));
#20753=CARTESIAN_POINT('Ctrl Pts',(-0.117483998834985,-0.0250372639622414,
1.08425605245455));
#20754=CARTESIAN_POINT('Ctrl Pts',(-0.0972946570053161,-0.0896524615425008,
1.08859514626182));
#20755=CARTESIAN_POINT('Ctrl Pts',(0.00904258428980543,-0.13891320121148,
1.09558056994819));
#20756=CARTESIAN_POINT('Ctrl Pts',(0.121617839487272,-0.067732908692211,
1.1035195595855));
#20757=CARTESIAN_POINT('Ctrl Pts',(0.122860297649024,0.0654522196953821,
1.1114585492228));
#20758=CARTESIAN_POINT('Ctrl Pts',(0.0116325734791967,0.138720326685422,
1.11939753886011));
#20759=CARTESIAN_POINT('Ctrl Pts',(-0.096364912740844,0.0911171059582243,
1.1264324519613));
#20760=CARTESIAN_POINT('Ctrl Pts',(-0.117478530206868,0.0257550656131636,
1.13082103518339));
#20761=CARTESIAN_POINT('Ctrl Pts',(-0.117657565919426,-8.78585414499974E-5,
1.13256328852638));
#20762=CARTESIAN_POINT('Ctrl Pts',(-0.117630591849015,-7.42484764288814E-5,
1.09243671147362));
#20763=CARTESIAN_POINT('Ctrl Pts',(-0.117715241483118,-0.0147626739157663,
1.09342639206478));
#20764=CARTESIAN_POINT('Ctrl Pts',(-0.108350501834675,-0.0686384992808382,
1.0970634620302));
#20765=CARTESIAN_POINT('Ctrl Pts',(-0.0276126195379174,-0.136460326620484,
1.10334792136989));
#20766=CARTESIAN_POINT('Ctrl Pts',(0.0997182217817603,-0.0971604536002107,
1.11129008949267));
#20767=CARTESIAN_POINT('Ctrl Pts',(0.135696927507188,0.0311483765905046,
1.11923225761545));
#20768=CARTESIAN_POINT('Ctrl Pts',(0.0473633069609982,0.130922093830007,
1.12717442573822));
#20769=CARTESIAN_POINT('Ctrl Pts',(-0.0809210029008042,0.111284164335459,
1.13490924369095));
#20770=CARTESIAN_POINT('Ctrl Pts',(-0.117732242679493,0.0359183370635313,
1.13999667226941));
#20771=CARTESIAN_POINT('Ctrl Pts',(-0.117937823388479,-5.41724899699178E-5,
1.14243671147362));
#20772=CARTESIAN_POINT('Origin',(0.,0.,-0.0924367114736175));
#20773=CARTESIAN_POINT('',(-0.117948158721073,4.38502512853227E-5,1.03256328852638));
#20774=CARTESIAN_POINT('',(-0.117667547954054,9.20194976846214E-5,1.04243671147362));
#20775=CARTESIAN_POINT('',(-0.117775,2.85464118895969E-14,-0.0924367114736175));
#20776=CARTESIAN_POINT('Ctrl Pts',(-0.117948158721073,4.38502512853157E-5,
1.03256328852638));
#20777=CARTESIAN_POINT('Ctrl Pts',(-0.117773439871091,-0.0365306738650768,
1.03504473984661));
#20778=CARTESIAN_POINT('Ctrl Pts',(-0.0798690478914953,-0.112422454385097,
1.04017252104593));
#20779=CARTESIAN_POINT('Ctrl Pts',(0.0493427524230464,-0.130168884856471,
1.04794663212436));
#20780=CARTESIAN_POINT('Ctrl Pts',(0.136125055048066,-0.0291310004912345,
1.05588562176166));
#20781=CARTESIAN_POINT('Ctrl Pts',(0.0982941990358779,0.0985743183458784,
1.06382461139897));
#20782=CARTESIAN_POINT('Ctrl Pts',(-0.0295182596522469,0.136041604476578,
1.07176360103627));
#20783=CARTESIAN_POINT('Ctrl Pts',(-0.108818061611988,0.067537217334308,
1.07800982674541));
#20784=CARTESIAN_POINT('Ctrl Pts',(-0.11773014713001,0.0142293884972668,
1.08160972257545));
#20785=CARTESIAN_POINT('Ctrl Pts',(-0.117641451221435,8.02292831111745E-5,
1.08256328852638));
#20786=CARTESIAN_POINT('Ctrl Pts',(-0.117667547954054,9.20194976846197E-5,
1.04243671147362));
#20787=CARTESIAN_POINT('Ctrl Pts',(-0.117475882803567,-0.0261866690710452,
1.04420872248589));
#20788=CARTESIAN_POINT('Ctrl Pts',(-0.0957916308421219,-0.0920126959480487,
1.04862812287242));
#20789=CARTESIAN_POINT('Ctrl Pts',(0.0132451643780021,-0.13859452774087,
1.05569491263321));
#20790=CARTESIAN_POINT('Ctrl Pts',(0.123654649330263,-0.0639797248987874,
1.06363708075599));
#20791=CARTESIAN_POINT('Ctrl Pts',(0.120783771971213,0.0692470788374567,
1.07157924887876));
#20792=CARTESIAN_POINT('Ctrl Pts',(0.00726255089817806,0.139036444335888,
1.07952141700155));
#20793=CARTESIAN_POINT('Ctrl Pts',(-0.0979368667310299,0.0886295245336828,
1.08647390453316));
#20794=CARTESIAN_POINT('Ctrl Pts',(-0.117488804242801,0.0245287720112504,
1.09077900269052));
#20795=CARTESIAN_POINT('Ctrl Pts',(-0.117630591849015,-7.42484764288814E-5,
1.09243671147362));
#20796=CARTESIAN_POINT('Origin',(0.,0.,-0.0924367114736175));
#20797=CARTESIAN_POINT('',(-0.117771476475648,-0.000107683352847938,0.982563288526384));
#20798=CARTESIAN_POINT('',(-0.11796176292438,2.53781033017321E-5,0.992436711473616));
#20799=CARTESIAN_POINT('',(-0.117775,2.85464118895969E-14,-0.0924367114736175));
#20800=CARTESIAN_POINT('Ctrl Pts',(-0.117771476475648,-0.000107683352847945,
0.982563288526384));
#20801=CARTESIAN_POINT('Ctrl Pts',(-0.117856103358663,-0.00933799346614349,
0.983187097359559));
#20802=CARTESIAN_POINT('Ctrl Pts',(-0.112646870919438,-0.057630810124202,
0.986457236071836));
#20803=CARTESIAN_POINT('Ctrl Pts',(-0.0461590140787468,-0.131331607851033,
0.992373704663214));
#20804=CARTESIAN_POINT('Ctrl Pts',(0.0853128637208732,-0.110001641284132,
1.00031269430052));
#20805=CARTESIAN_POINT('Ctrl Pts',(0.138686661656432,0.0120272889735618,
1.00825168393783));
#20806=CARTESIAN_POINT('Ctrl Pts',(0.0651023256631918,0.123046060459907,
1.01619067357513));
#20807=CARTESIAN_POINT('Ctrl Pts',(-0.0680787277209358,0.121424596492465,
1.02412966321244));
#20808=CARTESIAN_POINT('Ctrl Pts',(-0.116790117880403,0.0438975063746073,
1.02958720152952));
#20809=CARTESIAN_POINT('Ctrl Pts',(-0.11795976781127,0.00247402277930658,
1.0323984099675));
#20810=CARTESIAN_POINT('Ctrl Pts',(-0.117948158721073,4.38502512853157E-5,
1.03256328852638));
#20811=CARTESIAN_POINT('Ctrl Pts',(-0.11796176292438,2.53781033017319E-5,
0.992436711473616));
#20812=CARTESIAN_POINT('Ctrl Pts',(-0.117851518882229,-0.0376119105440478,
0.994991052906992));
#20813=CARTESIAN_POINT('Ctrl Pts',(-0.077958511321084,-0.114458475672252,
1.00019278371463));
#20814=CARTESIAN_POINT('Ctrl Pts',(0.0529591494285269,-0.128760265574912,
1.00804190389653));
#20815=CARTESIAN_POINT('Ctrl Pts',(0.136912761112491,-0.0252739657289669,
1.0159840720193));
#20816=CARTESIAN_POINT('Ctrl Pts',(0.0954402180350474,0.101365883217864,
1.02392624014209));
#20817=CARTESIAN_POINT('Ctrl Pts',(-0.0334653697086341,0.135144169424284,
1.03186840826486));
#20818=CARTESIAN_POINT('Ctrl Pts',(-0.109792739119276,0.0652029671457737,
1.03803856537538));
#20819=CARTESIAN_POINT('Ctrl Pts',(-0.117762231070763,0.0130737646421874,
1.04156133311163));
#20820=CARTESIAN_POINT('Ctrl Pts',(-0.117667547954054,9.20194976846197E-5,
1.04243671147362));
#20821=CARTESIAN_POINT('Origin',(0.,0.,-0.0924367114736175));
#20822=CARTESIAN_POINT('',(-0.117585265278523,2.16484251076657E-5,0.932563288526384));
#20823=CARTESIAN_POINT('',(-0.117742563953077,-0.000107211314308964,0.942436711473616));
#20824=CARTESIAN_POINT('',(-0.117775,2.85464118895969E-14,-0.0924367114736175));
#20825=CARTESIAN_POINT('Ctrl Pts',(-0.117585265278523,2.16484251076635E-5,
0.932563288526384));
#20826=CARTESIAN_POINT('Ctrl Pts',(-0.117550805757046,-0.0209622679161363,
0.933975784751614));
#20827=CARTESIAN_POINT('Ctrl Pts',(-0.102172791552808,-0.0813069697478888,
0.938034610855947));
#20828=CARTESIAN_POINT('Ctrl Pts',(-0.00565790085648466,-0.139092177922979,
0.944739766839381));
#20829=CARTESIAN_POINT('Ctrl Pts',(0.113796373024222,-0.0801812402497705,
0.952678756476687));
#20830=CARTESIAN_POINT('Ctrl Pts',(0.129077866376032,0.0521301276928276,
0.960617746113992));
#20831=CARTESIAN_POINT('Ctrl Pts',(0.026197419344502,0.13671993644362,0.968556735751298));
#20832=CARTESIAN_POINT('Ctrl Pts',(-0.0906967139502387,0.0993396518733501,
0.975871916555428));
#20833=CARTESIAN_POINT('Ctrl Pts',(-0.117497098103867,0.02981894716558,
0.980540767480457));
#20834=CARTESIAN_POINT('Ctrl Pts',(-0.117771476475648,-0.000107683352847945,
0.982563288526384));
#20835=CARTESIAN_POINT('Ctrl Pts',(-0.117742563953077,-0.000107211314308957,
0.942436711473616));
#20836=CARTESIAN_POINT('Ctrl Pts',(-0.117833632602859,-0.0103126986533654,
0.943125993953839));
#20837=CARTESIAN_POINT('Ctrl Pts',(-0.111944766202914,-0.0596118697348184,
0.946462665808322));
#20838=CARTESIAN_POINT('Ctrl Pts',(-0.0428565117498991,-0.132465832952297,
0.952446727037066));
#20839=CARTESIAN_POINT('Ctrl Pts',(0.0880997963686447,-0.107806787258123,
0.960388895159846));
#20840=CARTESIAN_POINT('Ctrl Pts',(0.138347640177547,0.0156143509765511,
0.968331063282625));
#20841=CARTESIAN_POINT('Ctrl Pts',(0.061854832590724,0.124731139593481,
0.976273231405407));
#20842=CARTESIAN_POINT('Ctrl Pts',(-0.0713033562375951,0.119581390225944,
0.984215399528185));
#20843=CARTESIAN_POINT('Ctrl Pts',(-0.117322772537986,0.0417718924351975,
0.989603226217589));
#20844=CARTESIAN_POINT('Ctrl Pts',(-0.11796577882491,0.00139640554830399,
0.992343663532733));
#20845=CARTESIAN_POINT('Ctrl Pts',(-0.11796176292438,2.53781033017319E-5,
0.992436711473616));
#20846=CARTESIAN_POINT('Origin',(0.,0.,-0.0924367114736175));
#20847=CARTESIAN_POINT('',(-0.117850913371472,9.6525574830472E-5,0.882563288526384));
#20848=CARTESIAN_POINT('',(-0.117591231449503,3.54948526558943E-5,0.892436711473616));
#20849=CARTESIAN_POINT('',(-0.117775,2.85464118895969E-14,-0.0924367114736175));
#20850=CARTESIAN_POINT('Ctrl Pts',(-0.117850913371472,9.65255748304767E-5,
0.882563288526384));
#20851=CARTESIAN_POINT('Ctrl Pts',(-0.117563006813672,-0.0324172738354332,
0.884764472143669));
#20852=CARTESIAN_POINT('Ctrl Pts',(-0.0867151192651892,-0.104499852648429,
0.889611985640057));
#20853=CARTESIAN_POINT('Ctrl Pts',(0.0353397195745277,-0.134646760160997,
0.897105829015547));
#20854=CARTESIAN_POINT('Ctrl Pts',(0.132293719443212,-0.0433245611326863,
0.905044818652852));
#20855=CARTESIAN_POINT('Ctrl Pts',(0.108141885842356,0.0876583043865096,
0.912983808290157));
#20856=CARTESIAN_POINT('Ctrl Pts',(-0.0150064327997127,0.138395999855801,
0.920922797927463));
#20857=CARTESIAN_POINT('Ctrl Pts',(-0.104951114476159,0.0759553573435841,
0.927449291339539));
#20858=CARTESIAN_POINT('Ctrl Pts',(-0.117615366114572,0.01835136974357,
0.931329454872513));
#20859=CARTESIAN_POINT('Ctrl Pts',(-0.117585265278523,2.16484251076635E-5,
0.932563288526384));
#20860=CARTESIAN_POINT('Ctrl Pts',(-0.117591231449503,3.54948526559117E-5,
0.892436711473616));
#20861=CARTESIAN_POINT('Ctrl Pts',(-0.117532234588281,-0.0218238662162972,
0.893908324374946));
#20862=CARTESIAN_POINT('Ctrl Pts',(-0.101194437785642,-0.0830895288483654,
0.898027326650536));
#20863=CARTESIAN_POINT('Ctrl Pts',(-0.00250162451743248,-0.139203517821528,
0.904793718300386));
#20864=CARTESIAN_POINT('Ctrl Pts',(0.115632500949424,-0.0775435504945224,
0.912735886423165));
#20865=CARTESIAN_POINT('Ctrl Pts',(0.127835376168433,0.0551542754370876,
0.920678054545947));
#20866=CARTESIAN_POINT('Ctrl Pts',(0.0229279137899797,0.137325118854324,
0.928620222668725));
#20867=CARTESIAN_POINT('Ctrl Pts',(-0.0920562790907298,0.0974788594069619,
0.935873108311283));
#20868=CARTESIAN_POINT('Ctrl Pts',(-0.117483857027998,0.0288844367965532,
0.94047860457958));
#20869=CARTESIAN_POINT('Ctrl Pts',(-0.117742563953077,-0.000107211314308957,
0.942436711473616));
#20870=CARTESIAN_POINT('Origin',(0.,0.,-0.0924367114736175));
#20871=CARTESIAN_POINT('',(-0.11789232318732,-8.18790992476613E-5,0.832563288526384));
#20872=CARTESIAN_POINT('',(-0.117872825429845,8.99519344067963E-5,0.842436711473616));
#20873=CARTESIAN_POINT('',(-0.117775,2.85464118895969E-14,-0.0924367114736175));
#20874=CARTESIAN_POINT('Ctrl Pts',(-0.11789232318732,-8.18790992476734E-5,
0.832563288526384));
#20875=CARTESIAN_POINT('Ctrl Pts',(-0.117932494517479,-0.00515170743829337,
0.832906829656623));
#20876=CARTESIAN_POINT('Ctrl Pts',(-0.115332713682068,-0.0492334187378749,
0.835896700665964));
#20877=CARTESIAN_POINT('Ctrl Pts',(-0.059752088941783,-0.125731196083361,
0.841532901554406));
#20878=CARTESIAN_POINT('Ctrl Pts',(0.0732361146625898,-0.118385460722959,
0.849471891191712));
#20879=CARTESIAN_POINT('Ctrl Pts',(0.139181674492094,-0.00266594955618734,
0.857410880829018));
#20880=CARTESIAN_POINT('Ctrl Pts',(0.077715950067195,0.115494055719818,
0.865349870466323));
#20881=CARTESIAN_POINT('Ctrl Pts',(-0.0548934004223171,0.127927168308903,
0.87328886010363));
#20882=CARTESIAN_POINT('Ctrl Pts',(-0.114416768398411,0.0522742940766184,
0.879026666123649));
#20883=CARTESIAN_POINT('Ctrl Pts',(-0.117909136832228,0.0066718045071592,
0.882118142264567));
#20884=CARTESIAN_POINT('Ctrl Pts',(-0.117850913371472,9.65255748304767E-5,
0.882563288526384));
#20885=CARTESIAN_POINT('Ctrl Pts',(-0.117872825429845,8.99519344067998E-5,
0.842436711473616));
#20886=CARTESIAN_POINT('Ctrl Pts',(-0.117591169542271,-0.0331870933343037,
0.844690654796053));
#20887=CARTESIAN_POINT('Ctrl Pts',(-0.0854771005934613,-0.106025606004136,
0.84959198749275));
#20888=CARTESIAN_POINT('Ctrl Pts',(0.0380692928980519,-0.133920149482284,
0.857140709563706));
#20889=CARTESIAN_POINT('Ctrl Pts',(0.133179650076608,-0.0405839661022353,
0.865082877686486));
#20890=CARTESIAN_POINT('Ctrl Pts',(0.106283765719693,0.0899312995767124,
0.873025045809266));
#20891=CARTESIAN_POINT('Ctrl Pts',(-0.0179789669825735,0.138060255849953,
0.880967213932046));
#20892=CARTESIAN_POINT('Ctrl Pts',(-0.105798194743126,0.0742290978659706,
0.887437769153496));
#20893=CARTESIAN_POINT('Ctrl Pts',(-0.117638368248411,0.0175004969839459,
0.891260935000686));
#20894=CARTESIAN_POINT('Ctrl Pts',(-0.117591231449503,3.54948526559117E-5,
0.892436711473616));
#20895=CARTESIAN_POINT('Origin',(0.,0.,-0.0924367114736175));
#20896=CARTESIAN_POINT('',(-0.117598114366551,-4.51832715892789E-5,0.782563288526384));
#20897=CARTESIAN_POINT('',(-0.117874685330111,-8.92836445515327E-5,0.792436711473617));
#20898=CARTESIAN_POINT('',(-0.117775,2.85464118895969E-14,-0.0924367114736175));
#20899=CARTESIAN_POINT('Ctrl Pts',(-0.117598114366551,-4.518327158929E-5,
0.782563288526384));
#20900=CARTESIAN_POINT('Ctrl Pts',(-0.117656123976761,-0.0168608793038394,
0.783695517048678));
#20901=CARTESIAN_POINT('Ctrl Pts',(-0.106420815930739,-0.0729055463807818,
0.787474075450074));
#20902=CARTESIAN_POINT('Ctrl Pts',(-0.0202952816069424,-0.137719814645367,
0.793898963730571));
#20903=CARTESIAN_POINT('Ctrl Pts',(0.104705698854998,-0.0917352845351548,
0.801837953367879));
#20904=CARTESIAN_POINT('Ctrl Pts',(0.133855787965376,0.0382266115373486,
0.809776943005182));
#20905=CARTESIAN_POINT('Ctrl Pts',(0.0404700769297216,0.133194664588195,
0.81771593264249));
#20906=CARTESIAN_POINT('Ctrl Pts',(-0.0843190215395119,0.107398870964955,
0.825311381149555));
#20907=CARTESIAN_POINT('Ctrl Pts',(-0.117623050954756,0.0339016606582783,
0.830260499777521));
#20908=CARTESIAN_POINT('Ctrl Pts',(-0.11789232318732,-8.18790992476734E-5,
0.832563288526384));
#20909=CARTESIAN_POINT('Ctrl Pts',(-0.117874685330111,-8.9283644551537E-5,
0.792436711473617));
#20910=CARTESIAN_POINT('Ctrl Pts',(-0.11792303416021,-0.00583050672374999,
0.7928255958429));
#20911=CARTESIAN_POINT('Ctrl Pts',(-0.114931453360353,-0.0506053896743902,
0.795861869586443));
#20912=CARTESIAN_POINT('Ctrl Pts',(-0.0575513573065257,-0.126774282767806,
0.801545532704245));
#20913=CARTESIAN_POINT('Ctrl Pts',(0.0753527000357912,-0.117071978271622,
0.809487700827026));
#20914=CARTESIAN_POINT('Ctrl Pts',(0.139225942868322,-0.000119714417332432,
0.817429868949805));
#20915=CARTESIAN_POINT('Ctrl Pts',(0.0755539188089132,0.116942220141962,
0.825372037072586));
#20916=CARTESIAN_POINT('Ctrl Pts',(-0.0573332568284509,0.12687306712048,
0.833314205195366));
#20917=CARTESIAN_POINT('Ctrl Pts',(-0.114890414736801,0.0507419104293215,
0.839002429995709));
#20918=CARTESIAN_POINT('Ctrl Pts',(-0.117921990994851,0.00589875908008548,
0.842043265421793));
#20919=CARTESIAN_POINT('Ctrl Pts',(-0.117872825429845,8.99519344067998E-5,
0.842436711473616));
#20920=CARTESIAN_POINT('Origin',(0.,0.,-0.0924367114736175));
#20921=CARTESIAN_POINT('',(-0.11772691567491,0.000105512987197037,0.732563288526384));
#20922=CARTESIAN_POINT('',(-0.117591850253004,-3.65476421498312E-5,0.742436711473616));
#20923=CARTESIAN_POINT('',(-0.117775,2.85464118895969E-14,-0.0924367114736175));
#20924=CARTESIAN_POINT('Ctrl Pts',(-0.11772691567491,0.000105512987197042,
0.732563288526384));
#20925=CARTESIAN_POINT('Ctrl Pts',(-0.117479624464894,-0.0283451130369189,
0.734484204440733));
#20926=CARTESIAN_POINT('Ctrl Pts',(-0.0928318426870313,-0.096374559506161,
0.739051450234184));
#20927=CARTESIAN_POINT('Ctrl Pts',(0.0209425314183671,-0.137622876656644,
0.746265025906738));
#20928=CARTESIAN_POINT('Ctrl Pts',(0.126986869252672,-0.0570349089493802,
0.754204015544043));
#20929=CARTESIAN_POINT('Ctrl Pts',(0.11678343126468,0.0757646090434518,
0.762143005181349));
#20930=CARTESIAN_POINT('Ctrl Pts',(-0.000327234354877375,0.139206819944772,
0.770081994818654));
#20931=CARTESIAN_POINT('Ctrl Pts',(-0.100479183608201,0.0843410365921374,
0.776888755933667));
#20932=CARTESIAN_POINT('Ctrl Pts',(-0.117520539541507,0.0224420334666934,
0.781049187169576));
#20933=CARTESIAN_POINT('Ctrl Pts',(-0.117598114366551,-4.518327158929E-5,
0.782563288526384));
#20934=CARTESIAN_POINT('Ctrl Pts',(-0.117591850253004,-3.65476421498364E-5,
0.742436711473616));
#20935=CARTESIAN_POINT('Ctrl Pts',(-0.117640211257931,-0.0174335619022046,
0.743607926264006));
#20936=CARTESIAN_POINT('Ctrl Pts',(-0.105863856762799,-0.0740921523660566,
0.747426530428656));
#20937=CARTESIAN_POINT('Ctrl Pts',(-0.0182163644075178,-0.138029133036789,
0.753892523967566));
#20938=CARTESIAN_POINT('Ctrl Pts',(0.106128952536144,-0.0901139441634624,
0.761834692090347));
#20939=CARTESIAN_POINT('Ctrl Pts',(0.133249245915149,0.0403548753208232,
0.769776860213125));
#20940=CARTESIAN_POINT('Ctrl Pts',(0.0382995408207276,0.133854483197375,
0.777719028335907));
#20941=CARTESIAN_POINT('Ctrl Pts',(-0.0853693283863186,0.106155717082476,
0.785272312089402));
#20942=CARTESIAN_POINT('Ctrl Pts',(-0.117593892160246,0.0332537408718532,
0.79017820646864));
#20943=CARTESIAN_POINT('Ctrl Pts',(-0.117874685330111,-8.9283644551537E-5,
0.792436711473617));
#20944=CARTESIAN_POINT('Origin',(0.,0.,-0.0924367114736175));
#20945=CARTESIAN_POINT('',(-0.117964947617991,-1.73329198795185E-5,0.682563288526384));
#20946=CARTESIAN_POINT('',(-0.117740574064672,0.000107068518266168,0.692436711473616));
#20947=CARTESIAN_POINT('',(-0.117775,2.85464118895969E-14,-0.0924367114736175));
#20948=CARTESIAN_POINT('Ctrl Pts',(-0.117964947617991,-1.73329198795367E-5,
0.682563288526384));
#20949=CARTESIAN_POINT('Ctrl Pts',(-0.117966864156947,-0.000949576032666658,
0.682626561953687));
#20950=CARTESIAN_POINT('Ctrl Pts',(-0.117534558560489,-0.0408698671952461,
0.685336165260092));
#20951=CARTESIAN_POINT('Ctrl Pts',(-0.0726787294560835,-0.118728463672822,
0.690692098445597));
#20952=CARTESIAN_POINT('Ctrl Pts',(0.0603425395611779,-0.125448888878168,
0.698631088082904));
#20953=CARTESIAN_POINT('Ctrl Pts',(0.138124349154501,-0.0173294538893964,
0.706570077720209));
#20954=CARTESIAN_POINT('Ctrl Pts',(0.0894627833767505,0.106653908470079,
0.714509067357515));
#20955=CARTESIAN_POINT('Ctrl Pts',(-0.0410958292974484,0.133002927094911,
0.72244805699482));
#20956=CARTESIAN_POINT('Ctrl Pts',(-0.111546724107196,0.0606813038481789,
0.728466130717777));
#20957=CARTESIAN_POINT('Ctrl Pts',(-0.117820302634623,0.0108495967181263,
0.731837874561632));
#20958=CARTESIAN_POINT('Ctrl Pts',(-0.11772691567491,0.000105512987197042,
0.732563288526384));
#20959=CARTESIAN_POINT('Ctrl Pts',(-0.117740574064672,0.000107068518266165,
0.692436711473616));
#20960=CARTESIAN_POINT('Ctrl Pts',(-0.117483171888848,-0.0288182833237499,
0.694390256685113));
#20961=CARTESIAN_POINT('Ctrl Pts',(-0.0921515028359353,-0.0973455904149804,
0.698991191270869));
#20962=CARTESIAN_POINT('Ctrl Pts',(0.022691720100341,-0.137364345221032,
0.706239515230886));
#20963=CARTESIAN_POINT('Ctrl Pts',(0.127740337615313,-0.0553740340325759,
0.714181683353665));
#20964=CARTESIAN_POINT('Ctrl Pts',(0.115765682611161,0.077344581120379,
0.722123851476446));
#20965=CARTESIAN_POINT('Ctrl Pts',(-0.00226223072526165,0.139207614056346,
0.730066019599226));
#20966=CARTESIAN_POINT('Ctrl Pts',(-0.101117998472899,0.083225715609228,
0.736836972931616));
#20967=CARTESIAN_POINT('Ctrl Pts',(-0.117530897055598,0.0218902846491045,
0.740960536889746));
#20968=CARTESIAN_POINT('Ctrl Pts',(-0.117591850253004,-3.65476421498364E-5,
0.742436711473616));
#20969=CARTESIAN_POINT('Origin',(0.,0.,-0.0924367114736175));
#20970=CARTESIAN_POINT('',(-0.117676160015555,-9.46906955630148E-5,0.632563288526383));
#20971=CARTESIAN_POINT('',(-0.117962383120995,-2.41598447144192E-5,0.642436711473616));
#20972=CARTESIAN_POINT('',(-0.117775,2.85464118895969E-14,-0.0924367114736175));
#20973=CARTESIAN_POINT('Ctrl Pts',(-0.117676160015555,-9.46906955630045E-5,
0.632563288526383));
#20974=CARTESIAN_POINT('Ctrl Pts',(-0.117771520970562,-0.0127268345011372,
0.633415249345741));
#20975=CARTESIAN_POINT('Ctrl Pts',(-0.110078248258936,-0.064483421762156,
0.636913540044201));
#20976=CARTESIAN_POINT('Ctrl Pts',(-0.0347063025259737,-0.134811417789573,
0.643058160621763));
#20977=CARTESIAN_POINT('Ctrl Pts',(0.0944472082050275,-0.102266175560326,
0.65099715025907));
#20978=CARTESIAN_POINT('Ctrl Pts',(0.137140772714236,0.0238967416356601,
0.658936139896373));
#20979=CARTESIAN_POINT('Ctrl Pts',(0.054291358674537,0.128183829614862,
0.666875129533682));
#20980=CARTESIAN_POINT('Ctrl Pts',(-0.0772016597727435,0.11523146575827,
0.674750845743682));
#20981=CARTESIAN_POINT('Ctrl Pts',(-0.117886707375211,0.0380402955314478,
0.679980232074585));
#20982=CARTESIAN_POINT('Ctrl Pts',(-0.117964947617991,-1.73329198795367E-5,
0.682563288526384));
#20983=CARTESIAN_POINT('Ctrl Pts',(-0.117962383120995,-2.41598447144253E-5,
0.642436711473616));
#20984=CARTESIAN_POINT('Ctrl Pts',(-0.117966033213387,-0.0013279541977536,
0.642525197731959));
#20985=CARTESIAN_POINT('Ctrl Pts',(-0.117355585052125,-0.0416360146359673,
0.645261073364563));
#20986=CARTESIAN_POINT('Ctrl Pts',(-0.0715088964667609,-0.119458592094588,
0.650644338371427));
#20987=CARTESIAN_POINT('Ctrl Pts',(0.0616402393688536,-0.124837327709565,
0.658586506494205));
#20988=CARTESIAN_POINT('Ctrl Pts',(0.138320583400205,-0.0158522461166236,
0.666528674616987));
#20989=CARTESIAN_POINT('Ctrl Pts',(0.0882850628235238,0.107655121482266,
0.674470842739765));
#20990=CARTESIAN_POINT('Ctrl Pts',(-0.0426286451686149,0.132539337972556,
0.682413010862546));
#20991=CARTESIAN_POINT('Ctrl Pts',(-0.111894847147975,0.059748848130285,
0.68840163377383));
#20992=CARTESIAN_POINT('Ctrl Pts',(-0.117831996057943,0.0103805377030848,
0.691742867310853));
#20993=CARTESIAN_POINT('Ctrl Pts',(-0.117740574064672,0.000107068518266165,
0.692436711473616));
#20994=CARTESIAN_POINT('Origin',(0.,0.,-0.0924367114736175));
#20995=CARTESIAN_POINT('',(-0.117626285855324,7.11112359239178E-5,0.582563288526384));
#20996=CARTESIAN_POINT('',(-0.11766919235599,-9.26074537421634E-5,0.592436711473616));
#20997=CARTESIAN_POINT('',(-0.117775,2.85464118895969E-14,-0.0924367114736175));
#20998=CARTESIAN_POINT('Ctrl Pts',(-0.117626285855324,7.11112359239024E-5,
0.582563288526383));
#20999=CARTESIAN_POINT('Ctrl Pts',(-0.117492102008102,-0.0242809575267813,
0.584203936737797));
#21000=CARTESIAN_POINT('Ctrl Pts',(-0.0982512120079041,-0.0881067492982899,
0.588490914828312));
#21001=CARTESIAN_POINT('Ctrl Pts',(0.00631176444456456,-0.139064040754811,
0.595424222797929));
#21002=CARTESIAN_POINT('Ctrl Pts',(0.120263693490807,-0.0701091280034811,
0.603363212435234));
#21003=CARTESIAN_POINT('Ctrl Pts',(0.124122453355413,0.0630258865426945,
0.611302202072541));
#21004=CARTESIAN_POINT('Ctrl Pts',(0.0143556138404206,0.138465021405133,
0.619241191709845));
#21005=CARTESIAN_POINT('Ctrl Pts',(-0.0953630726970595,0.0926558297308384,
0.626328220527794));
#21006=CARTESIAN_POINT('Ctrl Pts',(-0.117475314221613,0.0265106736450616,
0.630768919466639));
#21007=CARTESIAN_POINT('Ctrl Pts',(-0.117676160015555,-9.46906955630045E-5,
0.632563288526383));
#21008=CARTESIAN_POINT('Ctrl Pts',(-0.11766919235599,-9.26074537421669E-5,
0.592436711473616));
#21009=CARTESIAN_POINT('Ctrl Pts',(-0.117764072896019,-0.0130062487266101,
0.593307528153066));
#21010=CARTESIAN_POINT('Ctrl Pts',(-0.109848366281979,-0.0650658641993071,
0.596825734206776));
#21011=CARTESIAN_POINT('Ctrl Pts',(-0.0336977294021144,-0.135086418755761,
0.602991329634746));
#21012=CARTESIAN_POINT('Ctrl Pts',(0.0952657566843092,-0.101529863106778,
0.610933497757526));
#21013=CARTESIAN_POINT('Ctrl Pts',(0.136956022624868,0.025038477707157,
0.618875665880307));
#21014=CARTESIAN_POINT('Ctrl Pts',(0.0531805018142573,0.128669000640787,
0.626817834003085));
#21015=CARTESIAN_POINT('Ctrl Pts',(-0.0778376600742765,0.114584191752874,
0.634671515867523));
#21016=CARTESIAN_POINT('Ctrl Pts',(-0.117856827377429,0.0376798124439797,
0.639877808357699));
#21017=CARTESIAN_POINT('Ctrl Pts',(-0.117962383120995,-2.41598447144253E-5,
0.642436711473616));
#21018=CARTESIAN_POINT('Origin',(0.,0.,-0.0924367114736175));
#21019=CARTESIAN_POINT('',(-0.117934829819181,5.63106208242181E-5,0.532563288526383));
#21020=CARTESIAN_POINT('',(-0.117629301205424,7.34277634442948E-5,0.542436711473615));
#21021=CARTESIAN_POINT('',(-0.117775,2.85464118895969E-14,-0.0924367114736175));
#21022=CARTESIAN_POINT('Ctrl Pts',(-0.117934829819181,5.63106208242166E-5,
0.532563288526383));
#21023=CARTESIAN_POINT('Ctrl Pts',(-0.117723349859012,-0.0357608023914865,
0.534992624129852));
#21024=CARTESIAN_POINT('Ctrl Pts',(-0.0811985738067347,-0.110967619805887,
0.540068289612422));
#21025=CARTESIAN_POINT('Ctrl Pts',(0.0467759446245483,-0.131113145053959,
0.547790284974095));
#21026=CARTESIAN_POINT('Ctrl Pts',(0.135526478334676,-0.031799677225719,
0.555729274611401));
#21027=CARTESIAN_POINT('Ctrl Pts',(0.100211809365564,0.0966242157284558,
0.563668264248707));
#21028=CARTESIAN_POINT('Ctrl Pts',(-0.0268399031138932,0.136595261273209,
0.571607253886012));
#21029=CARTESIAN_POINT('Ctrl Pts',(-0.108142973925314,0.0691035501437442,
0.577905595311905));
#21030=CARTESIAN_POINT('Ctrl Pts',(-0.117708537635025,0.0149983997031143,
0.581557606858695));
#21031=CARTESIAN_POINT('Ctrl Pts',(-0.117626285855324,7.11112359239024E-5,
0.582563288526383));
#21032=CARTESIAN_POINT('Ctrl Pts',(-0.117629301205424,7.34277634442983E-5,
0.542436711473615));
#21033=CARTESIAN_POINT('Ctrl Pts',(-0.11748956090956,-0.0244625652698295,
0.544089858574172));
#21034=CARTESIAN_POINT('Ctrl Pts',(-0.0980201725405651,-0.0884941619373469,
0.548390395048989));
#21035=CARTESIAN_POINT('Ctrl Pts',(0.00702343738442799,-0.139048728244533,
0.555338320898066));
#21036=CARTESIAN_POINT('Ctrl Pts',(0.12066450826877,-0.0694546898587181,
0.563280489020846));
#21037=CARTESIAN_POINT('Ctrl Pts',(0.123764493242992,0.063766979789076,
0.571222657143626));
#21038=CARTESIAN_POINT('Ctrl Pts',(0.0134834875971477,0.13857154491934,
0.579164825266405));
#21039=CARTESIAN_POINT('Ctrl Pts',(-0.0957036897026042,0.092147346049863,
0.586236176709736));
#21040=CARTESIAN_POINT('Ctrl Pts',(-0.117475624432153,0.0262528025703711,
0.590660138778806));
#21041=CARTESIAN_POINT('Ctrl Pts',(-0.11766919235599,-9.26074537421669E-5,
0.592436711473616));
#21042=CARTESIAN_POINT('Origin',(0.,0.,-0.0924367114736175));
#21043=CARTESIAN_POINT('',(-0.117794891956694,-0.000106411733115368,0.482563288526384));
#21044=CARTESIAN_POINT('',(-0.117936566864074,5.52347650140707E-5,0.492436711473616));
#21045=CARTESIAN_POINT('',(-0.117775,2.85464118895969E-14,-0.0924367114736175));
#21046=CARTESIAN_POINT('Ctrl Pts',(-0.117794891956694,-0.000106411733115381,
0.482563288526384));
#21047=CARTESIAN_POINT('Ctrl Pts',(-0.117872998614688,-0.00856127641466401,
0.483134981642805));
#21048=CARTESIAN_POINT('Ctrl Pts',(-0.113184542395844,-0.0560672187853419,
0.486353004638329));
#21049=CARTESIAN_POINT('Ctrl Pts',(-0.0487302328423073,-0.130399425645183,
0.492217357512954));
#21050=CARTESIAN_POINT('Ctrl Pts',(0.0831353173341669,-0.111656458896056,
0.50015634715026));
#21051=CARTESIAN_POINT('Ctrl Pts',(0.13889618212661,0.00930034365552528,
0.508095336787567));
#21052=CARTESIAN_POINT('Ctrl Pts',(0.0675071113591811,0.12174331898465,
0.516034326424871));
#21053=CARTESIAN_POINT('Ctrl Pts',(-0.0656800932930844,0.122738629397884,
0.523973316062178));
#21054=CARTESIAN_POINT('Ctrl Pts',(-0.116384786286051,0.04545243224792,
0.529482970096015));
#21055=CARTESIAN_POINT('Ctrl Pts',(-0.117953719733239,0.00325558390455253,
0.53234629425075));
#21056=CARTESIAN_POINT('Ctrl Pts',(-0.117934829819181,5.63106208242166E-5,
0.532563288526383));
#21057=CARTESIAN_POINT('Ctrl Pts',(-0.117936566864074,5.52347650140663E-5,
0.492436711473616));
#21058=CARTESIAN_POINT('Ctrl Pts',(-0.117728017843002,-0.0358510361847084,
0.494872188995279));
#21059=CARTESIAN_POINT('Ctrl Pts',(-0.0810366231971402,-0.111156550628637,
0.499955055891203));
#21060=CARTESIAN_POINT('Ctrl Pts',(0.0471380885036503,-0.131003351527116,
0.507685312161385));
#21061=CARTESIAN_POINT('Ctrl Pts',(0.135643160584381,-0.031381690295376,
0.515627480284167));
#21062=CARTESIAN_POINT('Ctrl Pts',(0.0998851624184703,0.0969888232104648,
0.523569648406945));
#21063=CARTESIAN_POINT('Ctrl Pts',(-0.0273779061153799,0.136507610615132,
0.531511816529727));
#21064=CARTESIAN_POINT('Ctrl Pts',(-0.108290992649607,0.0687756007668377,
0.537800837551949));
#21065=CARTESIAN_POINT('Ctrl Pts',(-0.117713344367368,0.0148299618267192,
0.541442469199912));
#21066=CARTESIAN_POINT('Ctrl Pts',(-0.117629301205424,7.34277634442983E-5,
0.542436711473615));
#21067=CARTESIAN_POINT('Origin',(0.,0.,-0.0924367114736175));
#21068=CARTESIAN_POINT('',(-0.117582256074849,9.06819982020624E-6,0.432563288526383));
#21069=CARTESIAN_POINT('',(-0.11779560903417,-0.000106574656651148,0.442436711473616));
#21070=CARTESIAN_POINT('',(-0.117775,2.85464118895969E-14,-0.0924367114736175));
#21071=CARTESIAN_POINT('Ctrl Pts',(-0.117582256074849,9.06819982019261E-6,
0.432563288526383));
#21072=CARTESIAN_POINT('Ctrl Pts',(-0.117568373935691,-0.020201912089319,
0.43392366903486));
#21073=CARTESIAN_POINT('Ctrl Pts',(-0.10300922874285,-0.0797477867736473,
0.437930379422439));
#21074=CARTESIAN_POINT('Ctrl Pts',(-0.00838939967687663,-0.138954178686792,
0.44458341968912));
#21075=CARTESIAN_POINT('Ctrl Pts',(0.11219917790857,-0.0824013973067221,
0.452522409326426));
#21076=CARTESIAN_POINT('Ctrl Pts',(0.13007709763057,0.0495842159710775,
0.460461398963732));
#21077=CARTESIAN_POINT('Ctrl Pts',(0.0288783492374893,0.136178877755608,
0.468400388601037));
#21078=CARTESIAN_POINT('Ctrl Pts',(-0.0895654556576369,0.100852400902523,
0.475767685121922));
#21079=CARTESIAN_POINT('Ctrl Pts',(-0.117511448025972,0.0305757367622385,
0.480488651763704));
#21080=CARTESIAN_POINT('Ctrl Pts',(-0.117794891956694,-0.000106411733115381,
0.482563288526384));
#21081=CARTESIAN_POINT('Ctrl Pts',(-0.11779560903417,-0.000106574656651151,
0.442436711473616));
#21082=CARTESIAN_POINT('Ctrl Pts',(-0.117873644338608,-0.00854245500997505,
0.443007130042126));
#21083=CARTESIAN_POINT('Ctrl Pts',(-0.113196618671047,-0.056044542179559,
0.446224937984896));
#21084=CARTESIAN_POINT('Ctrl Pts',(-0.0487473834415776,-0.130413074907061,
0.452090135301926));
#21085=CARTESIAN_POINT('Ctrl Pts',(0.0831820848081396,-0.111645054821459,
0.460032303424706));
#21086=CARTESIAN_POINT('Ctrl Pts',(0.138908217753341,0.00940130521287039,
0.467974471547486));
#21087=CARTESIAN_POINT('Ctrl Pts',(0.0673801526530663,0.121835103839429,
0.475916639670265));
#21088=CARTESIAN_POINT('Ctrl Pts',(-0.0658750545035054,0.12265543075329,
0.483858807793047));
#21089=CARTESIAN_POINT('Ctrl Pts',(-0.116424939330292,0.0453161125527027,
0.489365498394162));
#21090=CARTESIAN_POINT('Ctrl Pts',(-0.11795471279604,0.00317945345687678,
0.492224799621019));
#21091=CARTESIAN_POINT('Ctrl Pts',(-0.117936566864074,5.52347650140663E-5,
0.492436711473616));
#21092=CARTESIAN_POINT('Origin',(0.,0.,-0.0924367114736175));
#21093=CARTESIAN_POINT('',(-0.117828183671793,0.000101754196006455,0.382563288526383));
#21094=CARTESIAN_POINT('',(-0.117581664177921,7.09484545444172E-6,0.392436711473616));
#21095=CARTESIAN_POINT('',(-0.117775,2.85464118895969E-14,-0.0924367114736175));
#21096=CARTESIAN_POINT('Ctrl Pts',(-0.117828183671793,0.000101754196006446,
0.382563288526384));
#21097=CARTESIAN_POINT('Ctrl Pts',(-0.117538790254565,-0.0316580736410773,
0.384712356426916));
#21098=CARTESIAN_POINT('Ctrl Pts',(-0.0879068326507716,-0.103002379129266,
0.38950775420655));
#21099=CARTESIAN_POINT('Ctrl Pts',(0.0326876424682324,-0.135315053971568,
0.396949481865287));
#21100=CARTESIAN_POINT('Ctrl Pts',(0.13141703692502,-0.0459152284901983,
0.404888471502591));
#21101=CARTESIAN_POINT('Ctrl Pts',(0.109843140674695,0.0855168418978295,
0.412827461139898));
#21102=CARTESIAN_POINT('Ctrl Pts',(-0.0122846228212416,0.13866410438033,
0.420766450777203));
#21103=CARTESIAN_POINT('Ctrl Pts',(-0.104166535924894,0.0775181589932739,
0.427345059906032));
#21104=CARTESIAN_POINT('Ctrl Pts',(-0.117595378674006,0.0191142356295008,
0.431277339155758));
#21105=CARTESIAN_POINT('Ctrl Pts',(-0.117582256074849,9.06819982019261E-6,
0.432563288526383));
#21106=CARTESIAN_POINT('Ctrl Pts',(-0.117581664177921,7.09484545444172E-6,
0.392436711473616));
#21107=CARTESIAN_POINT('Ctrl Pts',(-0.117570873504463,-0.0200907396801347,
0.393789460463232));
#21108=CARTESIAN_POINT('Ctrl Pts',(-0.10312708440739,-0.079535468422451,
0.397789598827109));
#21109=CARTESIAN_POINT('Ctrl Pts',(-0.00873482453528946,-0.138951719454826,
0.404437126565246));
#21110=CARTESIAN_POINT('Ctrl Pts',(0.112042812448737,-0.0826455423945668,
0.412379294688026));
#21111=CARTESIAN_POINT('Ctrl Pts',(0.130177722634257,0.049372441998279,
0.420321462810806));
#21112=CARTESIAN_POINT('Ctrl Pts',(0.0290564652212241,0.136160197297018,
0.428263630933586));
#21113=CARTESIAN_POINT('Ctrl Pts',(-0.0895090212855029,0.100936776489487,
0.435635380487856));
#21114=CARTESIAN_POINT('Ctrl Pts',(-0.117511471984497,0.0306096014671689,
0.440359740667866));
#21115=CARTESIAN_POINT('Ctrl Pts',(-0.11779560903417,-0.000106574656651151,
0.442436711473616));
#21116=CARTESIAN_POINT('Origin',(0.,0.,-0.0924367114736175));
#21117=CARTESIAN_POINT('',(-0.117911328466355,-7.22474488887591E-5,0.332563288526384));
#21118=CARTESIAN_POINT('',(-0.117821685414254,0.000103165543095151,0.342436711473616));
#21119=CARTESIAN_POINT('',(-0.117775,2.85464118895969E-14,-0.0924367114736175));
#21120=CARTESIAN_POINT('Ctrl Pts',(-0.117911328466355,-7.22474488887752E-5,
0.332563288526384));
#21121=CARTESIAN_POINT('Ctrl Pts',(-0.117942332027964,-0.00437115939612809,
0.332854713939869));
#21122=CARTESIAN_POINT('Ctrl Pts',(-0.115777752883067,-0.0476754067323583,
0.335792469232457));
#21123=CARTESIAN_POINT('Ctrl Pts',(-0.0622106591311991,-0.12453304658572,
0.341376554404146));
#21124=CARTESIAN_POINT('Ctrl Pts',(0.0708961914151981,-0.119801401679107,
0.349315544041452));
#21125=CARTESIAN_POINT('Ctrl Pts',(0.1391024375543,-0.00539978406154301,
0.357254533678757));
#21126=CARTESIAN_POINT('Ctrl Pts',(0.0799699354250877,0.113944965792994,
0.365193523316063));
#21127=CARTESIAN_POINT('Ctrl Pts',(-0.0523695618881846,0.128980908622551,
0.373132512953369));
#21128=CARTESIAN_POINT('Ctrl Pts',(-0.113921748517257,0.0538356345748906,
0.378922434690143));
#21129=CARTESIAN_POINT('Ctrl Pts',(-0.117895144954496,0.00745050051778832,
0.382066026547814));
#21130=CARTESIAN_POINT('Ctrl Pts',(-0.117828183671793,0.000101754196006446,
0.382563288526384));
#21131=CARTESIAN_POINT('Ctrl Pts',(-0.117821685414254,0.000103165543095145,
0.342436711473616));
#21132=CARTESIAN_POINT('Ctrl Pts',(-0.117532262555972,-0.0314544122979593,
0.344571790884339));
#21133=CARTESIAN_POINT('Ctrl Pts',(-0.0882170202347594,-0.102616110661261,
0.349354259669323));
#21134=CARTESIAN_POINT('Ctrl Pts',(0.0320320385160992,-0.135491055083419,
0.356784117828566));
#21135=CARTESIAN_POINT('Ctrl Pts',(0.131227975626944,-0.0465090949381858,
0.364726285951346));
#21136=CARTESIAN_POINT('Ctrl Pts',(0.110205605501345,0.0850799742312894,
0.372668454074126));
#21137=CARTESIAN_POINT('Ctrl Pts',(-0.0117764211155082,0.138727046407055,
0.380610622196906));
#21138=CARTESIAN_POINT('Ctrl Pts',(-0.10403099481448,0.0777947493501838,
0.387200041330069));
#21139=CARTESIAN_POINT('Ctrl Pts',(-0.117591991327853,0.019241607989002,
0.391142071088973));
#21140=CARTESIAN_POINT('Ctrl Pts',(-0.117581664177921,7.09484545444172E-6,
0.392436711473616));
#21141=CARTESIAN_POINT('Origin',(0.,0.,-0.0924367114736175));
#21142=CARTESIAN_POINT('',(-0.117608153246896,-5.64262068778628E-5,0.282563288526383));
#21143=CARTESIAN_POINT('',(-0.117918861549493,-6.80329776671096E-5,0.292436711473615));
#21144=CARTESIAN_POINT('',(-0.117775,2.85464118895969E-14,-0.0924367114736175));
#21145=CARTESIAN_POINT('Ctrl Pts',(-0.117608153246896,-5.64262068778604E-5,
0.282563288526383));
#21146=CARTESIAN_POINT('Ctrl Pts',(-0.117677606263852,-0.0160946837114709,
0.283643401331924));
#21147=CARTESIAN_POINT('Ctrl Pts',(-0.107144424846824,-0.0713401098021974,
0.287369844016567));
#21148=CARTESIAN_POINT('Ctrl Pts',(-0.0229969941138309,-0.137294515779738,
0.293742616580312));
#21149=CARTESIAN_POINT('Ctrl Pts',(0.102883268653204,-0.0937746172089793,
0.301681606217617));
#21150=CARTESIAN_POINT('Ctrl Pts',(0.134580950019115,0.0355895166223291,
0.309620595854923));
#21151=CARTESIAN_POINT('Ctrl Pts',(0.0430789950773988,0.13237388709478,
0.317559585492229));
#21152=CARTESIAN_POINT('Ctrl Pts',(-0.0830523456774332,0.10887452531409,
0.325207149716049));
#21153=CARTESIAN_POINT('Ctrl Pts',(-0.11766079978112,0.0346657214219864,
0.330208384060767));
#21154=CARTESIAN_POINT('Ctrl Pts',(-0.117911328466355,-7.22474488887752E-5,
0.332563288526384));
#21155=CARTESIAN_POINT('Ctrl Pts',(-0.117918861549493,-6.80329776671157E-5,
0.292436711473616));
#21156=CARTESIAN_POINT('Ctrl Pts',(-0.117946256357307,-0.00405052459867665,
0.292706731931186));
#21157=CARTESIAN_POINT('Ctrl Pts',(-0.11595553950755,-0.0470512577090033,
0.295624141763016));
#21158=CARTESIAN_POINT('Ctrl Pts',(-0.0631725212350128,-0.124068972994571,
0.301188940969106));
#21159=CARTESIAN_POINT('Ctrl Pts',(0.0700327441786229,-0.12032993078169,
0.309131109091886));
#21160=CARTESIAN_POINT('Ctrl Pts',(0.139080821187468,-0.00635631000930847,
0.317073277214666));
#21161=CARTESIAN_POINT('Ctrl Pts',(0.0807165776729536,0.11344034374014,
0.325015445337446));
#21162=CARTESIAN_POINT('Ctrl Pts',(-0.0515923433190751,0.129313988454311,
0.332957613460226));
#21163=CARTESIAN_POINT('Ctrl Pts',(-0.113774867115171,0.0543021652640841,
0.338764702172283));
#21164=CARTESIAN_POINT('Ctrl Pts',(-0.117891132111753,0.00767537174388221,
0.341924401510079));
#21165=CARTESIAN_POINT('Ctrl Pts',(-0.117821685414254,0.000103165543095145,
0.342436711473616));
#21166=CARTESIAN_POINT('Origin',(0.,0.,-0.0924367114736175));
#21167=CARTESIAN_POINT('',(-0.117705188630573,0.000102098618198066,0.232563288526383));
#21168=CARTESIAN_POINT('',(-0.1176142238744,-6.23262858038681E-5,0.242436711473616));
#21169=CARTESIAN_POINT('',(-0.117775,2.85464118895969E-14,-0.0924367114736175));
#21170=CARTESIAN_POINT('Ctrl Pts',(-0.117705188630573,0.000102098618198071,
0.232563288526383));
#21171=CARTESIAN_POINT('Ctrl Pts',(-0.117475649963863,-0.0275896003179174,
0.234432088723979));
#21172=CARTESIAN_POINT('Ctrl Pts',(-0.0938913217252411,-0.0948462909608301,
0.238947218800678));
#21173=CARTESIAN_POINT('Ctrl Pts',(0.0182347644767634,-0.138007750384372,
0.246108678756477));
#21174=CARTESIAN_POINT('Ctrl Pts',(0.125841858853055,-0.0595186723796334,
0.254047668393783));
#21175=CARTESIAN_POINT('Ctrl Pts',(0.118249355954961,0.073455671106145,
0.261986658031089));
#21176=CARTESIAN_POINT('Ctrl Pts',(0.00240767183786234,0.139186381940956,
0.269925647668394));
#21177=CARTESIAN_POINT('Ctrl Pts',(-0.0995777503027144,0.0858938305448248,
0.27678452450016));
#21178=CARTESIAN_POINT('Ctrl Pts',(-0.117507442931816,0.0231998416616275,
0.280997071452822));
#21179=CARTESIAN_POINT('Ctrl Pts',(-0.117608153246896,-5.64262068778604E-5,
0.282563288526383));
#21180=CARTESIAN_POINT('Ctrl Pts',(-0.1176142238744,-6.2326285803882E-5,
0.242436711473616));
#21181=CARTESIAN_POINT('Ctrl Pts',(-0.117689148257971,-0.0156863246439697,
0.243489062352292));
#21182=CARTESIAN_POINT('Ctrl Pts',(-0.107519643382358,-0.0705218816827611,
0.247188802605229));
#21183=CARTESIAN_POINT('Ctrl Pts',(-0.024381182195918,-0.137074561658528,
0.253535932232426));
#21184=CARTESIAN_POINT('Ctrl Pts',(0.101985705091022,-0.094777599970642,
0.261478100355206));
#21185=CARTESIAN_POINT('Ctrl Pts',(0.134923209124943,0.0343453801629359,
0.269420268477986));
#21186=CARTESIAN_POINT('Ctrl Pts',(0.0442571924125319,0.132004463632409,
0.277362436600766));
#21187=CARTESIAN_POINT('Ctrl Pts',(-0.0824920331482911,0.109525057495754,
0.285034584265976));
#21188=CARTESIAN_POINT('Ctrl Pts',(-0.117677666622401,0.0349954280503056,
0.290059342556926));
#21189=CARTESIAN_POINT('Ctrl Pts',(-0.117918861549493,-6.80329776671157E-5,
0.292436711473616));
#21190=CARTESIAN_POINT('Origin',(0.,0.,-0.0924367114736175));
#21191=CARTESIAN_POINT('',(-0.117967994073432,-3.0724305424694E-6,0.182563288526383));
#21192=CARTESIAN_POINT('',(-0.117691121003631,9.91971943564221E-5,0.192436711473615));
#21193=CARTESIAN_POINT('',(-0.117775,2.85464118895969E-14,-0.0924367114736175));
#21194=CARTESIAN_POINT('Ctrl Pts',(-0.117967994073432,-3.07243054247449E-6,
0.182563288526383));
#21195=CARTESIAN_POINT('Ctrl Pts',(-0.117968057042159,-0.000167453844217198,
0.182574446236933));
#21196=CARTESIAN_POINT('Ctrl Pts',(-0.117893299674953,-0.0393189363008842,
0.185231933826584));
#21197=CARTESIAN_POINT('Ctrl Pts',(-0.0749972298318695,-0.11727771015962,
0.190535751295337));
#21198=CARTESIAN_POINT('Ctrl Pts',(0.0578663373665801,-0.126610160769685,
0.198474740932643));
#21199=CARTESIAN_POINT('Ctrl Pts',(0.13775723856723,-0.0200396862227523,
0.206413730569949));
#21200=CARTESIAN_POINT('Ctrl Pts',(0.091540828968026,0.104875747581476,
0.214352720207254));
#21201=CARTESIAN_POINT('Ctrl Pts',(-0.0384749358425138,0.133784622116252,
0.22229170984456));
#21202=CARTESIAN_POINT('Ctrl Pts',(-0.110955338697302,0.0622468391270206,
0.22836189928427));
#21203=CARTESIAN_POINT('Ctrl Pts',(-0.11780069007939,0.0116234575531164,
0.231785758844877));
#21204=CARTESIAN_POINT('Ctrl Pts',(-0.117705188630573,0.000102098618198071,
0.232563288526383));
#21205=CARTESIAN_POINT('Ctrl Pts',(-0.117691121003631,9.91971943564221E-5,
0.192436711473615));
#21206=CARTESIAN_POINT('Ctrl Pts',(-0.117474218986382,-0.0270951350261672,
0.194271392773399));
#21207=CARTESIAN_POINT('Ctrl Pts',(-0.0945676524372527,-0.0938598508209937,
0.198753463447442));
#21208=CARTESIAN_POINT('Ctrl Pts',(0.0165156171993534,-0.138242945169174,
0.205882923495746));
#21209=CARTESIAN_POINT('Ctrl Pts',(0.125131592687617,-0.061040658666823,
0.213825091618526));
#21210=CARTESIAN_POINT('Ctrl Pts',(0.119114174013628,0.0720811421096423,
0.221767259741306));
#21211=CARTESIAN_POINT('Ctrl Pts',(0.0039759348809324,0.139169211541763,
0.229709427864086));
#21212=CARTESIAN_POINT('Ctrl Pts',(-0.0990660356104632,0.0867677816679632,
0.236599245108189));
#21213=CARTESIAN_POINT('Ctrl Pts',(-0.117500661679058,0.0236188235484957,
0.240841672978032));
#21214=CARTESIAN_POINT('Ctrl Pts',(-0.1176142238744,-6.2326285803882E-5,
0.242436711473616));
#21215=CARTESIAN_POINT('Origin',(0.,0.,-0.0924367114736175));
#21216=CARTESIAN_POINT('',(-0.117696212882312,-0.000100181105204699,0.132563288526383));
#21217=CARTESIAN_POINT('',(-0.117967699956222,8.3697257429456E-6,0.142436711473616));
#21218=CARTESIAN_POINT('',(-0.117775,2.85464118895969E-14,-0.0924367114736175));
#21219=CARTESIAN_POINT('Ctrl Pts',(-0.117696212882312,-0.000100181105204706,
0.132563288526383));
#21220=CARTESIAN_POINT('Ctrl Pts',(-0.117792074781153,-0.0119544960022407,
0.133363133628988));
#21221=CARTESIAN_POINT('Ctrl Pts',(-0.110696412003459,-0.0629173266909915,
0.136809308610694));
#21222=CARTESIAN_POINT('Ctrl Pts',(-0.0373480950846616,-0.134103559412242,
0.142901813471503));
#21223=CARTESIAN_POINT('Ctrl Pts',(0.0924198687735613,-0.104101940294199,
0.150840803108809));
#21224=CARTESIAN_POINT('Ctrl Pts',(0.137583777756591,0.0211978768359354,
0.158779792746114));
#21225=CARTESIAN_POINT('Ctrl Pts',(0.0567991668878991,0.127092487218924,
0.16671878238342));
#21226=CARTESIAN_POINT('Ctrl Pts',(-0.0757945745091616,0.116657324056303,
0.174646614310176));
#21227=CARTESIAN_POINT('Ctrl Pts',(-0.117953122434976,0.0388197061692436,
0.179928116357831));
#21228=CARTESIAN_POINT('Ctrl Pts',(-0.117967994073432,-3.07243054247449E-6,
0.182563288526383));
#21229=CARTESIAN_POINT('Ctrl Pts',(-0.117967699956222,8.3697257429579E-6,
0.142436711473616));
#21230=CARTESIAN_POINT('Ctrl Pts',(-0.117928252023989,-0.038547130539091,
0.145053723194506));
#21231=CARTESIAN_POINT('Ctrl Pts',(-0.0762804946418446,-0.116178754198862,
0.150318124289656));
#21232=CARTESIAN_POINT('Ctrl Pts',(0.0559861945572589,-0.127473226882309,
0.158229914759066));
#21233=CARTESIAN_POINT('Ctrl Pts',(0.137471621702818,-0.0220324926503626,
0.166172082881846));
#21234=CARTESIAN_POINT('Ctrl Pts',(0.0930189202108026,0.103592267873211,
0.174114251004626));
#21235=CARTESIAN_POINT('Ctrl Pts',(-0.0366486683060043,0.134315868829211,
0.182056419127406));
#21236=CARTESIAN_POINT('Ctrl Pts',(-0.110544190454925,0.0633195416932908,
0.188163905950403));
#21237=CARTESIAN_POINT('Ctrl Pts',(-0.11778720200735,0.0121454601492482,
0.191624003399139));
#21238=CARTESIAN_POINT('Ctrl Pts',(-0.117691121003631,9.91971943564221E-5,
0.192436711473615));
#21239=CARTESIAN_POINT('Origin',(0.,0.,-0.0924367114736175));
#21240=CARTESIAN_POINT('',(-0.117613109409711,6.11591708146705E-5,0.0825632885263832));
#21241=CARTESIAN_POINT('',(-0.117715749944134,-0.000104199409386274,0.0924367114736155));
#21242=CARTESIAN_POINT('',(-0.117775,2.85464118895969E-14,-0.0924367114736175));
#21243=CARTESIAN_POINT('Ctrl Pts',(-0.117613109409711,6.11591708146765E-5,
0.0825632885263832));
#21244=CARTESIAN_POINT('Ctrl Pts',(-0.117502393620717,-0.0235240259785673,
0.0841518210210431));
#21245=CARTESIAN_POINT('Ctrl Pts',(-0.0991849320095013,-0.0865581493706475,
0.088386683394805));
#21246=CARTESIAN_POINT('Ctrl Pts',(0.00357853460314598,-0.139161043603659,
0.0952678756476685));
#21247=CARTESIAN_POINT('Ctrl Pts',(0.118863112008681,-0.0724583686054966,
0.103206865284975));
#21248=CARTESIAN_POINT('Ctrl Pts',(0.125336705278751,0.0605752693714656,
0.11114585492228));
#21249=CARTESIAN_POINT('Ctrl Pts',(0.0170731091066207,0.138156245709763,
0.119084844559586));
#21250=CARTESIAN_POINT('Ctrl Pts',(-0.094337657277608,0.0941904991302726,
0.126223989094287));
#21251=CARTESIAN_POINT('Ctrl Pts',(-0.11747491061231,0.0272661325996615,
0.130716803749886));
#21252=CARTESIAN_POINT('Ctrl Pts',(-0.117696212882312,-0.000100181105204706,
0.132563288526383));
#21253=CARTESIAN_POINT('Ctrl Pts',(-0.117715749944134,-0.000104199409386274,
0.0924367114736155));
#21254=CARTESIAN_POINT('Ctrl Pts',(-0.117810584636384,-0.011244028442556,
0.0931886642413524));
#21255=CARTESIAN_POINT('Ctrl Pts',(-0.111246641208053,-0.0614941526881817,
0.0965880063833492));
#21256=CARTESIAN_POINT('Ctrl Pts',(-0.0397151780004399,-0.133441281507892,
0.102634737899606));
#21257=CARTESIAN_POINT('Ctrl Pts',(0.0906220264938673,-0.105695447092796,
0.110576906022386));
#21258=CARTESIAN_POINT('Ctrl Pts',(0.137940159127448,0.0188783162799928,
0.118519074145166));
#21259=CARTESIAN_POINT('Ctrl Pts',(0.0588909273047484,0.126157580947307,
0.126461242267946));
#21260=CARTESIAN_POINT('Ctrl Pts',(-0.074108440039672,0.117863552156501,
0.134403410390726));
#21261=CARTESIAN_POINT('Ctrl Pts',(-0.117763087033452,0.0399060678969832,
0.139728566792616));
#21262=CARTESIAN_POINT('Ctrl Pts',(-0.117968157858494,0.000455912857932787,
0.142406333820246));
#21263=CARTESIAN_POINT('Ctrl Pts',(-0.117967699956222,8.3697257429579E-6,
0.142436711473616));
#21264=CARTESIAN_POINT('Origin',(0.,0.,-0.0924367114736175));
#21265=CARTESIAN_POINT('',(-0.117917485785546,7.60014832213593E-5,0.0325632885263832));
#21266=CARTESIAN_POINT('',(-0.117600989619072,5.04992496179954E-5,0.0424367114736154));
#21267=CARTESIAN_POINT('',(-0.117775,2.85464118895969E-14,-0.0924367114736175));
#21268=CARTESIAN_POINT('Ctrl Pts',(-0.117917485785546,7.60014832213644E-5,
0.0325632885263832));
#21269=CARTESIAN_POINT('Ctrl Pts',(-0.117676727567847,-0.0349830640657269,
0.0349405084130983));
#21270=CARTESIAN_POINT('Ctrl Pts',(-0.0825043195215805,-0.109517225708346,
0.0399640581789154));
#21271=CARTESIAN_POINT('Ctrl Pts',(0.0441923146003338,-0.131999388615902,
0.0476339378238343));
#21272=CARTESIAN_POINT('Ctrl Pts',(0.134874939024977,-0.034459980695041,
0.0555729274611401));
#21273=CARTESIAN_POINT('Ctrl Pts',(0.102091080224759,0.094638871230671,
0.0635119170984456));
#21274=CARTESIAN_POINT('Ctrl Pts',(-0.0241513666277066,0.137095110112719,
0.0714509067357516));
#21275=CARTESIAN_POINT('Ctrl Pts',(-0.107448046275642,0.0706698818446754,
0.0778013638783972));
#21276=CARTESIAN_POINT('Ctrl Pts',(-0.117686834607281,0.0157664388843013,
0.0815054911419412));
#21277=CARTESIAN_POINT('Ctrl Pts',(-0.117613109409711,6.11591708146765E-5,
0.0825632885263832));
#21278=CARTESIAN_POINT('Ctrl Pts',(-0.117600989619072,5.04992496179954E-5,
0.0424367114736154));
#21279=CARTESIAN_POINT('Ctrl Pts',(-0.117514779739531,-0.0227353060542692,
0.043970994662459));
#21280=CARTESIAN_POINT('Ctrl Pts',(-0.100129952091853,-0.0849605109884783,
0.0481526672255625));
#21281=CARTESIAN_POINT('Ctrl Pts',(0.000787973702835166,-0.139222729671589,
0.054981729162926));
#21282=CARTESIAN_POINT('Ctrl Pts',(0.117431922513572,-0.0747907597173192,
0.0629238972857061));
#21283=CARTESIAN_POINT('Ctrl Pts',(0.126496838785129,0.0581591461343325,
0.070866065408486));
#21284=CARTESIAN_POINT('Ctrl Pts',(0.0196773008918215,0.137828289815661,
0.0788082335312661));
#21285=CARTESIAN_POINT('Ctrl Pts',(-0.0933482651079043,0.0956446566614129,
0.085998448886309));
#21286=CARTESIAN_POINT('Ctrl Pts',(-0.11747670148927,0.0279758085988667,
0.0905412748670923));
#21287=CARTESIAN_POINT('Ctrl Pts',(-0.117715749944134,-0.000104199409386274,
0.0924367114736155));
#21288=CARTESIAN_POINT('Origin',(0.,0.,1.55));
#21289=CARTESIAN_POINT('',(-0.143211704627722,-5.70397197726547E-6,1.50700023576178));
#21290=CARTESIAN_POINT('Ctrl Pts',(-0.0334019664626774,0.112939183906323,
1.532225));
#21291=CARTESIAN_POINT('Ctrl Pts',(-0.0250606930336426,0.115799676338094,
1.53184761307169));
#21292=CARTESIAN_POINT('Ctrl Pts',(-0.0164287086124659,0.117635554524944,
1.53147359869818));
#21293=CARTESIAN_POINT('Ctrl Pts',(-0.00767226928320402,0.118510614220874,
1.53110056493424));
#21294=CARTESIAN_POINT('Ctrl Pts',(-0.0042150196872779,0.118856108509867,
1.53095328237096));
#21295=CARTESIAN_POINT('Ctrl Pts',(-0.000736351480830917,0.119051293525916,
1.53080607672538));
#21296=CARTESIAN_POINT('Ctrl Pts',(0.00274830211697625,0.119097943881266,
1.53065904037218));
#21297=CARTESIAN_POINT('Ctrl Pts',(0.00972321854123044,0.119191319684798,
1.53036473098213));
#21298=CARTESIAN_POINT('Ctrl Pts',(0.0166907125456733,0.118690968429664,
1.53007241075126));
#21299=CARTESIAN_POINT('Ctrl Pts',(0.0235721318645625,0.11762150546261,
1.52978094357425));
#21300=CARTESIAN_POINT('Ctrl Pts',(0.0273478463565568,0.117034709826966,
1.52962102062912));
#21301=CARTESIAN_POINT('Ctrl Pts',(0.0310977188904398,0.116276259986281,
1.52946135449799));
#21302=CARTESIAN_POINT('Ctrl Pts',(0.0348087249896146,0.115347945392283,
1.52930175751644));
#21303=CARTESIAN_POINT('Ctrl Pts',(0.0378768737129624,0.114580442682688,
1.52916980751093));
#21304=CARTESIAN_POINT('Ctrl Pts',(0.0409182562642153,0.113696477767379,
1.52903790896105));
#21305=CARTESIAN_POINT('Ctrl Pts',(0.0439120268522727,0.112701821307647,
1.52890655030309));
#21306=CARTESIAN_POINT('Ctrl Pts',(0.0504861734289241,0.110517613410832,
1.52861809430882));
#21307=CARTESIAN_POINT('Ctrl Pts',(0.0568477403450367,0.107796947733889,
1.528331525126));
#21308=CARTESIAN_POINT('Ctrl Pts',(0.0629211062797432,0.10455513280498,
1.52804576869741));
#21309=CARTESIAN_POINT('Ctrl Pts',(0.0667529140263229,0.102509807084265,
1.52786547926507));
#21310=CARTESIAN_POINT('Ctrl Pts',(0.0704699809867569,0.100256700264741,
1.52768551335768));
#21311=CARTESIAN_POINT('Ctrl Pts',(0.0740519796445933,0.0977963961590643,
1.52750560123222));
#21312=CARTESIAN_POINT('Ctrl Pts',(0.0761474027326905,0.0963571499395001,
1.52740035495562));
#21313=CARTESIAN_POINT('Ctrl Pts',(0.0781972522873126,0.0948464165467323,
1.52729509152825));
#21314=CARTESIAN_POINT('Ctrl Pts',(0.0801950758490376,0.0932655888959708,
1.52718986717129));
#21315=CARTESIAN_POINT('Ctrl Pts',(0.0872135629190184,0.0877120362002772,
1.52682020700562));
#21316=CARTESIAN_POINT('Ctrl Pts',(0.0935342345834078,0.0813437113039547,
1.52645409167081));
#21317=CARTESIAN_POINT('Ctrl Pts',(0.0991216768718319,0.0743433873765979,
1.52608928877518));
#21318=CARTESIAN_POINT('Ctrl Pts',(0.101857856375295,0.0709153174549959,
1.52591064420861));
#21319=CARTESIAN_POINT('Ctrl Pts',(0.104417791592617,0.0673349702414553,
1.52573231437502));
#21320=CARTESIAN_POINT('Ctrl Pts',(0.106794530290299,0.0636205708890664,
1.52555403711528));
#21321=CARTESIAN_POINT('Ctrl Pts',(0.108394385735532,0.0611202951812291,
1.52543403324399));
#21322=CARTESIAN_POINT('Ctrl Pts',(0.109912312880749,0.0585571637778213,
1.52531395827658));
#21323=CARTESIAN_POINT('Ctrl Pts',(0.111341951189028,0.0559432008961949,
1.5251940432238));
#21324=CARTESIAN_POINT('Ctrl Pts',(0.115894033640165,0.0476201345006791,
1.52481222412716));
#21325=CARTESIAN_POINT('Ctrl Pts',(0.119530893641226,0.0388304356906876,
1.52443409356659));
#21326=CARTESIAN_POINT('Ctrl Pts',(0.122195159250079,0.0297595052710396,
1.52405718851832));
#21327=CARTESIAN_POINT('Ctrl Pts',(0.123464283518865,0.0254385629829291,
1.52387764960816));
#21328=CARTESIAN_POINT('Ctrl Pts',(0.124512110981915,0.0210533134598664,
1.52369838877875));
#21329=CARTESIAN_POINT('Ctrl Pts',(0.12532867129748,0.0166220814218575,
1.52351913980531));
#21330=CARTESIAN_POINT('Ctrl Pts',(0.126067828800149,0.012610891624201,
1.52335688207487));
#21331=CARTESIAN_POINT('Ctrl Pts',(0.12661735951473,0.00855739899605222,
1.52319445303817));
#21332=CARTESIAN_POINT('Ctrl Pts',(0.126966826155483,0.00450415768051923,
1.52303280899981));
#21333=CARTESIAN_POINT('Ctrl Pts',(0.127602972227412,-0.00287409603749457,
1.52273856283131));
#21334=CARTESIAN_POINT('Ctrl Pts',(0.12758177643555,-0.010267620141741,
1.52244625042084));
#21335=CARTESIAN_POINT('Ctrl Pts',(0.126865581413421,-0.0175939782534482,
1.52215473434257));
#21336=CARTESIAN_POINT('Ctrl Pts',(0.126426462283551,-0.0220859726121444,
1.52197599770985));
#21337=CARTESIAN_POINT('Ctrl Pts',(0.12572570473317,-0.0265528301690258,
1.52179756043894));
#21338=CARTESIAN_POINT('Ctrl Pts',(0.124776542651163,-0.0309793260681717,
1.52161916036391));
#21339=CARTESIAN_POINT('Ctrl Pts',(0.124151644840291,-0.0338935887106027,
1.52150170748789));
#21340=CARTESIAN_POINT('Ctrl Pts',(0.123418330834614,-0.0367926408403149,
1.52138417707714));
#21341=CARTESIAN_POINT('Ctrl Pts',(0.122581975874549,-0.0396644408336013,
1.52126680258073));
#21342=CARTESIAN_POINT('Ctrl Pts',(0.120074191833131,-0.0482754427851461,
1.52091485884509));
#21343=CARTESIAN_POINT('Ctrl Pts',(0.116656903439717,-0.0566007293654626,
1.52056600333313));
#21344=CARTESIAN_POINT('Ctrl Pts',(0.112443760417108,-0.0645262187619275,
1.52021830866717));
#21345=CARTESIAN_POINT('Ctrl Pts',(0.109356904590302,-0.0703330102694749,
1.51996356219884));
#21346=CARTESIAN_POINT('Ctrl Pts',(0.105841781173658,-0.0759253337267248,
1.51970943888381));
#21347=CARTESIAN_POINT('Ctrl Pts',(0.101930367117466,-0.0812537151913617,
1.51945518067311));
#21348=CARTESIAN_POINT('Ctrl Pts',(0.100130771446666,-0.0837052409256295,
1.51933819945644));
#21349=CARTESIAN_POINT('Ctrl Pts',(0.0982476276828181,-0.0860996963839449,
1.51922123442864));
#21350=CARTESIAN_POINT('Ctrl Pts',(0.0962924325256194,-0.0884227179472683,
1.51910469697823));
#21351=CARTESIAN_POINT('Ctrl Pts',(0.0906946176521128,-0.0950736369671782,
1.51877104482549));
#21352=CARTESIAN_POINT('Ctrl Pts',(0.0844921899154374,-0.101162815315101,
1.51843983772287));
#21353=CARTESIAN_POINT('Ctrl Pts',(0.0777644521522082,-0.106582693579069,
1.51810941878));
#21354=CARTESIAN_POINT('Ctrl Pts',(0.0731067700043679,-0.110334931124879,
1.5178806663426));
#21355=CARTESIAN_POINT('Ctrl Pts',(0.0681966627772886,-0.113766151308436,
1.51765229166508));
#21356=CARTESIAN_POINT('Ctrl Pts',(0.0630541948599911,-0.116833686038022,
1.5174237449583));
#21357=CARTESIAN_POINT('Ctrl Pts',(0.0607686815400033,-0.118197018118406,
1.51732216988754));
#21358=CARTESIAN_POINT('Ctrl Pts',(0.0584414404741937,-0.119485783651375,
1.51722075040181));
#21359=CARTESIAN_POINT('Ctrl Pts',(0.0560784264268894,-0.12069488199044,
1.51711960151386));
#21360=CARTESIAN_POINT('Ctrl Pts',(0.0475595529450054,-0.125053787850271,
1.51675495087613));
#21361=CARTESIAN_POINT('Ctrl Pts',(0.038563113830939,-0.128389854466075,
1.51639315730301));
#21362=CARTESIAN_POINT('Ctrl Pts',(0.0292711048986314,-0.130741856378471,
1.51603205677802));
#21363=CARTESIAN_POINT('Ctrl Pts',(0.0254547302664753,-0.13170786066222,
1.51588374709674));
#21364=CARTESIAN_POINT('Ctrl Pts',(0.0215881861914954,-0.132507324978224,
1.51573555432397));
#21365=CARTESIAN_POINT('Ctrl Pts',(0.0176832233642019,-0.13314066674995,
1.51558732853105));
#21366=CARTESIAN_POINT('Ctrl Pts',(0.0144414794405867,-0.133666441752394,
1.51546427740745));
#21367=CARTESIAN_POINT('Ctrl Pts',(0.0111713231872828,-0.134077605234841,
1.5153411329761));
#21368=CARTESIAN_POINT('Ctrl Pts',(0.00789687394913892,-0.134372952697723,
1.51521845803943));
#21369=CARTESIAN_POINT('Ctrl Pts',(-0.00208492598009478,-0.135273287095873,
1.51484449692866));
#21370=CARTESIAN_POINT('Ctrl Pts',(-0.0121386692885745,-0.135107999768821,
1.51447364169918));
#21371=CARTESIAN_POINT('Ctrl Pts',(-0.0220717676774029,-0.133899092645375,
1.51410356562093));
#21372=CARTESIAN_POINT('Ctrl Pts',(-0.0271373055616968,-0.133282591671289,
1.51391483957382));
#21373=CARTESIAN_POINT('Ctrl Pts',(-0.0321716696217597,-0.132393849601707,
1.51372631615657));
#21374=CARTESIAN_POINT('Ctrl Pts',(-0.0371491047637803,-0.131230566976147,
1.51353768678866));
#21375=CARTESIAN_POINT('Ctrl Pts',(-0.0401763453142056,-0.130523066780721,
1.51342296375255));
#21376=CARTESIAN_POINT('Ctrl Pts',(-0.0431793745847511,-0.129714439573166,
1.51330831773957));
#21377=CARTESIAN_POINT('Ctrl Pts',(-0.0461427198170546,-0.128807808452418,
1.51319405707679));
#21378=CARTESIAN_POINT('Ctrl Pts',(-0.0557912886485991,-0.125855842991896,
1.51282202756853));
#21379=CARTESIAN_POINT('Ctrl Pts',(-0.0650506639775802,-0.121862017750276,
1.51245293010828));
#21380=CARTESIAN_POINT('Ctrl Pts',(-0.0737251756215706,-0.116823260910032,
1.51208446868514));
#21381=CARTESIAN_POINT('Ctrl Pts',(-0.0774533877539874,-0.114657657224767,
1.51192610791459));
#21382=CARTESIAN_POINT('Ctrl Pts',(-0.0810733781510443,-0.112298364258586,
1.51176786463208));
#21383=CARTESIAN_POINT('Ctrl Pts',(-0.0845783705992567,-0.109758519633299,
1.51160955655689));
#21384=CARTESIAN_POINT('Ctrl Pts',(-0.0871260289206952,-0.107912394030924,
1.51149448786814));
#21385=CARTESIAN_POINT('Ctrl Pts',(-0.0896122610481647,-0.105970921032248,
1.51137940572563));
#21386=CARTESIAN_POINT('Ctrl Pts',(-0.0920243025666997,-0.10394826075131,
1.51126473391974));
#21387=CARTESIAN_POINT('Ctrl Pts',(-0.0995315444015674,-0.0976529296958118,
1.51090782920982));
#21388=CARTESIAN_POINT('Ctrl Pts',(-0.106349817996106,-0.090554906599088,
1.51055366538392));
#21389=CARTESIAN_POINT('Ctrl Pts',(-0.112409916721278,-0.0828189535999138,
1.51020021897155));
#21390=CARTESIAN_POINT('Ctrl Pts',(-0.11567060314877,-0.0786565598680515,
1.51001004419521));
#21391=CARTESIAN_POINT('Ctrl Pts',(-0.118711357121208,-0.0743087544864998,
1.50982007711492));
#21392=CARTESIAN_POINT('Ctrl Pts',(-0.121517490738653,-0.0697974244982526,
1.50963000253165));
#21393=CARTESIAN_POINT('Ctrl Pts',(-0.123184827969132,-0.0671169005197731,
1.50951706477726));
#21394=CARTESIAN_POINT('Ctrl Pts',(-0.124768226583796,-0.064379797453554,
1.50940414472167));
#21395=CARTESIAN_POINT('Ctrl Pts',(-0.12625918933752,-0.0616017405091787,
1.50929161182319));
#21396=CARTESIAN_POINT('Ctrl Pts',(-0.131254477666307,-0.0522942005345653,
1.50891458411209));
#21397=CARTESIAN_POINT('Ctrl Pts',(-0.135235816373665,-0.0424980109473837,
1.50854057440173));
#21398=CARTESIAN_POINT('Ctrl Pts',(-0.138100316247284,-0.0323932585971084,
1.50816719719795));
#21399=CARTESIAN_POINT('Ctrl Pts',(-0.139428601593765,-0.027707625827389,
1.5079940600046));
#21400=CARTESIAN_POINT('Ctrl Pts',(-0.140516076092011,-0.0229552175461711,
1.50782105881478));
#21401=CARTESIAN_POINT('Ctrl Pts',(-0.14134846970832,-0.01815262603916,
1.50764795577689));
#21402=CARTESIAN_POINT('Ctrl Pts',(-0.141840021659925,-0.0153165600461233,
1.5075457335416));
#21403=CARTESIAN_POINT('Ctrl Pts',(-0.142241997144177,-0.0124651428186592,
1.50744355431084));
#21404=CARTESIAN_POINT('Ctrl Pts',(-0.142550993842162,-0.00961078035088443,
1.50734168592779));
#21405=CARTESIAN_POINT('Ctrl Pts',(-0.142847161918882,-0.00687492249914849,
1.50724404681617));
#21406=CARTESIAN_POINT('Ctrl Pts',(-0.143058332724879,-0.00413406598225375,
1.5071466105924));
#21407=CARTESIAN_POINT('Ctrl Pts',(-0.143182669649515,-0.00139134585336764,
1.50704933585643));
#21408=CARTESIAN_POINT('Ctrl Pts',(-0.143203595382121,-0.00092974984559876,
1.50703296465278));
#21409=CARTESIAN_POINT('Ctrl Pts',(-0.143222061023464,-0.000468100854706259,
1.50701659802318));
#21410=CARTESIAN_POINT('Ctrl Pts',(-0.143238079070951,-6.41379011939899E-6,
1.50700023577028));
#21411=CARTESIAN_POINT('',(-0.00156744678985144,0.146109855568756,1.50365));
#21412=CARTESIAN_POINT('Ctrl Pts',(-0.00156962371672063,0.146072546381438,
1.50365));
#21413=CARTESIAN_POINT('Ctrl Pts',(-0.011711474284147,0.144648739717271,
1.50495065132295));
#21414=CARTESIAN_POINT('Ctrl Pts',(-0.0216501921041044,0.142222471223284,
1.50626105010813));
#21415=CARTESIAN_POINT('Ctrl Pts',(-0.0312062965385204,0.138804788898175,
1.50759029209282));
#21416=CARTESIAN_POINT('Ctrl Pts',(-0.0379863325344082,0.136379950477271,
1.50853338648503));
#21417=CARTESIAN_POINT('Ctrl Pts',(-0.0445735484268955,0.133455002060128,
1.5094859663039));
#21418=CARTESIAN_POINT('Ctrl Pts',(-0.0508923708069948,0.130021662144985,
1.51045128011208));
#21419=CARTESIAN_POINT('Ctrl Pts',(-0.053607485163773,0.128546401418451,
1.51086606268101));
#21420=CARTESIAN_POINT('Ctrl Pts',(-0.0562647183424556,0.126981576978965,
1.51128195276517));
#21421=CARTESIAN_POINT('Ctrl Pts',(-0.0588579379029418,0.125328026221608,
1.51169910067666));
#21422=CARTESIAN_POINT('Ctrl Pts',(-0.0624505046767585,0.123037247762191,
1.51227700458785));
#21423=CARTESIAN_POINT('Ctrl Pts',(-0.0659209207101175,0.120575889029892,
1.51285741907924));
#21424=CARTESIAN_POINT('Ctrl Pts',(-0.0692542752175272,0.117943487410649,
1.51344114883776));
#21425=CARTESIAN_POINT('Ctrl Pts',(-0.0735613784355843,0.114542101371374,
1.51419539934302));
#21426=CARTESIAN_POINT('Ctrl Pts',(-0.0776398170223455,0.110855132244726,
1.51495518495604));
#21427=CARTESIAN_POINT('Ctrl Pts',(-0.0814741368103916,0.106911749311875,
1.51572224163114));
#21428=CARTESIAN_POINT('Ctrl Pts',(-0.0845038784997064,0.103795829845314,
1.51632834224744));
#21429=CARTESIAN_POINT('Ctrl Pts',(-0.087381117690253,0.10051973853988,
1.51693898261853));
#21430=CARTESIAN_POINT('Ctrl Pts',(-0.0900959757046659,0.0970973798321736,
1.51755501917095));
#21431=CARTESIAN_POINT('Ctrl Pts',(-0.0920052356275281,0.0946905606587243,
1.51798825505079));
#21432=CARTESIAN_POINT('Ctrl Pts',(-0.093830595110286,0.092215607777745,
1.51842338946406));
#21433=CARTESIAN_POINT('Ctrl Pts',(-0.0955653742165971,0.0896840982544811,
1.51885969689116));
#21434=CARTESIAN_POINT('Ctrl Pts',(-0.0997851775729162,0.0835262696618028,
1.51992100293214));
#21435=CARTESIAN_POINT('Ctrl Pts',(-0.103479134251024,0.0770231540939269,
1.52099120961793));
#21436=CARTESIAN_POINT('Ctrl Pts',(-0.106606394578922,0.0702509006766953,
1.52207541818308));
#21437=CARTESIAN_POINT('Ctrl Pts',(-0.108879606303698,0.0653281362576702,
1.52286353153598));
#21438=CARTESIAN_POINT('Ctrl Pts',(-0.110852991156964,0.0602629640702717,
1.52365904329275));
#21439=CARTESIAN_POINT('Ctrl Pts',(-0.112503888351057,0.0550849881514033,
1.524463912762));
#21440=CARTESIAN_POINT('Ctrl Pts',(-0.113450017754745,0.0521174894567802,
1.52492518356294));
#21441=CARTESIAN_POINT('Ctrl Pts',(-0.114289979676541,0.0491121240008169,
1.52538965304266));
#21442=CARTESIAN_POINT('Ctrl Pts',(-0.115015874151616,0.0460903162170444,
1.52585530945224));
#21443=CARTESIAN_POINT('Ctrl Pts',(-0.117053612444637,0.0376074669234184,
1.52716250482259));
#21444=CARTESIAN_POINT('Ctrl Pts',(-0.118206139871793,0.0289652499882669,
1.52848357355921));
#21445=CARTESIAN_POINT('Ctrl Pts',(-0.11838625730212,0.0202925750432425,
1.52982832573377));
#21446=CARTESIAN_POINT('Ctrl Pts',(-0.118492077855379,0.015197303257165,
1.53061837930521));
#21447=CARTESIAN_POINT('Ctrl Pts',(-0.118261361656021,0.0100916471271278,
1.53141660760476));
#21448=CARTESIAN_POINT('Ctrl Pts',(-0.11766859746431,0.00500517689818842,
1.532225));
#21449=CARTESIAN_POINT('',(-0.115079981391543,0.0902137050004572,1.50365));
#21450=CARTESIAN_POINT('Origin',(0.,0.,1.50365));
#21451=CARTESIAN_POINT('Ctrl Pts',(-0.143238079070951,-6.41379011939899E-6,
1.50700023577028));
#21452=CARTESIAN_POINT('Ctrl Pts',(-0.143514357617001,0.00795674345750163,
1.50671802038504));
#21453=CARTESIAN_POINT('Ctrl Pts',(-0.14306421847979,0.0159310909218757,
1.50643710681857));
#21454=CARTESIAN_POINT('Ctrl Pts',(-0.141940608246003,0.023841490005315,
1.50615648267927));
#21455=CARTESIAN_POINT('Ctrl Pts',(-0.141317731836386,0.0282266413964,1.50600091791928));
#21456=CARTESIAN_POINT('Ctrl Pts',(-0.14048752132733,0.0325921818867556,
1.50584544210227));
#21457=CARTESIAN_POINT('Ctrl Pts',(-0.139456452513291,0.0369250818702156,
1.5056898827608));
#21458=CARTESIAN_POINT('Ctrl Pts',(-0.138790989895207,0.0397215809279161,
1.50558948313156));
#21459=CARTESIAN_POINT('Ctrl Pts',(-0.138042009924554,0.0425029011667524,
1.50548910366784));
#21460=CARTESIAN_POINT('Ctrl Pts',(-0.137214434473447,0.0452564915355094,
1.50538902890071));
#21461=CARTESIAN_POINT('Ctrl Pts',(-0.134176751889031,0.0553637675507716,
1.50502169637912));
#21462=CARTESIAN_POINT('Ctrl Pts',(-0.130076454936343,0.0651325632434767,
1.50465723703036));
#21463=CARTESIAN_POINT('Ctrl Pts',(-0.125018127980614,0.0743940890034878,
1.50429344851366));
#21464=CARTESIAN_POINT('Ctrl Pts',(-0.122034683484208,0.0798566160996726,
1.50407888293545));
#21465=CARTESIAN_POINT('Ctrl Pts',(-0.118716925567465,0.0851425936725427,
1.50386455072235));
#21466=CARTESIAN_POINT('Ctrl Pts',(-0.115078604842436,0.0902138214954005,
1.50365));
#21467=CARTESIAN_POINT('',(-0.05,-6.12323399573677E-18,1.6));
#21468=CARTESIAN_POINT('',(-0.1,-1.22464679914735E-17,1.55));
#21469=CARTESIAN_POINT('Origin',(0.,0.,1.6));
#21470=CARTESIAN_POINT('Ctrl Pts',(0.0850780204044575,-0.11908002747757,
-0.0164977839420936));
#21471=CARTESIAN_POINT('Ctrl Pts',(0.124677800165771,-0.0907875342533835,
-0.0138514540629917));
#21472=CARTESIAN_POINT('Ctrl Pts',(0.172751483861701,0.00791416360185712,
-0.00855879430478784));
#21473=CARTESIAN_POINT('Ctrl Pts',(0.0868617128612901,0.149726167188418,
-0.000619804667482127));
#21474=CARTESIAN_POINT('Ctrl Pts',(-0.078614020905812,0.154028602276276,
0.00731918496982359));
#21475=CARTESIAN_POINT('Ctrl Pts',(-0.172087192378165,0.0175525219725009,
0.0152581746071293));
#21476=CARTESIAN_POINT('Ctrl Pts',(-0.108045720411827,-0.135108484733225,
0.0231971642444351));
#21477=CARTESIAN_POINT('Ctrl Pts',(0.0549144151285058,-0.164025561655164,
0.0311361538817407));
#21478=CARTESIAN_POINT('Ctrl Pts',(0.167598788591005,-0.0428207868793744,
0.0390751435190465));
#21479=CARTESIAN_POINT('Ctrl Pts',(0.126860790413016,0.117600499296196,
0.0470141331563521));
#21480=CARTESIAN_POINT('Ctrl Pts',(-0.0300110592737492,0.170357625684536,
0.054953122793658));
#21481=CARTESIAN_POINT('Ctrl Pts',(-0.159409054995301,0.0671687418111174,
0.0628921124309635));
#21482=CARTESIAN_POINT('Ctrl Pts',(-0.142879399887002,-0.0975110083167992,
0.0708311020682695));
#21483=CARTESIAN_POINT('Ctrl Pts',(0.00444677171871267,-0.172924803493063,
0.078770091705575));
#21484=CARTESIAN_POINT('Ctrl Pts',(0.147702113712341,-0.0900384822365835,
0.0867090813428809));
#21485=CARTESIAN_POINT('Ctrl Pts',(0.155746353789385,0.0752722621313087,
0.0946480709801864));
#21486=CARTESIAN_POINT('Ctrl Pts',(0.021215449100004,0.17167621786987,0.102587060617492));
#21487=CARTESIAN_POINT('Ctrl Pts',(-0.132736728465598,0.110922462699857,
0.110526050254798));
#21488=CARTESIAN_POINT('Ctrl Pts',(-0.165177537004225,-0.0513732581591355,
0.118465039892104));
#21489=CARTESIAN_POINT('Ctrl Pts',(-0.0464096261145344,-0.166640254043574,
0.126404029529409));
#21490=CARTESIAN_POINT('Ctrl Pts',(0.114843114370719,-0.129359532685675,
0.134343019166715));
#21491=CARTESIAN_POINT('Ctrl Pts',(0.170964855654229,0.0263409830179588,
0.142282008804021));
#21492=CARTESIAN_POINT('Ctrl Pts',(0.0705799878925336,0.157928129946847,
0.150220998441327));
#21493=CARTESIAN_POINT('Ctrl Pts',(-0.0944160212638482,0.144942899583874,
0.158159988078632));
#21494=CARTESIAN_POINT('Ctrl Pts',(-0.172980633894512,-0.000727622896455919,
0.166098977715938));
#21495=CARTESIAN_POINT('Ctrl Pts',(-0.0931933312323777,-0.145732055885043,
0.174037967353244));
#21496=CARTESIAN_POINT('Ctrl Pts',(0.0719060791645076,-0.157328779695546,
0.181976956990549));
#21497=CARTESIAN_POINT('Ctrl Pts',(0.171180402159323,-0.0249017879745179,
0.189915946627855));
#21498=CARTESIAN_POINT('Ctrl Pts',(0.113750798721884,0.13032108391891,0.197854936265161));
#21499=CARTESIAN_POINT('Ctrl Pts',(-0.0478098650864174,0.16624393501773,
0.205793925902467));
#21500=CARTESIAN_POINT('Ctrl Pts',(-0.16560387403618,0.0499818570245514,
0.213732915539772));
#21501=CARTESIAN_POINT('Ctrl Pts',(-0.131798885878402,-0.112035185581475,
0.221671905177078));
#21502=CARTESIAN_POINT('Ctrl Pts',(0.0226589495323734,-0.171491694067101,
0.229610894814384));
#21503=CARTESIAN_POINT('Ctrl Pts',(0.156374069566079,-0.073959309724122,
0.237549884451689));
#21504=CARTESIAN_POINT('Ctrl Pts',(0.146939445926624,0.0912777539068999,
0.245488874088995));
#21505=CARTESIAN_POINT('Ctrl Pts',(0.00299182995941577,0.172956289510158,
0.253427863726301));
#21506=CARTESIAN_POINT('Ctrl Pts',(-0.143694601292225,0.0963051955349955,
0.261366853363607));
#21507=CARTESIAN_POINT('Ctrl Pts',(-0.15883847309497,-0.0685067047260848,
0.269305843000912));
#21508=CARTESIAN_POINT('Ctrl Pts',(-0.0285766086907934,-0.170605411881679,
0.277244832638218));
#21509=CARTESIAN_POINT('Ctrl Pts',(0.12784518248692,-0.116526556812001,
0.285183822275524));
#21510=CARTESIAN_POINT('Ctrl Pts',(0.167233470900423,0.0442243749325307,
0.293122811912829));
#21511=CARTESIAN_POINT('Ctrl Pts',(0.0535309779628647,0.164490922320707,
0.301061801550136));
#21512=CARTESIAN_POINT('Ctrl Pts',(-0.109175456582181,0.134177303623408,
0.309000791187441));
#21513=CARTESIAN_POINT('Ctrl Pts',(-0.171939242908932,-0.0189664407699395,
0.316939780824747));
#21514=CARTESIAN_POINT('Ctrl Pts',(-0.0773044361184472,-0.154747708493488,
0.324878770462053));
#21515=CARTESIAN_POINT('Ctrl Pts',(0.0880972839194656,-0.148868054644337,
0.332817760099358));
#21516=CARTESIAN_POINT('Ctrl Pts',(0.172851978230285,-0.00670989936239309,
0.340756749736664));
#21517=CARTESIAN_POINT('Ctrl Pts',(0.0993725327910066,0.141590708926387,
0.34869573937397));
#21518=CARTESIAN_POINT('Ctrl Pts',(-0.0650756559739905,0.160274727038081,
0.356634729011275));
#21519=CARTESIAN_POINT('Ctrl Pts',(-0.169951541620772,0.0322382168908211,
0.364573718648582));
#21520=CARTESIAN_POINT('Ctrl Pts',(-0.119248438453561,-0.125310171390688,
0.372512708285886));
#21521=CARTESIAN_POINT('Ctrl Pts',(0.0406184374886585,-0.168145685830938,
0.380451697923193));
#21522=CARTESIAN_POINT('Ctrl Pts',(0.163301917673335,-0.0570553486694088,
0.388390687560498));
#21523=CARTESIAN_POINT('Ctrl Pts',(0.136493684039406,0.106265249940549,
0.396329677197804));
#21524=CARTESIAN_POINT('Ctrl Pts',(-0.0152651628095069,0.172307295063139,
0.404268666835109));
#21525=CARTESIAN_POINT('Ctrl Pts',(-0.153049799296248,0.0806138205455782,
0.412207656472416));
#21526=CARTESIAN_POINT('Ctrl Pts',(-0.150727833715048,-0.0848760818555219,
0.420146646109721));
#21527=CARTESIAN_POINT('Ctrl Pts',(-0.0104248664208018,-0.172667748255674,
0.428085635747027));
#21528=CARTESIAN_POINT('Ctrl Pts',(0.139421351618932,-0.10239392482138,
0.436024625384332));
#21529=CARTESIAN_POINT('Ctrl Pts',(0.16163687742079,0.0616145192729195,
0.443963615021638));
#21530=CARTESIAN_POINT('Ctrl Pts',(0.0358849196425865,0.169219093691645,
0.451902604658944));
#21531=CARTESIAN_POINT('Ctrl Pts',(-0.122717222714247,0.121915185177559,
0.45984159429625));
#21532=CARTESIAN_POINT('Ctrl Pts',(-0.168980158036723,-0.0369937199732681,
0.467780583933555));
#21533=CARTESIAN_POINT('Ctrl Pts',(-0.0605533396431397,-0.162037409833775,
0.475719573570861));
#21534=CARTESIAN_POINT('Ctrl Pts',(0.103305911202344,-0.138746956140414,
0.483658563208167));
#21535=CARTESIAN_POINT('Ctrl Pts',(0.172595680358559,0.0115568269495825,
0.491597552845473));
#21536=CARTESIAN_POINT('Ctrl Pts',(0.0838859329010004,0.151281127008313,
0.499536542482778));
#21537=CARTESIAN_POINT('Ctrl Pts',(-0.0816156370489812,0.152517923263679,
0.507475532120084));
#21538=CARTESIAN_POINT('Ctrl Pts',(-0.172403684765527,0.0141350135070757,
0.51541452175739));
#21539=CARTESIAN_POINT('Ctrl Pts',(-0.105367974675403,-0.137187532379513,
0.523353511394695));
#21540=CARTESIAN_POINT('Ctrl Pts',(0.0581248948911363,-0.162924294448283,
0.531292501032001));
#21541=CARTESIAN_POINT('Ctrl Pts',(0.168408406744046,-0.039515030880773,
0.539231490669306));
#21542=CARTESIAN_POINT('Ctrl Pts',(0.124525564004667,0.120067535316156,
0.547170480306613));
#21543=CARTESIAN_POINT('Ctrl Pts',(-0.0333518982867267,0.169736501696743,
0.555109469943918));
#21544=CARTESIAN_POINT('Ctrl Pts',(-0.160697983451488,0.0640233335761385,
0.563048459581225));
#21545=CARTESIAN_POINT('Ctrl Pts',(-0.14093607811848,-0.100298808627811,
0.570987449218529));
#21546=CARTESIAN_POINT('Ctrl Pts',(0.00784314775175556,-0.172804265459278,
0.578926438855836));
#21547=CARTESIAN_POINT('Ctrl Pts',(0.149442509381278,-0.0871192603125336,
0.586865428493141));
#21548=CARTESIAN_POINT('Ctrl Pts',(0.154237495636292,0.0783174569774929,
0.594804418130446));
#21549=CARTESIAN_POINT('Ctrl Pts',(0.0178386252221998,0.172059909850489,
0.602743407767753));
#21550=CARTESIAN_POINT('Ctrl Pts',(-0.134890284021987,0.108293307291099,
0.610682397405058));
#21551=CARTESIAN_POINT('Ctrl Pts',(-0.164136382878957,-0.0546083962682395,
0.618621387042364));
#21552=CARTESIAN_POINT('Ctrl Pts',(-0.0431268722112106,-0.167519855601819,
0.62656037667967));
#21553=CARTESIAN_POINT('Ctrl Pts',(0.117362334288317,-0.127078368017432,
0.634499366316975));
#21554=CARTESIAN_POINT('Ctrl Pts',(0.170414367112955,0.0296946562375699,
0.642438355954282));
#21555=CARTESIAN_POINT('Ctrl Pts',(0.0674637261050104,0.159284257814778,
0.650377345591586));
#21556=CARTESIAN_POINT('Ctrl Pts',(-0.0972453325609638,0.143060037825677,
0.658316335228894));
#21557=CARTESIAN_POINT('Ctrl Pts',(-0.172932953925271,-0.00412584224812367,
0.666255324866198));
#21558=CARTESIAN_POINT('Ctrl Pts',(-0.0903123078403481,-0.147534796506203,
0.674194314503505));
#21559=CARTESIAN_POINT('Ctrl Pts',(0.0749830665657334,-0.155885755782802,
0.68213330414081));
#21560=CARTESIAN_POINT('Ctrl Pts',(0.17163658245605,-0.021533989188811,
0.690072293778116));
#21561=CARTESIAN_POINT('Ctrl Pts',(0.11116857013107,0.132530668686874,0.698011283415421));
#21562=CARTESIAN_POINT('Ctrl Pts',(-0.0510666492692211,0.165272582299639,
0.705950273052727));
#21563=CARTESIAN_POINT('Ctrl Pts',(-0.166553851089581,0.0467187736868841,
0.713889262690032));
#21564=CARTESIAN_POINT('Ctrl Pts',(-0.129572416918314,-0.114602870389546,
0.721828252327339));
#21565=CARTESIAN_POINT('Ctrl Pts',(0.0260236847639906,-0.171013440871999,
0.729767241964644));
#21566=CARTESIAN_POINT('Ctrl Pts',(0.157796886564457,-0.0708729265526718,
0.73770623160195));
#21567=CARTESIAN_POINT('Ctrl Pts',(0.145117853242075,0.0941468947867542,
0.745645221239255));
#21568=CARTESIAN_POINT('Ctrl Pts',(-0.000406629147419015,0.172981686256994,
0.753584210876562));
#21569=CARTESIAN_POINT('Ctrl Pts',(-0.145558870420566,0.0934635991681543,
0.761523200513868));
#21570=CARTESIAN_POINT('Ctrl Pts',(-0.157461941624574,-0.0716140074803496,
0.769462190151172));
#21571=CARTESIAN_POINT('Ctrl Pts',(-0.0252193968429213,-0.17113389830906,
0.777401179788479));
#21572=CARTESIAN_POINT('Ctrl Pts',(0.130109777350283,-0.113992433807847,
0.785340169425784));
#21573=CARTESIAN_POINT('Ctrl Pts',(0.166332367384696,0.0475012914327479,
0.793279159063091));
#21574=CARTESIAN_POINT('Ctrl Pts',(0.0502890745800368,0.165510839842773,
0.801218148700395));
#21575=CARTESIAN_POINT('Ctrl Pts',(-0.111790419467279,0.132006557575396,
0.809157138337702));
#21576=CARTESIAN_POINT('Ctrl Pts',(-0.171533445990104,-0.0223406811520247,
0.817096127975007));
#21577=CARTESIAN_POINT('Ctrl Pts',(-0.0742493586638003,-0.156236557391639,
0.825035117612313));
#21578=CARTESIAN_POINT('Ctrl Pts',(0.0910049278783345,-0.147108572929777,
0.832974107249618));
#21579=CARTESIAN_POINT('Ctrl Pts',(0.172950439922886,-0.00331277195964383,
0.840913096886925));
#21580=CARTESIAN_POINT('Ctrl Pts',(0.0965716772857839,0.143515644700454,
0.848852086524229));
#21581=CARTESIAN_POINT('Ctrl Pts',(-0.0682118374171683,0.158965324406771,
0.856791076161536));
#21582=CARTESIAN_POINT('Ctrl Pts',(-0.170552089827228,0.0288931442238776,
0.864730065798841));
#21583=CARTESIAN_POINT('Ctrl Pts',(-0.116763592698541,-0.127628729319482,
0.872669055436147));
#21584=CARTESIAN_POINT('Ctrl Pts',(0.0439139712140358,-0.167315248138923,
0.880608045073453));
#21585=CARTESIAN_POINT('Ctrl Pts',(0.164391304101163,-0.0538361241500125,
0.888547034710759));
#21586=CARTESIAN_POINT('Ctrl Pts',(0.134379664555536,0.108926281867684,
0.896486024348063));
#21587=CARTESIAN_POINT('Ctrl Pts',(-0.018647348250808,0.17197414204115,
0.904425013985371));
#21588=CARTESIAN_POINT('Ctrl Pts',(-0.154603991719776,0.0775914613336281,
0.912364003622676));
#21589=CARTESIAN_POINT('Ctrl Pts',(-0.149031276472826,-0.0878208845346985,
0.920302993259982));
#21590=CARTESIAN_POINT('Ctrl Pts',(-0.00703064139541984,-0.172839229369798,
0.928241982897287));
#21591=CARTESIAN_POINT('Ctrl Pts',(0.141406064038169,-0.099635105162837,
0.936180972534593));
#21592=CARTESIAN_POINT('Ctrl Pts',(0.160395209035295,0.064778129380991,
0.944119962171899));
#21593=CARTESIAN_POINT('Ctrl Pts',(0.03255353276219,0.169891426011666,0.952058951809204));
#21594=CARTESIAN_POINT('Ctrl Pts',(-0.125088671715395,0.119480765548496,
0.959997941446511));
#21595=CARTESIAN_POINT('Ctrl Pts',(-0.168220770124088,-0.040306347222682,
0.967936931083815));
#21596=CARTESIAN_POINT('Ctrl Pts',(-0.0573582824064844,-0.163195761485875,
0.975875920721122));
#21597=CARTESIAN_POINT('Ctrl Pts',(0.106011781834435,-0.136690640644722,
0.983814910358427));
#21598=CARTESIAN_POINT('Ctrl Pts',(0.17233532526783,0.014945393685262,0.991753899995733));
#21599=CARTESIAN_POINT('Ctrl Pts',(0.0808976893297158,0.152899944371113,
0.999692889633039));
#21600=CARTESIAN_POINT('Ctrl Pts',(-0.0845962369090198,0.150885074902754,
1.00763187927034));
#21601=CARTESIAN_POINT('Ctrl Pts',(-0.172648106016301,0.0107452601904448,
1.01557086890765));
#21602=CARTESIAN_POINT('Ctrl Pts',(-0.102652466413112,-0.13923110380544,
1.02350985854496));
#21603=CARTESIAN_POINT('Ctrl Pts',(0.0613144709582997,-0.161750934398167,
1.03144884818226));
#21604=CARTESIAN_POINT('Ctrl Pts',(0.169152212322519,-0.0361988700648799,
1.03938783781957));
#21605=CARTESIAN_POINT('Ctrl Pts',(0.122142696063681,0.12249077894222,1.04732682745687));
#21606=CARTESIAN_POINT('Ctrl Pts',(-0.0366800874558037,0.169048514669047,
1.05526581709418));
#21607=CARTESIAN_POINT('Ctrl Pts',(-0.161924764760067,0.0608539208677085,
1.06320480673148));
#21608=CARTESIAN_POINT('Ctrl Pts',(-0.138938417355371,-0.103048266896446,
1.07114379636879));
#21609=CARTESIAN_POINT('Ctrl Pts',(0.011236529066559,-0.172616828675865,
1.0790827860061));
#21610=CARTESIAN_POINT('Ctrl Pts',(0.151125203217684,-0.0841665140064042,
1.0870217756434));
#21611=CARTESIAN_POINT('Ctrl Pts',(0.152669111109608,0.0813324759279986,
1.09496076528071));
#21612=CARTESIAN_POINT('Ctrl Pts',(0.0144549108781955,0.172377158228925,
1.10289975491801));
#21613=CARTESIAN_POINT('Ctrl Pts',(-0.136991769602464,0.10562236594946,
1.11083874455532));
#21614=CARTESIAN_POINT('Ctrl Pts',(-0.163031873671196,-0.0578224635832477,
1.11877773419263));
#21615=CARTESIAN_POINT('Ctrl Pts',(-0.0398274706979539,-0.168334790537727,
1.12671672382993));
#21616=CARTESIAN_POINT('Ctrl Pts',(0.119836252144435,-0.124748153491552,
1.13465571346724));
#21617=CARTESIAN_POINT('Ctrl Pts',(0.169798099063322,0.0330368685268242,
1.14259470310454));
#21618=CARTESIAN_POINT('Ctrl Pts',(0.0643214233134591,0.160578901573361,
1.15053369274185));
#21619=CARTESIAN_POINT('Ctrl Pts',(-0.100037107244844,0.141121955420339,
1.15847268237915));
#21620=CARTESIAN_POINT('Ctrl Pts',(-0.172818522111203,-0.00752246920075927,
1.16641167201646));
#21621=CARTESIAN_POINT('Ctrl Pts',(-0.0873964240115842,-0.149280588817046,
1.17435066165376));
#21622=CARTESIAN_POINT('Ctrl Pts',(0.0780311106025284,-0.154382560238235,
1.18228965129107));
#21623=CARTESIAN_POINT('Ctrl Pts',(0.172026511281289,-0.01815787828917,
1.19022864092837));
#21624=CARTESIAN_POINT('Ctrl Pts',(0.10854343062882,0.134689096792963,1.19816763056568));
#21625=CARTESIAN_POINT('Ctrl Pts',(-0.0543037217972188,0.164237434607784,
1.20610662020299));
#21626=CARTESIAN_POINT('Ctrl Pts',(-0.167439538594998,0.0434376569656869,
1.21404560984029));
#21627=CARTESIAN_POINT('Ctrl Pts',(-0.127295933190098,-0.117126318651471,
1.2219845994776));
#21628=CARTESIAN_POINT('Ctrl Pts',(0.0293783748903316,-0.170469176734012,
1.2299235891149));
#21629=CARTESIAN_POINT('Ctrl Pts',(0.159158794190081,-0.0677591865323411,
1.23786257875221));
#21630=CARTESIAN_POINT('Ctrl Pts',(0.143240245273553,0.0969796950995427,
1.24580156838952));
#21631=CARTESIAN_POINT('Ctrl Pts',(-0.00380493129617075,0.172940312320012,
1.25374055802682));
#21632=CARTESIAN_POINT('Ctrl Pts',(-0.147366954032488,0.0905859259858403,
1.26167954766413));
#21633=CARTESIAN_POINT('Ctrl Pts',(-0.156024630070406,-0.074693667330688,
1.26961853730143));
#21634=CARTESIAN_POINT('Ctrl Pts',(-0.0218524503424686,-0.171596327294885,
1.27755752693874));
#21635=CARTESIAN_POINT('Ctrl Pts',(0.132324150022753,-0.111414309889572,
1.28549651657604));
#21636=CARTESIAN_POINT('Ctrl Pts',(0.165367059817933,0.0507598725070622,
1.29343550621335));
#21637=CARTESIAN_POINT('Ctrl Pts',(0.0470277596764783,0.166466870408131,
1.30137449585065));
#21638=CARTESIAN_POINT('Ctrl Pts',(-0.114362231391601,0.129784857201791,
1.30931348548797));
#21639=CARTESIAN_POINT('Ctrl Pts',(-0.171061437441431,-0.0257062980954763,
1.31725247512526));
#21640=CARTESIAN_POINT('Ctrl Pts',(-0.071165620995849,-0.157665099140374,
1.32519146476257));
#21641=CARTESIAN_POINT('Ctrl Pts',(0.0938774439379855,-0.145292307632914,
1.33313045439988));
#21642=CARTESIAN_POINT('Ctrl Pts',(0.172982143233999,8.56343898915854E-5,
1.34106944403719));
#21643=CARTESIAN_POINT('Ctrl Pts',(0.0937335447930804,0.145385183220099,
1.34900843367449));
#21644=CARTESIAN_POINT('Ctrl Pts',(-0.0713216883190155,0.157594562185848,
1.3569474233118));
#21645=CARTESIAN_POINT('Ctrl Pts',(-0.171086806821499,0.0255369173285507,
1.3648864129491));
#21646=CARTESIAN_POINT('Ctrl Pts',(-0.114233673229396,-0.129898019862958,
1.37282540258641));
#21647=CARTESIAN_POINT('Ctrl Pts',(0.0471925482590101,-0.166420232464351,
1.38076439222371));
#21648=CARTESIAN_POINT('Ctrl Pts',(0.165417247017141,-0.0505961085897048,
1.38870338186102));
#21649=CARTESIAN_POINT('Ctrl Pts',(0.132213753266125,0.111545248710567,
1.39664237149832));
#21650=CARTESIAN_POINT('Ctrl Pts',(-0.0220222951247444,0.17157464463752,
1.40458136113563));
#21651=CARTESIAN_POINT('Ctrl Pts',(-0.156098584526576,0.0745390809398717,
1.41252035077293));
#21652=CARTESIAN_POINT('Ctrl Pts',(-0.147277046608992,-0.0907316537045687,
1.42045934041024));
#21653=CARTESIAN_POINT('Ctrl Pts',(-0.00363398118293899,-0.172944250658386,
1.42839833004755));
#21654=CARTESIAN_POINT('Ctrl Pts',(0.143336722904634,-0.0968373407211472,
1.43633731968485));
#21655=CARTESIAN_POINT('Ctrl Pts',(0.159090624036536,0.0679158129692223,
1.44427630932216));
#21656=CARTESIAN_POINT('Ctrl Pts',(0.0292114869387437,0.170499931406899,
1.45221529895946));
#21657=CARTESIAN_POINT('Ctrl Pts',(-0.127415456569397,0.116996902323752,
1.46015428859677));
#21658=CARTESIAN_POINT('Ctrl Pts',(-0.167389576437263,-0.0435971050111283,
1.46809327823408));
#21659=CARTESIAN_POINT('Ctrl Pts',(-0.0541541359620402,-0.164303103757731,
1.47603226787138));
#21660=CARTESIAN_POINT('Ctrl Pts',(0.108701533888403,-0.13455879509903,
1.48397125750869));
#21661=CARTESIAN_POINT('Ctrl Pts',(0.171961157005542,0.0182848320604298,
1.49191024714599));
#21662=CARTESIAN_POINT('Ctrl Pts',(0.0779697431325927,0.154543202561513,
1.4998492367833));
#21663=CARTESIAN_POINT('Ctrl Pts',(-0.0877325682749983,0.149025855561406,
1.5077882264206));
#21664=CARTESIAN_POINT('Ctrl Pts',(-0.144149484752264,0.0548439265155397,
1.51308088617881));
#21665=CARTESIAN_POINT('Ctrl Pts',(-0.146217781693078,0.00621955116994065,
1.51572721605791));
#21666=CARTESIAN_POINT('Ctrl Pts',(0.0795408277542855,-0.111329858282327,
-0.0109985226280624));
#21667=CARTESIAN_POINT('Ctrl Pts',(0.116563307192903,-0.0848787452970238,
-0.00835219274896048));
#21668=CARTESIAN_POINT('Ctrl Pts',(0.16150817751539,0.00739908052493189,
-0.00305953299075667));
#21669=CARTESIAN_POINT('Ctrl Pts',(0.0812084309002137,0.139981433724326,
0.00487945664654907));
#21670=CARTESIAN_POINT('Ctrl Pts',(-0.0734975292821143,0.144003850402812,
0.0128184462838548));
#21671=CARTESIAN_POINT('Ctrl Pts',(-0.160887120581772,0.0164101388376342,
0.0207574359211605));
#21672=CARTESIAN_POINT('Ctrl Pts',(-0.101013704785435,-0.126315124179183,
0.0286964255584662));
#21673=CARTESIAN_POINT('Ctrl Pts',(0.0513403816191153,-0.153350170642076,
0.0366354151957719));
#21674=CARTESIAN_POINT('Ctrl Pts',(0.156690838735662,-0.0400338514845966,
0.0445744048330777));
#21675=CARTESIAN_POINT('Ctrl Pts',(0.118604220350264,0.109946623274354,
0.0525133944703833));
#21676=CARTESIAN_POINT('Ctrl Pts',(-0.0280578283917351,0.15927012049393,
0.0604523841076892));
#21677=CARTESIAN_POINT('Ctrl Pts',(-0.14903412333264,0.0627971513379326,
0.0683913737449947));
#21678=CARTESIAN_POINT('Ctrl Pts',(-0.133580279395553,-0.0911646307683348,
0.0763303633823007));
#21679=CARTESIAN_POINT('Ctrl Pts',(0.0041573593468571,-0.161670216863261,
0.0842693530196062));
#21680=CARTESIAN_POINT('Ctrl Pts',(0.138089113144455,-0.0841784443595545,
0.0922083426569122));
#21681=CARTESIAN_POINT('Ctrl Pts',(0.14560980428584,0.0703732645446943,
0.100147332294218));
#21682=CARTESIAN_POINT('Ctrl Pts',(0.0198346691022095,0.160502893816501,
0.108086321931524));
#21683=CARTESIAN_POINT('Ctrl Pts',(-0.124097730593135,0.103703218031488,
0.116025311568829));
#21684=CARTESIAN_POINT('Ctrl Pts',(-0.154427171169137,-0.0480296962598115,
0.123964301206135));
#21685=CARTESIAN_POINT('Ctrl Pts',(-0.0433891157712434,-0.155794689166463,
0.13190329084344));
#21686=CARTESIAN_POINT('Ctrl Pts',(0.107368699171666,-0.12094033522185,
0.139842280480747));
#21687=CARTESIAN_POINT('Ctrl Pts',(0.15983782968835,0.0246266142906177,
0.147781270118052));
#21688=CARTESIAN_POINT('Ctrl Pts',(0.0659863808909888,0.147649582370873,
0.155720259755358));
#21689=CARTESIAN_POINT('Ctrl Pts',(-0.0882710769349216,0.135509478890084,
0.163659249392663));
#21690=CARTESIAN_POINT('Ctrl Pts',(-0.161722413615419,-0.00068026650363694,
0.171598239029969));
#21691=CARTESIAN_POINT('Ctrl Pts',(-0.0871279640988751,-0.136247273976568,
0.179537228667275));
#21692=CARTESIAN_POINT('Ctrl Pts',(0.0672261652318651,-0.147089240053593,
0.187476218304581));
#21693=CARTESIAN_POINT('Ctrl Pts',(0.160039347628626,-0.023281087390596,
0.195415207941886));
#21694=CARTESIAN_POINT('Ctrl Pts',(0.106347475470598,0.121839305139765,
0.203354197579192));
#21695=CARTESIAN_POINT('Ctrl Pts',(-0.0446982220051161,0.15542416405057,
0.211293187216498));
#21696=CARTESIAN_POINT('Ctrl Pts',(-0.154825760608133,0.0467288526640558,
0.219232176853804));
#21697=CARTESIAN_POINT('Ctrl Pts',(-0.12322092627477,-0.104743520787053,
0.227171166491109));
#21698=CARTESIAN_POINT('Ctrl Pts',(0.0211842211805034,-0.160330379506191,
0.235110156128415));
#21699=CARTESIAN_POINT('Ctrl Pts',(0.146196665995071,-0.0691457639426259,
0.24304914576572));
#21700=CARTESIAN_POINT('Ctrl Pts',(0.137376082602736,0.0853370596399817,
0.250988135403027));
#21701=CARTESIAN_POINT('Ctrl Pts',(0.00279711058556459,0.161699653653757,
0.258927125040332));
#21702=CARTESIAN_POINT('Ctrl Pts',(-0.134342424474264,0.0900372967480426,
0.266866114677638));
#21703=CARTESIAN_POINT('Ctrl Pts',(-0.148500677015507,-0.0640480346713102,
0.274805104314944));
#21704=CARTESIAN_POINT('Ctrl Pts',(-0.0267167371651392,-0.159501779847699,
0.282744093952249));
#21705=CARTESIAN_POINT('Ctrl Pts',(0.119524544542348,-0.108942576944327,
0.290683083589556));
#21706=CARTESIAN_POINT('Ctrl Pts',(0.156349297273321,0.0413460888291301,
0.29862207322686));
#21707=CARTESIAN_POINT('Ctrl Pts',(0.0500469836677093,0.153785243912065,
0.306561062864167));
#21708=CARTESIAN_POINT('Ctrl Pts',(-0.102069913541897,0.125444547784578,
0.314500052501472));
#21709=CARTESIAN_POINT('Ctrl Pts',(-0.160748800211922,-0.0177320345633525,
0.322439042138778));
#21710=CARTESIAN_POINT('Ctrl Pts',(-0.0722731771226978,-0.144676154524232,
0.330378031776084));
#21711=CARTESIAN_POINT('Ctrl Pts',(0.082363586418043,-0.139179170322594,
0.338317021413389));
#21712=CARTESIAN_POINT('Ctrl Pts',(0.16160213133829,-0.00627319426210969,
0.346256011050695));
#21713=CARTESIAN_POINT('Ctrl Pts',(0.0929050003357002,0.132375461215256,
0.354195000688001));
#21714=CARTESIAN_POINT('Ctrl Pts',(-0.0608402912787218,0.149843454232904,
0.362133990325306));
#21715=CARTESIAN_POINT('Ctrl Pts',(-0.158890465884947,0.0301400343429239,
0.370072979962613));
#21716=CARTESIAN_POINT('Ctrl Pts',(-0.1114873084483,-0.117154521356547,
0.378011969599918));
#21717=CARTESIAN_POINT('Ctrl Pts',(0.0379748391485164,-0.157202141877815,
0.385950959237223));
#21718=CARTESIAN_POINT('Ctrl Pts',(0.152673624090564,-0.0533419752763387,
0.39388994887453));
#21719=CARTESIAN_POINT('Ctrl Pts',(0.127610169584502,0.0993491139263089,
0.401828938511835));
#21720=CARTESIAN_POINT('Ctrl Pts',(-0.014271649480085,0.16109289816887,
0.409767928149142));
#21721=CARTESIAN_POINT('Ctrl Pts',(-0.143088751545671,0.0753671745551693,
0.417706917786446));
#21722=CARTESIAN_POINT('Ctrl Pts',(-0.140917908083783,-0.0793520321139836,
0.425645907423752));
#21723=CARTESIAN_POINT('Ctrl Pts',(-0.00974637750615997,-0.161429891732714,
0.433584897061058));
#21724=CARTESIAN_POINT('Ctrl Pts',(0.130347293715478,-0.0957297489831606,
0.441523886698364));
#21725=CARTESIAN_POINT('Ctrl Pts',(0.15111695082405,0.0576044181723055,
0.449462876335669));
#21726=CARTESIAN_POINT('Ctrl Pts',(0.0335493961742207,0.158205688379633,
0.457401865972975));
#21727=CARTESIAN_POINT('Ctrl Pts',(-0.114730331382826,0.113980493419335,
0.465340855610281));
#21728=CARTESIAN_POINT('Ctrl Pts',(-0.157982303542021,-0.03458603167299,
0.473279845247587));
#21729=CARTESIAN_POINT('Ctrl Pts',(-0.0566123040428622,-0.151491415104245,
0.481218834884892));
#21730=CARTESIAN_POINT('Ctrl Pts',(0.0965823799129518,-0.129716790392294,
0.489157824522198));
#21731=CARTESIAN_POINT('Ctrl Pts',(0.161362514281243,0.0108046658515635,
0.497096814159504));
#21732=CARTESIAN_POINT('Ctrl Pts',(0.0784263257203939,0.141435191000425,
0.50503580379681));
#21733=CARTESIAN_POINT('Ctrl Pts',(-0.076303789130349,0.14259149197508,
0.512974793434115));
#21734=CARTESIAN_POINT('Ctrl Pts',(-0.161183014472451,0.0132150544797126,
0.520913783071421));
#21735=CARTESIAN_POINT('Ctrl Pts',(-0.0985102366584373,-0.128258859705,
0.528852772708727));
#21736=CARTESIAN_POINT('Ctrl Pts',(0.0543419114689404,-0.152320577983508,
0.536791762346032));
#21737=CARTESIAN_POINT('Ctrl Pts',(0.157447763940923,-0.0369432463290883,
0.544730751983338));
#21738=CARTESIAN_POINT('Ctrl Pts',(0.116420979124965,0.112253095453589,
0.552669741620643));
#21739=CARTESIAN_POINT('Ctrl Pts',(-0.0311812332291155,0.158689421555565,
0.56060873125795));
#21740=CARTESIAN_POINT('Ctrl Pts',(-0.150239163551416,0.0598564579197502,
0.568547720895255));
#21741=CARTESIAN_POINT('Ctrl Pts',(-0.131763436204723,-0.0937709907106254,
0.576486710532561));
#21742=CARTESIAN_POINT('Ctrl Pts',(0.00733268664935855,-0.161557523891122,
0.584425700169866));
#21743=CARTESIAN_POINT('Ctrl Pts',(0.139716237417787,-0.0814492162095161,
0.592364689807173));
#21744=CARTESIAN_POINT('Ctrl Pts',(0.144199148209332,0.0732202668325601,
0.600303679444478));
#21745=CARTESIAN_POINT('Ctrl Pts',(0.0166776214282734,0.160861613702037,
0.608242669081784));
#21746=CARTESIAN_POINT('Ctrl Pts',(-0.126111124778327,0.101245177793678,
0.616181658719089));
#21747=CARTESIAN_POINT('Ctrl Pts',(-0.153453779210204,-0.0510542795996006,
0.624120648356396));
#21748=CARTESIAN_POINT('Ctrl Pts',(-0.0403200156494649,-0.156617042997737,
0.6320596379937));
#21749=CARTESIAN_POINT('Ctrl Pts',(0.10972395892722,-0.118807637198397,
0.639998627631007));
#21750=CARTESIAN_POINT('Ctrl Pts',(0.159323168980049,0.0277620180369333,
0.647937617268312));
#21751=CARTESIAN_POINT('Ctrl Pts',(0.0630729369615192,0.148917448414806,
0.655876606905618));
#21752=CARTESIAN_POINT('Ctrl Pts',(-0.0909162461746061,0.133749160748195,
0.663815596542924));
#21753=CARTESIAN_POINT('Ctrl Pts',(-0.161677836835157,-0.00385731715476066,
0.671754586180229));
#21754=CARTESIAN_POINT('Ctrl Pts',(-0.0844344483789265,-0.137932685561743,
0.679693575817536));
#21755=CARTESIAN_POINT('Ctrl Pts',(0.0701028908975481,-0.145740133481257,
0.687632565454841));
#21756=CARTESIAN_POINT('Ctrl Pts',(0.1604658380222,-0.0201324774223393,
0.695571555092147));
#21757=CARTESIAN_POINT('Ctrl Pts',(0.10393330787963,0.123905081947942,0.703510544729453));
#21758=CARTESIAN_POINT('Ctrl Pts',(-0.0477430426119635,0.15451603056473,
0.711449534366758));
#21759=CARTESIAN_POINT('Ctrl Pts',(-0.155713909636705,0.0436781428746717,
0.719388524004064));
#21760=CARTESIAN_POINT('Ctrl Pts',(-0.121139364160222,-0.10714409115852,
0.72732751364137));
#21761=CARTESIAN_POINT('Ctrl Pts',(0.0243299669821161,-0.159883252800214,
0.735266503278675));
#21762=CARTESIAN_POINT('Ctrl Pts',(0.147526880793862,-0.0662602540182413,
0.743205492915981));
#21763=CARTESIAN_POINT('Ctrl Pts',(0.135673045916277,0.0880194662056535,
0.751144482553287));
#21764=CARTESIAN_POINT('Ctrl Pts',(-0.000380164216571841,0.161723397486253,
0.759083472190592));
#21765=CARTESIAN_POINT('Ctrl Pts',(-0.136085360063504,0.0873806419964673,
0.767022461827899));
#21766=CARTESIAN_POINT('Ctrl Pts',(-0.147213735311121,-0.0669531026545853,
0.774961451465203));
#21767=CARTESIAN_POINT('Ctrl Pts',(-0.023578025097595,-0.159995870421162,
0.78290044110251));
#21768=CARTESIAN_POINT('Ctrl Pts',(0.121641751185188,-0.106573384050283,
0.790839430739816));
#21769=CARTESIAN_POINT('Ctrl Pts',(0.155506840911589,0.0444097314676148,
0.798778420377121));
#21770=CARTESIAN_POINT('Ctrl Pts',(0.047016075363265,0.15473878142458,0.806717410014428));
#21771=CARTESIAN_POINT('Ctrl Pts',(-0.104514684958047,0.123415081928621,
0.814656399651731));
#21772=CARTESIAN_POINT('Ctrl Pts',(-0.16036941405942,-0.020886666885039,
0.82259538928904));
#21773=CARTESIAN_POINT('Ctrl Pts',(-0.0694169354231278,-0.146068103622213,
0.830534378926343));
#21774=CARTESIAN_POINT('Ctrl Pts',(0.085081990139753,-0.137534202194171,
0.838473368563651));
#21775=CARTESIAN_POINT('Ctrl Pts',(0.161694184779289,-0.00309716449182502,
0.846412358200955));
#21776=CARTESIAN_POINT('Ctrl Pts',(0.0902864348795877,0.134175115040242,
0.854351347838261));
#21777=CARTESIAN_POINT('Ctrl Pts',(-0.0637723584188847,0.148619272374149,
0.862290337475567));
#21778=CARTESIAN_POINT('Ctrl Pts',(-0.159451928190027,0.0270126713934565,
0.870229327112872));
#21779=CARTESIAN_POINT('Ctrl Pts',(-0.109164185657521,-0.119322178948671,
0.878168316750179));
#21780=CARTESIAN_POINT('Ctrl Pts',(0.0410558873341998,-0.156425752146281,
0.886107306387484));
#21781=CARTESIAN_POINT('Ctrl Pts',(0.153692109215179,-0.0503322698109037,
0.894046296024789));
#21782=CARTESIAN_POINT('Ctrl Pts',(0.125633738317809,0.101836956040625,
0.901985285662096));
#21783=CARTESIAN_POINT('Ctrl Pts',(-0.0174337097671096,0.160781427979367,
0.909924275299401));
#21784=CARTESIAN_POINT('Ctrl Pts',(-0.144541791370401,0.072541521673891,
0.917863264936708));
#21785=CARTESIAN_POINT('Ctrl Pts',(-0.13933176907,-0.082105176128868,0.925802254574012));
#21786=CARTESIAN_POINT('Ctrl Pts',(-0.00657306121577474,-0.161590212220858,
0.933741244211319));
#21787=CARTESIAN_POINT('Ctrl Pts',(0.132202833700187,-0.0931504835251481,
0.941680233848624));
#21788=CARTESIAN_POINT('Ctrl Pts',(0.149956094815541,0.0605621288182698,
0.949619223485929));
#21789=CARTESIAN_POINT('Ctrl Pts',(0.0304348282896272,0.158834262822317,
0.957558213123236));
#21790=CARTESIAN_POINT('Ctrl Pts',(-0.116947437700435,0.111704514835484,
0.965497202760542));
#21791=CARTESIAN_POINT('Ctrl Pts',(-0.157272339407096,-0.0376830608728604,
0.973436192397847));
#21792=CARTESIAN_POINT('Ctrl Pts',(-0.0536251929639052,-0.152574376940928,
0.981375182035153));
#21793=CARTESIAN_POINT('Ctrl Pts',(0.0991121424632477,-0.127794307524525,
0.989314171672459));
#21794=CARTESIAN_POINT('Ctrl Pts',(0.161119104064031,0.0139726921146952,
0.997253161309763));
#21795=CARTESIAN_POINT('Ctrl Pts',(0.0756325681075411,0.142948649734045,
1.00519215094707));
#21796=CARTESIAN_POINT('Ctrl Pts',(-0.0790904005129918,0.141064915432658,
1.01313114058437));
#21797=CARTESIAN_POINT('Ctrl Pts',(-0.161411527883023,0.0100459188627121,
1.02107013022168));
#21798=CARTESIAN_POINT('Ctrl Pts',(-0.095971463730607,-0.130169427934261,
1.02900911985899));
#21799=CARTESIAN_POINT('Ctrl Pts',(0.0573238981132153,-0.151223584550935,
1.03694810949629));
#21800=CARTESIAN_POINT('Ctrl Pts',(0.158143159897702,-0.0338429135403315,
1.0448870991336));
#21801=CARTESIAN_POINT('Ctrl Pts',(0.114193197054413,0.114518625410106,
1.0528260887709));
#21802=CARTESIAN_POINT('Ctrl Pts',(-0.0342928115212847,0.158046211271557,
1.06076507840821));
#21803=CARTESIAN_POINT('Ctrl Pts',(-0.151386101389109,0.0568933223281485,
1.06870406804552));
#21804=CARTESIAN_POINT('Ctrl Pts',(-0.129895790602315,-0.0963415040526547,
1.07664305768282));
#21805=CARTESIAN_POINT('Ctrl Pts',(0.0105052141409744,-0.161382286187737,
1.08458204732013));
#21806=CARTESIAN_POINT('Ctrl Pts',(0.141289415307547,-0.0786886455683398,
1.09252103695743));
#21807=CARTESIAN_POINT('Ctrl Pts',(0.14273283995608,0.076039057183793,1.10046002659474));
#21808=CARTESIAN_POINT('Ctrl Pts',(0.013514131745196,0.161158214381091,
1.10839901623204));
#21809=CARTESIAN_POINT('Ctrl Pts',(-0.128075837894479,0.0987480712062529,
1.11633800586935));
#21810=CARTESIAN_POINT('Ctrl Pts',(-0.152421155552179,-0.0540591635106084,
1.12427699550666));
#21811=CARTESIAN_POINT('Ctrl Pts',(-0.0372353514058616,-0.157378938949945,
1.13221598514396));
#21812=CARTESIAN_POINT('Ctrl Pts',(0.11203686504723,-0.116629081663695,
1.14015497478127));
#21813=CARTESIAN_POINT('Ctrl Pts',(0.158747009937404,0.0308867067726846,
1.14809396441857));
#21814=CARTESIAN_POINT('Ctrl Pts',(0.0601351468730053,0.150127831962932,
1.15603295405588));
#21815=CARTESIAN_POINT('Ctrl Pts',(-0.0935263218228598,0.13193721592339,
1.16397194369318));
#21816=CARTESIAN_POINT('Ctrl Pts',(-0.161570852667341,-0.00703287904607843,
1.17191093333049));
#21817=CARTESIAN_POINT('Ctrl Pts',(-0.0817083410685703,-0.13956485524354,
1.17984992296779));
#21818=CARTESIAN_POINT('Ctrl Pts',(0.0729525569401478,-0.144334771469742,
1.1877889126051));
#21819=CARTESIAN_POINT('Ctrl Pts',(0.160830388835411,-0.016976096323307,
1.19572790224241));
#21820=CARTESIAN_POINT('Ctrl Pts',(0.101479022178261,0.125923031559255,
1.20366689187971));
#21821=CARTESIAN_POINT('Ctrl Pts',(-0.0507694344715009,0.153548254118279,
1.21160588151702));
#21822=CARTESIAN_POINT('Ctrl Pts',(-0.15654195331917,0.0406105733811438,
1.21954487115432));
#21823=CARTESIAN_POINT('Ctrl Pts',(-0.119011042423884,-0.109503304062093,
1.22748386079163));
#21824=CARTESIAN_POINT('Ctrl Pts',(0.0274663214511058,-0.159374411387982,
1.23542285042894));
#21825=CARTESIAN_POINT('Ctrl Pts',(0.148800150427453,-0.0633491677300162,
1.24336184006624));
#21826=CARTESIAN_POINT('Ctrl Pts',(0.133917639627974,0.0906678973829495,
1.25130082970354));
#21827=CARTESIAN_POINT('Ctrl Pts',(-0.00355729227603857,0.161684716318317,
1.25923981934086));
#21828=CARTESIAN_POINT('Ctrl Pts',(-0.137775766897813,0.0846902584421788,
1.26717880897816));
#21829=CARTESIAN_POINT('Ctrl Pts',(-0.14586996931591,-0.0698323268364953,
1.27511779861547));
#21830=CARTESIAN_POINT('Ctrl Pts',(-0.0204302119447119,-0.160428202816007,
1.28305678825277));
#21831=CARTESIAN_POINT('Ctrl Pts',(0.123712004283314,-0.104163053984564,
1.29099577789008));
#21832=CARTESIAN_POINT('Ctrl Pts',(0.15460435913624,0.0474562320176185,
1.29893476752738));
#21833=CARTESIAN_POINT('Ctrl Pts',(0.043967018911749,0.155632589980133,
1.30687375716469));
#21834=CARTESIAN_POINT('Ctrl Pts',(-0.106919113837756,0.121337978043289,
1.31481274680199));
#21835=CARTESIAN_POINT('Ctrl Pts',(-0.159928125575155,-0.0240332370134145,
1.3227517364393));
#21836=CARTESIAN_POINT('Ctrl Pts',(-0.0665338988230771,-0.147403670583407,
1.33069072607661));
#21837=CARTESIAN_POINT('Ctrl Pts',(0.0877675522160205,-0.135836146169277,
1.33862971571391));
#21838=CARTESIAN_POINT('Ctrl Pts',(0.161723824721502,8.00609866524728E-5,
1.34656870535122));
#21839=CARTESIAN_POINT('Ctrl Pts',(0.0876330185603928,0.135922977069285,
1.35450769498852));
#21840=CARTESIAN_POINT('Ctrl Pts',(-0.0666798087068602,0.147337724435113,
1.36244668462583));
#21841=CARTESIAN_POINT('Ctrl Pts',(-0.159951843822013,0.0238748801740983,
1.37038567426313));
#21842=CARTESIAN_POINT('Ctrl Pts',(-0.106798922716859,-0.121443775659372,
1.37832466390044));
#21843=CARTESIAN_POINT('Ctrl Pts',(0.0441210824430389,-0.155588987406456,
1.38626365353774));
#21844=CARTESIAN_POINT('Ctrl Pts',(0.154651279966657,-0.0473031264624986,
1.39420264317505));
#21845=CARTESIAN_POINT('Ctrl Pts',(0.123608792556459,0.10428547082216,1.40214163281236));
#21846=CARTESIAN_POINT('Ctrl Pts',(-0.020589002599541,0.160407931346284,
1.41008062244966));
#21847=CARTESIAN_POINT('Ctrl Pts',(-0.145939110542184,0.0696878015005003,
1.41801961208697));
#21848=CARTESIAN_POINT('Ctrl Pts',(-0.137691710982408,-0.0848265016612731,
1.42595860172427));
#21849=CARTESIAN_POINT('Ctrl Pts',(-0.00339746822928561,-0.161688398335044,
1.43389759136158));
#21850=CARTESIAN_POINT('Ctrl Pts',(0.134007838137522,-0.0905348079547059,
1.44183658099889));
#21851=CARTESIAN_POINT('Ctrl Pts',(0.148736417039967,0.0634956003383226,
1.44977557063619));
#21852=CARTESIAN_POINT('Ctrl Pts',(0.0273102951854726,0.159403164432859,
1.4577145602735));
#21853=CARTESIAN_POINT('Ctrl Pts',(-0.119122786779006,0.109382310628272,
1.4656535499108));
#21854=CARTESIAN_POINT('Ctrl Pts',(-0.156495242883694,-0.0407596439572756,
1.47359253954811));
#21855=CARTESIAN_POINT('Ctrl Pts',(-0.0506295842364637,-0.153609649276743,
1.48153152918541));
#21856=CARTESIAN_POINT('Ctrl Pts',(0.10162683549218,-0.125801210382132,
1.48947051882272));
#21857=CARTESIAN_POINT('Ctrl Pts',(0.160769288057966,0.017094787472962,
1.49740950846002));
#21858=CARTESIAN_POINT('Ctrl Pts',(0.0728951834924312,0.144484958595688,
1.50534849809733));
#21859=CARTESIAN_POINT('Ctrl Pts',(-0.0820226078184241,0.139326700971572,
1.51328748773464));
#21860=CARTESIAN_POINT('Ctrl Pts',(-0.134767702434085,0.0512744806661359,
1.51858014749284));
#21861=CARTESIAN_POINT('Ctrl Pts',(-0.136701386950156,0.00581475974600206,
1.52122647737194));
#21862=CARTESIAN_POINT('Ctrl Pts',(0.0740036351041134,-0.103579689087085,
-0.0054992613140312));
#21863=CARTESIAN_POINT('Ctrl Pts',(0.108448814220036,-0.0789699563406641,
-0.00285293143492929));
#21864=CARTESIAN_POINT('Ctrl Pts',(0.150264871169078,0.00688399744800666,
0.00243972832327453));
#21865=CARTESIAN_POINT('Ctrl Pts',(0.0755551489391376,0.130236700260234,
0.0103787179605803));
#21866=CARTESIAN_POINT('Ctrl Pts',(-0.0683810376584167,0.133979098529349,
0.0183177075978859));
#21867=CARTESIAN_POINT('Ctrl Pts',(-0.14968704878538,0.0152677557027674,
0.0262566972351917));
#21868=CARTESIAN_POINT('Ctrl Pts',(-0.0939816891590436,-0.11752176362514,
0.0341956868724974));
#21869=CARTESIAN_POINT('Ctrl Pts',(0.0477663481097245,-0.142674779628989,
0.0421346765098031));
#21870=CARTESIAN_POINT('Ctrl Pts',(0.14578288888032,-0.0372469160898187,
0.0500736661471088));
#21871=CARTESIAN_POINT('Ctrl Pts',(0.110347650287512,0.102292747252513,
0.0580126557844146));
#21872=CARTESIAN_POINT('Ctrl Pts',(-0.0261045975097209,0.148182615303324,
0.0659516454217203));
#21873=CARTESIAN_POINT('Ctrl Pts',(-0.13865919166998,0.0584255608647477,
0.073890635059026));
#21874=CARTESIAN_POINT('Ctrl Pts',(-0.124281158904105,-0.0848182532198701,
0.0818296246963318));
#21875=CARTESIAN_POINT('Ctrl Pts',(0.00386794697500161,-0.15041563023346,
0.0897686143336374));
#21876=CARTESIAN_POINT('Ctrl Pts',(0.128476112576568,-0.0783184064825255,
0.0977076039709433));
#21877=CARTESIAN_POINT('Ctrl Pts',(0.135473254782295,0.0654742669580799,
0.105646593608249));
#21878=CARTESIAN_POINT('Ctrl Pts',(0.0184538891044151,0.149329569763132,
0.113585583245555));
#21879=CARTESIAN_POINT('Ctrl Pts',(-0.115458732720671,0.096483973363118,
0.12152457288286));
#21880=CARTESIAN_POINT('Ctrl Pts',(-0.143676805334049,-0.0446861343604874,
0.129463562520166));
#21881=CARTESIAN_POINT('Ctrl Pts',(-0.0403686054279526,-0.144949124289353,
0.137402552157472));
#21882=CARTESIAN_POINT('Ctrl Pts',(0.0998942839726139,-0.112521137758025,
0.145341541794778));
#21883=CARTESIAN_POINT('Ctrl Pts',(0.14871080372247,0.0229122455632766,
0.153280531432083));
#21884=CARTESIAN_POINT('Ctrl Pts',(0.0613927738894439,0.137371034794898,
0.161219521069389));
#21885=CARTESIAN_POINT('Ctrl Pts',(-0.0821261326059948,0.126076058196294,
0.169158510706695));
#21886=CARTESIAN_POINT('Ctrl Pts',(-0.150464193336327,-0.000632910110818063,
0.177097500344));
#21887=CARTESIAN_POINT('Ctrl Pts',(-0.0810625969653723,-0.126762492068094,
0.185036489981306));
#21888=CARTESIAN_POINT('Ctrl Pts',(0.0625462512992226,-0.136849700411639,
0.192975479618612));
#21889=CARTESIAN_POINT('Ctrl Pts',(0.148898293097928,-0.0216603868066741,
0.200914469255917));
#21890=CARTESIAN_POINT('Ctrl Pts',(0.0989441522193119,0.113357526360621,
0.208853458893223));
#21891=CARTESIAN_POINT('Ctrl Pts',(-0.0415865789238149,0.144604393083411,
0.216792448530529));
#21892=CARTESIAN_POINT('Ctrl Pts',(-0.144047647180085,0.0434758483035601,
0.224731438167835));
#21893=CARTESIAN_POINT('Ctrl Pts',(-0.114642966671137,-0.0974518559926297,
0.232670427805141));
#21894=CARTESIAN_POINT('Ctrl Pts',(0.0197094928286333,-0.149169064945282,
0.240609417442446));
#21895=CARTESIAN_POINT('Ctrl Pts',(0.136019262424063,-0.0643322181611298,
0.248548407079752));
#21896=CARTESIAN_POINT('Ctrl Pts',(0.127812719278849,0.0793963653730636,
0.256487396717058));
#21897=CARTESIAN_POINT('Ctrl Pts',(0.00260239121171357,0.150443017797356,
0.264426386354363));
#21898=CARTESIAN_POINT('Ctrl Pts',(-0.124990247656303,0.0837693979610897,
0.272365375991669));
#21899=CARTESIAN_POINT('Ctrl Pts',(-0.138162880936044,-0.0595893646165358,
0.280304365628975));
#21900=CARTESIAN_POINT('Ctrl Pts',(-0.0248568656394851,-0.148398147813718,
0.288243355266281));
#21901=CARTESIAN_POINT('Ctrl Pts',(0.111203906597776,-0.101358597076653,
0.296182344903586));
#21902=CARTESIAN_POINT('Ctrl Pts',(0.145465123646218,0.0384678027257296,
0.304121334540892));
#21903=CARTESIAN_POINT('Ctrl Pts',(0.0465629893725541,0.143079565503422,
0.312060324178198));
#21904=CARTESIAN_POINT('Ctrl Pts',(-0.0949643705016135,0.116711791945748,
0.319999313815503));
#21905=CARTESIAN_POINT('Ctrl Pts',(-0.149558357514911,-0.0164976283567656,
0.327938303452809));
#21906=CARTESIAN_POINT('Ctrl Pts',(-0.0672419181269484,-0.134604600554976,
0.335877293090115));
#21907=CARTESIAN_POINT('Ctrl Pts',(0.0766298889166206,-0.12949028600085,
0.343816282727421));
#21908=CARTESIAN_POINT('Ctrl Pts',(0.150352284446295,-0.00583648916182633,
0.351755272364726));
#21909=CARTESIAN_POINT('Ctrl Pts',(0.0864374678803939,0.123160213504125,
0.359694262002032));
#21910=CARTESIAN_POINT('Ctrl Pts',(-0.0566049265834532,0.139412181427728,
0.367633251639338));
#21911=CARTESIAN_POINT('Ctrl Pts',(-0.147829390149123,0.0280418517950267,
0.375572241276644));
#21912=CARTESIAN_POINT('Ctrl Pts',(-0.103726178443039,-0.108998871322406,
0.383511230913949));
#21913=CARTESIAN_POINT('Ctrl Pts',(0.0353312408083745,-0.146258597924691,
0.391450220551255));
#21914=CARTESIAN_POINT('Ctrl Pts',(0.142045330507792,-0.0496286018832686,
0.399389210188561));
#21915=CARTESIAN_POINT('Ctrl Pts',(0.118726655129599,0.0924329779120693,
0.407328199825866));
#21916=CARTESIAN_POINT('Ctrl Pts',(-0.0132781361506635,0.1498785012746,
0.415267189463172));
#21917=CARTESIAN_POINT('Ctrl Pts',(-0.133127703795094,0.0701205285647604,
0.423206179100478));
#21918=CARTESIAN_POINT('Ctrl Pts',(-0.131107982452518,-0.0738279823724454,
0.431145168737783));
#21919=CARTESIAN_POINT('Ctrl Pts',(-0.00906788859151817,-0.150192035209753,
0.439084158375089));
#21920=CARTESIAN_POINT('Ctrl Pts',(0.121273235812024,-0.0890655731449414,
0.447023148012395));
#21921=CARTESIAN_POINT('Ctrl Pts',(0.14059702422731,0.0535943170716914,
0.4549621376497));
#21922=CARTESIAN_POINT('Ctrl Pts',(0.031213872705855,0.14719228306762,0.462901127287006));
#21923=CARTESIAN_POINT('Ctrl Pts',(-0.106743440051405,0.106045801661112,
0.470840116924312));
#21924=CARTESIAN_POINT('Ctrl Pts',(-0.146984449047318,-0.0321783433727119,
0.478779106561618));
#21925=CARTESIAN_POINT('Ctrl Pts',(-0.0526712684425847,-0.140945420374714,
0.486718096198923));
#21926=CARTESIAN_POINT('Ctrl Pts',(0.0898588486235595,-0.120686624644175,
0.49465708583623));
#21927=CARTESIAN_POINT('Ctrl Pts',(0.150129348203927,0.0100525047535443,
0.502596075473534));
#21928=CARTESIAN_POINT('Ctrl Pts',(0.0729667185397875,0.131589254992538,
0.510535065110842));
#21929=CARTESIAN_POINT('Ctrl Pts',(-0.0709919412117167,0.132665060686482,
0.518474054748145));
#21930=CARTESIAN_POINT('Ctrl Pts',(-0.149962344179375,0.0122950954523496,
0.526413044385453));
#21931=CARTESIAN_POINT('Ctrl Pts',(-0.0916524986414713,-0.119330187030486,
0.534352034022757));
#21932=CARTESIAN_POINT('Ctrl Pts',(0.0505589280467443,-0.141716861518734,
0.542291023660064));
#21933=CARTESIAN_POINT('Ctrl Pts',(0.146487121137799,-0.0343714617774037,
0.550230013297369));
#21934=CARTESIAN_POINT('Ctrl Pts',(0.108316394245265,0.104438655591022,
0.558169002934674));
#21935=CARTESIAN_POINT('Ctrl Pts',(-0.0290105681715044,0.147642341414387,
0.566107992571982));
#21936=CARTESIAN_POINT('Ctrl Pts',(-0.139780343651344,0.0556895822633619,
0.574046982209285));
#21937=CARTESIAN_POINT('Ctrl Pts',(-0.122590794290966,-0.0872431727934394,
0.581985971846593));
#21938=CARTESIAN_POINT('Ctrl Pts',(0.00682222554696161,-0.150310782322966,
0.589924961483898));
#21939=CARTESIAN_POINT('Ctrl Pts',(0.129989965454297,-0.0757791721064987,
0.597863951121203));
#21940=CARTESIAN_POINT('Ctrl Pts',(0.134160800782372,0.0681230766876274,
0.60580294075851));
#21941=CARTESIAN_POINT('Ctrl Pts',(0.015516617634347,0.149663317553585,
0.613741930395814));
#21942=CARTESIAN_POINT('Ctrl Pts',(-0.117331965534667,0.0941970482962578,
0.621680920033121));
#21943=CARTESIAN_POINT('Ctrl Pts',(-0.142771175541451,-0.0475001629309618,
0.629619909670426));
#21944=CARTESIAN_POINT('Ctrl Pts',(-0.0375131590877193,-0.145714230393655,
0.637558899307733));
#21945=CARTESIAN_POINT('Ctrl Pts',(0.102085583566124,-0.110536906379362,
0.645497888945037));
#21946=CARTESIAN_POINT('Ctrl Pts',(0.148231970847143,0.0258293798362968,
0.653436878582344));
#21947=CARTESIAN_POINT('Ctrl Pts',(0.0586821478180281,0.138550639014834,
0.661375868219649));
#21948=CARTESIAN_POINT('Ctrl Pts',(-0.0845871597882484,0.124438283670714,
0.669314857856955));
#21949=CARTESIAN_POINT('Ctrl Pts',(-0.150422719745043,-0.00358879206139753,
0.67725384749426));
#21950=CARTESIAN_POINT('Ctrl Pts',(-0.078556588917505,-0.128330574617282,
0.685192837131567));
#21951=CARTESIAN_POINT('Ctrl Pts',(0.065222715229363,-0.135594511179713,
0.693131826768872));
#21952=CARTESIAN_POINT('Ctrl Pts',(0.149295093588351,-0.0187309656558678,
0.701070816406178));
#21953=CARTESIAN_POINT('Ctrl Pts',(0.0966980456281902,0.11527949520901,
0.709009806043483));
#21954=CARTESIAN_POINT('Ctrl Pts',(-0.044419435954706,0.14375947882982,
0.716948795680789));
#21955=CARTESIAN_POINT('Ctrl Pts',(-0.144873968183829,0.0406375120624596,
0.724887785318095));
#21956=CARTESIAN_POINT('Ctrl Pts',(-0.112706311402131,-0.099685311927494,
0.732826774955401));
#21957=CARTESIAN_POINT('Ctrl Pts',(0.0226362492002416,-0.148753064728429,
0.740765764592706));
#21958=CARTESIAN_POINT('Ctrl Pts',(0.137256875023267,-0.0616475814838108,
0.748704754230013));
#21959=CARTESIAN_POINT('Ctrl Pts',(0.126228238590478,0.0818920376245527,
0.756643743867318));
#21960=CARTESIAN_POINT('Ctrl Pts',(-0.000353699285724532,0.150465108715513,
0.764582733504624));
#21961=CARTESIAN_POINT('Ctrl Pts',(-0.126611849706441,0.0812976848247803,
0.772521723141928));
#21962=CARTESIAN_POINT('Ctrl Pts',(-0.136965528997667,-0.0622921978288208,
0.780460712779236));
#21963=CARTESIAN_POINT('Ctrl Pts',(-0.0219366533522686,-0.148857842533265,
0.788399702416541));
#21964=CARTESIAN_POINT('Ctrl Pts',(0.113173725020093,-0.0991543342927188,
0.796338692053846));
#21965=CARTESIAN_POINT('Ctrl Pts',(0.144681314438483,0.0413181715024817,
0.804277681691154));
#21966=CARTESIAN_POINT('Ctrl Pts',(0.0437430761464933,0.143966723006387,
0.812216671328456));
#21967=CARTESIAN_POINT('Ctrl Pts',(-0.0972389504488157,0.114823606281847,
0.820155660965765));
#21968=CARTESIAN_POINT('Ctrl Pts',(-0.149205382128735,-0.0194326526180533,
0.828094650603069));
#21969=CARTESIAN_POINT('Ctrl Pts',(-0.0645845121824554,-0.135899649852787,
0.836033640240376));
#21970=CARTESIAN_POINT('Ctrl Pts',(0.0791590524011713,-0.127959831458565,
0.843972629877681));
#21971=CARTESIAN_POINT('Ctrl Pts',(0.150437929635691,-0.00288155702400619,
0.851911619514986));
#21972=CARTESIAN_POINT('Ctrl Pts',(0.0840011924733913,0.12483458538003,
0.859850609152293));
#21973=CARTESIAN_POINT('Ctrl Pts',(-0.0593328794206009,0.138273220341526,
0.867789598789597));
#21974=CARTESIAN_POINT('Ctrl Pts',(-0.148351766552825,0.0251321985630355,
0.875728588426904));
#21975=CARTESIAN_POINT('Ctrl Pts',(-0.1015647786165,-0.111015628577859,
0.883667578064211));
#21976=CARTESIAN_POINT('Ctrl Pts',(0.0381978034543637,-0.145536256153639,
0.891606567701514));
#21977=CARTESIAN_POINT('Ctrl Pts',(0.142992914329196,-0.046828415471795,
0.899545557338823));
#21978=CARTESIAN_POINT('Ctrl Pts',(0.116887812080083,0.0947476302135675,
0.907484546976125));
#21979=CARTESIAN_POINT('Ctrl Pts',(-0.0162200712834111,0.149588713917584,
0.915423536613434));
#21980=CARTESIAN_POINT('Ctrl Pts',(-0.134479591021026,0.067491582014154,
0.923362526250738));
#21981=CARTESIAN_POINT('Ctrl Pts',(-0.129632261667175,-0.0763894677230377,
0.931301515888044));
#21982=CARTESIAN_POINT('Ctrl Pts',(-0.00611548103612966,-0.150341195071919,
0.93924050552535));
#21983=CARTESIAN_POINT('Ctrl Pts',(0.122999603362204,-0.0866658618874593,
0.947179495162656));
#21984=CARTESIAN_POINT('Ctrl Pts',(0.139516980595786,0.0563461282555487,
0.95511848479996));
#21985=CARTESIAN_POINT('Ctrl Pts',(0.0283161238170646,0.147777099632969,
0.963057474437267));
#21986=CARTESIAN_POINT('Ctrl Pts',(-0.108806203685475,0.103928264122473,
0.970996464074573));
#21987=CARTESIAN_POINT('Ctrl Pts',(-0.146323908690103,-0.0350597745230392,
0.978935453711877));
#21988=CARTESIAN_POINT('Ctrl Pts',(-0.049892103521326,-0.14195299239598,
0.986874443349185));
#21989=CARTESIAN_POINT('Ctrl Pts',(0.0922125030920605,-0.118897974404329,
0.994813432986488));
#21990=CARTESIAN_POINT('Ctrl Pts',(0.149902882860231,0.0129999905441286,
1.0027524226238));
#21991=CARTESIAN_POINT('Ctrl Pts',(0.0703674468853664,0.132997355096976,
1.0106914122611));
#21992=CARTESIAN_POINT('Ctrl Pts',(-0.0735845641169637,0.131244755962562,
1.01863040189841));
#21993=CARTESIAN_POINT('Ctrl Pts',(-0.150174949749745,0.00934657753497952,
1.02656939153571));
#21994=CARTESIAN_POINT('Ctrl Pts',(-0.0892904610481016,-0.121107752063083,
1.03450838117302));
#21995=CARTESIAN_POINT('Ctrl Pts',(0.0533333252681307,-0.140696234703703,
1.04244737081032));
#21996=CARTESIAN_POINT('Ctrl Pts',(0.147134107472884,-0.031486957015783,
1.05038636044763));
#21997=CARTESIAN_POINT('Ctrl Pts',(0.106243698045146,0.106546471877992,
1.05832535008494));
#21998=CARTESIAN_POINT('Ctrl Pts',(-0.0319055355867657,0.147043907874068,
1.06626433972224));
#21999=CARTESIAN_POINT('Ctrl Pts',(-0.14084743801815,0.0529327237885883,
1.07420332935955));
#22000=CARTESIAN_POINT('Ctrl Pts',(-0.120853163849259,-0.0896347412088629,
1.08214231899685));
#22001=CARTESIAN_POINT('Ctrl Pts',(0.00977389921538986,-0.150147743699608,
1.09008130863416));
#22002=CARTESIAN_POINT('Ctrl Pts',(0.13145362739741,-0.0732107771302755,
1.09802029827146));
#22003=CARTESIAN_POINT('Ctrl Pts',(0.132796568802552,0.0707456384395876,
1.10595928790877));
#22004=CARTESIAN_POINT('Ctrl Pts',(0.0125733526121963,0.149939270533256,
1.11389827754607));
#22005=CARTESIAN_POINT('Ctrl Pts',(-0.119159906186493,0.0918737764630459,
1.12183726718338));
#22006=CARTESIAN_POINT('Ctrl Pts',(-0.141810437433163,-0.0502958634379693,
1.12977625682069));
#22007=CARTESIAN_POINT('Ctrl Pts',(-0.0346432321137694,-0.146423087362162,
1.13771524645799));
#22008=CARTESIAN_POINT('Ctrl Pts',(0.104237477950025,-0.108510009835838,
1.1456542360953));
#22009=CARTESIAN_POINT('Ctrl Pts',(0.147695920811486,0.0287365450185451,
1.1535932257326));
#22010=CARTESIAN_POINT('Ctrl Pts',(0.0559488704325515,0.139676762352502,
1.16153221536991));
#22011=CARTESIAN_POINT('Ctrl Pts',(-0.0870155364008756,0.12275247642644,
1.16947120500722));
#22012=CARTESIAN_POINT('Ctrl Pts',(-0.150323183223479,-0.00654328889139735,
1.17741019464452));
#22013=CARTESIAN_POINT('Ctrl Pts',(-0.0760202581255566,-0.129849121670035,
1.18534918428183));
#22014=CARTESIAN_POINT('Ctrl Pts',(0.0678740032777675,-0.134286982701248,
1.19328817391913));
#22015=CARTESIAN_POINT('Ctrl Pts',(0.149634266389533,-0.0157943143574443,
1.20122716355644));
#22016=CARTESIAN_POINT('Ctrl Pts',(0.0944146137277022,0.117156966325547,
1.20916615319374));
#22017=CARTESIAN_POINT('Ctrl Pts',(-0.047235147145783,0.142859073628774,
1.21710514283105));
#22018=CARTESIAN_POINT('Ctrl Pts',(-0.145644368043342,0.037783489796601,
1.22504413246835));
#22019=CARTESIAN_POINT('Ctrl Pts',(-0.11072615165767,-0.101880289472715,
1.23298312210566));
#22020=CARTESIAN_POINT('Ctrl Pts',(0.0255542680118797,-0.148279646041953,
1.24092211174296));
#22021=CARTESIAN_POINT('Ctrl Pts',(0.138441506664824,-0.0589391489276913,
1.24886110138027));
#22022=CARTESIAN_POINT('Ctrl Pts',(0.124595033982396,0.0843560996663564,
1.25680009101758));
#22023=CARTESIAN_POINT('Ctrl Pts',(-0.00330965325590636,0.150429120316621,
1.26473908065488));
#22024=CARTESIAN_POINT('Ctrl Pts',(-0.128184579763139,0.0787945908985174,
1.27267807029219));
#22025=CARTESIAN_POINT('Ctrl Pts',(-0.135715308561414,-0.0649709863423027,
1.2806170599295));
#22026=CARTESIAN_POINT('Ctrl Pts',(-0.0190079735469551,-0.149260078337129,
1.2885560495668));
#22027=CARTESIAN_POINT('Ctrl Pts',(0.115099858543875,-0.0969117980795561,
1.29649503920411));
#22028=CARTESIAN_POINT('Ctrl Pts',(0.143841658454547,0.0441525915281748,
1.30443402884141));
#22029=CARTESIAN_POINT('Ctrl Pts',(0.0409062781470196,0.144798309552134,
1.31237301847872));
#22030=CARTESIAN_POINT('Ctrl Pts',(-0.0994759962839106,0.112891098884786,
1.32031200811602));
#22031=CARTESIAN_POINT('Ctrl Pts',(-0.148794813708878,-0.0223601759313527,
1.32825099775333));
#22032=CARTESIAN_POINT('Ctrl Pts',(-0.0619021766503053,-0.13714224202644,
1.33618998739064));
#22033=CARTESIAN_POINT('Ctrl Pts',(0.0816576604940555,-0.126379984705639,
1.34412897702794));
#22034=CARTESIAN_POINT('Ctrl Pts',(0.150465506209006,7.4487583413377E-5,
1.35206796666525));
#22035=CARTESIAN_POINT('Ctrl Pts',(0.0815324923277053,0.126460770918471,
1.36000695630255));
#22036=CARTESIAN_POINT('Ctrl Pts',(-0.062037929094705,0.137080886684378,
1.36794594593986));
#22037=CARTESIAN_POINT('Ctrl Pts',(-0.148816880822527,0.0222128430196456,
1.37588493557716));
#22038=CARTESIAN_POINT('Ctrl Pts',(-0.0993641722043223,-0.112989531455785,
1.38382392521447));
#22039=CARTESIAN_POINT('Ctrl Pts',(0.0410496166270677,-0.144757742348562,
1.39176291485178));
#22040=CARTESIAN_POINT('Ctrl Pts',(0.143885312916173,-0.0440101443352923,
1.39970190448908));
#22041=CARTESIAN_POINT('Ctrl Pts',(0.115003831846793,0.0970256929337524,
1.40764089412639));
#22042=CARTESIAN_POINT('Ctrl Pts',(-0.0191557100743377,0.149241218055048,
1.41557988376369));
#22043=CARTESIAN_POINT('Ctrl Pts',(-0.135779636557791,0.0648365220611291,
1.423518873401));
#22044=CARTESIAN_POINT('Ctrl Pts',(-0.128106375355825,-0.0789213496179777,
1.4314578630383));
#22045=CARTESIAN_POINT('Ctrl Pts',(-0.00316095527563228,-0.150432546011701,
1.43939685267561));
#22046=CARTESIAN_POINT('Ctrl Pts',(0.12467895337041,-0.0842322751882648,
1.44733584231291));
#22047=CARTESIAN_POINT('Ctrl Pts',(0.138382210043398,0.0590753877074232,
1.45527483195022));
#22048=CARTESIAN_POINT('Ctrl Pts',(0.0254091034322018,0.148306397458819,
1.46321382158753));
#22049=CARTESIAN_POINT('Ctrl Pts',(-0.110830116988615,0.101767718932792,
1.47115281122483));
#22050=CARTESIAN_POINT('Ctrl Pts',(-0.145600909330124,-0.0379221829034233,
1.47909180086214));
#22051=CARTESIAN_POINT('Ctrl Pts',(-0.0471050325108872,-0.142916194795756,
1.48703079049945));
#22052=CARTESIAN_POINT('Ctrl Pts',(0.0945521370959566,-0.117043625665234,
1.49496978013675));
#22053=CARTESIAN_POINT('Ctrl Pts',(0.14957741911039,0.0159047428854941,
1.50290876977406));
#22054=CARTESIAN_POINT('Ctrl Pts',(0.0678206238522695,0.134426714629862,
1.51084775941136));
#22055=CARTESIAN_POINT('Ctrl Pts',(-0.0763126473618499,0.129627546381738,
1.51878674904867));
#22056=CARTESIAN_POINT('Ctrl Pts',(-0.125385920115907,0.0477050348167321,
1.52407940880687));
#22057=CARTESIAN_POINT('Ctrl Pts',(-0.127184992207234,0.00540996832206346,
1.52672573868597));
#22058=CARTESIAN_POINT('Ctrl Pts',(0.0684664424539414,-0.095829519891843,
-1.38777878078145E-17));
#22059=CARTESIAN_POINT('Ctrl Pts',(0.100334321247169,-0.0730611673843044,
0.00264632987910189));
#22060=CARTESIAN_POINT('Ctrl Pts',(0.139021564822767,0.00636891437108143,
0.00793898963730573));
#22061=CARTESIAN_POINT('Ctrl Pts',(0.0699018669780613,0.120491966796142,
0.0158779792746114));
#22062=CARTESIAN_POINT('Ctrl Pts',(-0.0632645460347191,0.123954346655885,
0.0238169689119172));
#22063=CARTESIAN_POINT('Ctrl Pts',(-0.138486976988987,0.0141253725679007,
0.0317559585492228));
#22064=CARTESIAN_POINT('Ctrl Pts',(-0.0869496735326521,-0.108728403071097,
0.0396949481865287));
#22065=CARTESIAN_POINT('Ctrl Pts',(0.0441923146003338,-0.131999388615902,
0.0476339378238343));
#22066=CARTESIAN_POINT('Ctrl Pts',(0.134874939024977,-0.034459980695041,
0.0555729274611401));
#22067=CARTESIAN_POINT('Ctrl Pts',(0.102091080224759,0.094638871230671,
0.0635119170984456));
#22068=CARTESIAN_POINT('Ctrl Pts',(-0.0241513666277066,0.137095110112719,
0.0714509067357516));
#22069=CARTESIAN_POINT('Ctrl Pts',(-0.128284260007319,0.0540539703915629,
0.0793898963730571));
#22070=CARTESIAN_POINT('Ctrl Pts',(-0.114982038412656,-0.0784718756714057,
0.0873288860103631));
#22071=CARTESIAN_POINT('Ctrl Pts',(0.00357853460314598,-0.139161043603659,
0.0952678756476685));
#22072=CARTESIAN_POINT('Ctrl Pts',(0.118863112008681,-0.0724583686054966,
0.103206865284975));
#22073=CARTESIAN_POINT('Ctrl Pts',(0.125336705278751,0.0605752693714656,
0.11114585492228));
#22074=CARTESIAN_POINT('Ctrl Pts',(0.0170731091066207,0.138156245709763,
0.119084844559586));
#22075=CARTESIAN_POINT('Ctrl Pts',(-0.106819734848208,0.0892647286947484,
0.127023834196891));
#22076=CARTESIAN_POINT('Ctrl Pts',(-0.132926439498961,-0.0413425724611633,
0.134962823834197));
#22077=CARTESIAN_POINT('Ctrl Pts',(-0.0373480950846616,-0.134103559412242,
0.142901813471503));
#22078=CARTESIAN_POINT('Ctrl Pts',(0.0924198687735613,-0.104101940294199,
0.150840803108809));
#22079=CARTESIAN_POINT('Ctrl Pts',(0.137583777756591,0.0211978768359354,
0.158779792746114));
#22080=CARTESIAN_POINT('Ctrl Pts',(0.0567991668878991,0.127092487218924,
0.16671878238342));
#22081=CARTESIAN_POINT('Ctrl Pts',(-0.075981188277068,0.116642637502503,
0.174657772020726));
#22082=CARTESIAN_POINT('Ctrl Pts',(-0.139205973057234,-0.000585553717998882,
0.182596761658032));
#22083=CARTESIAN_POINT('Ctrl Pts',(-0.0749972298318695,-0.11727771015962,
0.190535751295337));
#22084=CARTESIAN_POINT('Ctrl Pts',(0.0578663373665801,-0.126610160769685,
0.198474740932643));
#22085=CARTESIAN_POINT('Ctrl Pts',(0.13775723856723,-0.0200396862227523,
0.206413730569949));
#22086=CARTESIAN_POINT('Ctrl Pts',(0.091540828968026,0.104875747581476,
0.214352720207254));
#22087=CARTESIAN_POINT('Ctrl Pts',(-0.0384749358425138,0.133784622116252,
0.22229170984456));
#22088=CARTESIAN_POINT('Ctrl Pts',(-0.133269533752038,0.0402228439430644,
0.230230699481866));
#22089=CARTESIAN_POINT('Ctrl Pts',(-0.106065007067505,-0.0901601911982067,
0.238169689119172));
#22090=CARTESIAN_POINT('Ctrl Pts',(0.0182347644767634,-0.138007750384372,
0.246108678756477));
#22091=CARTESIAN_POINT('Ctrl Pts',(0.125841858853055,-0.0595186723796334,
0.254047668393783));
#22092=CARTESIAN_POINT('Ctrl Pts',(0.118249355954961,0.073455671106145,
0.261986658031089));
#22093=CARTESIAN_POINT('Ctrl Pts',(0.00240767183786234,0.139186381940956,
0.269925647668394));
#22094=CARTESIAN_POINT('Ctrl Pts',(-0.115638070838342,0.0775014991741366,
0.277864637305701));
#22095=CARTESIAN_POINT('Ctrl Pts',(-0.12782508485658,-0.0551306945617612,
0.285803626943006));
#22096=CARTESIAN_POINT('Ctrl Pts',(-0.0229969941138309,-0.137294515779738,
0.293742616580312));
#22097=CARTESIAN_POINT('Ctrl Pts',(0.102883268653204,-0.0937746172089793,
0.301681606217617));
#22098=CARTESIAN_POINT('Ctrl Pts',(0.134580950019115,0.0355895166223291,
0.309620595854923));
#22099=CARTESIAN_POINT('Ctrl Pts',(0.0430789950773988,0.13237388709478,
0.317559585492229));
#22100=CARTESIAN_POINT('Ctrl Pts',(-0.0878588274613298,0.107979036106918,
0.325498575129534));
#22101=CARTESIAN_POINT('Ctrl Pts',(-0.1383679148179,-0.0152632221501787,
0.33343756476684));
#22102=CARTESIAN_POINT('Ctrl Pts',(-0.0622106591311991,-0.12453304658572,
0.341376554404146));
#22103=CARTESIAN_POINT('Ctrl Pts',(0.0708961914151981,-0.119801401679107,
0.349315544041452));
#22104=CARTESIAN_POINT('Ctrl Pts',(0.1391024375543,-0.00539978406154301,
0.357254533678757));
#22105=CARTESIAN_POINT('Ctrl Pts',(0.0799699354250877,0.113944965792994,
0.365193523316063));
#22106=CARTESIAN_POINT('Ctrl Pts',(-0.0523695618881846,0.128980908622551,
0.373132512953369));
#22107=CARTESIAN_POINT('Ctrl Pts',(-0.136768314413298,0.0259436692471295,
0.381071502590675));
#22108=CARTESIAN_POINT('Ctrl Pts',(-0.0959650484377783,-0.100843221288265,
0.38901049222798));
#22109=CARTESIAN_POINT('Ctrl Pts',(0.0326876424682324,-0.135315053971568,
0.396949481865287));
#22110=CARTESIAN_POINT('Ctrl Pts',(0.13141703692502,-0.0459152284901983,
0.404888471502591));
#22111=CARTESIAN_POINT('Ctrl Pts',(0.109843140674695,0.0855168418978295,
0.412827461139898));
#22112=CARTESIAN_POINT('Ctrl Pts',(-0.0122846228212416,0.13866410438033,
0.420766450777203));
#22113=CARTESIAN_POINT('Ctrl Pts',(-0.123166656044517,0.0648738825743514,
0.428705440414509));
#22114=CARTESIAN_POINT('Ctrl Pts',(-0.121298056821252,-0.0683039326309071,
0.436644430051815));
#22115=CARTESIAN_POINT('Ctrl Pts',(-0.00838939967687663,-0.138954178686792,
0.44458341968912));
#22116=CARTESIAN_POINT('Ctrl Pts',(0.11219917790857,-0.0824013973067221,
0.452522409326426));
#22117=CARTESIAN_POINT('Ctrl Pts',(0.13007709763057,0.0495842159710775,
0.460461398963732));
#22118=CARTESIAN_POINT('Ctrl Pts',(0.0288783492374893,0.136178877755608,
0.468400388601037));
#22119=CARTESIAN_POINT('Ctrl Pts',(-0.0987565487199846,0.0981111099028881,
0.476339378238344));
#22120=CARTESIAN_POINT('Ctrl Pts',(-0.135986594552616,-0.0297706550724338,
0.484278367875649));
#22121=CARTESIAN_POINT('Ctrl Pts',(-0.0487302328423073,-0.130399425645183,
0.492217357512954));
#22122=CARTESIAN_POINT('Ctrl Pts',(0.0831353173341669,-0.111656458896056,
0.50015634715026));
#22123=CARTESIAN_POINT('Ctrl Pts',(0.13889618212661,0.00930034365552528,
0.508095336787567));
#22124=CARTESIAN_POINT('Ctrl Pts',(0.0675071113591811,0.12174331898465,
0.516034326424871));
#22125=CARTESIAN_POINT('Ctrl Pts',(-0.0656800932930844,0.122738629397884,
0.523973316062178));
#22126=CARTESIAN_POINT('Ctrl Pts',(-0.138741673886299,0.0113751364249866,
0.531912305699483));
#22127=CARTESIAN_POINT('Ctrl Pts',(-0.0847947606245053,-0.110401514355972,
0.539851295336789));
#22128=CARTESIAN_POINT('Ctrl Pts',(0.0467759446245483,-0.131113145053959,
0.547790284974095));
#22129=CARTESIAN_POINT('Ctrl Pts',(0.135526478334676,-0.031799677225719,
0.555729274611401));
#22130=CARTESIAN_POINT('Ctrl Pts',(0.100211809365564,0.0966242157284558,
0.563668264248707));
#22131=CARTESIAN_POINT('Ctrl Pts',(-0.0268399031138932,0.136595261273209,
0.571607253886012));
#22132=CARTESIAN_POINT('Ctrl Pts',(-0.129321523751272,0.0515227066069736,
0.579546243523318));
#22133=CARTESIAN_POINT('Ctrl Pts',(-0.113418152377209,-0.0807153548762533,
0.587485233160623));
#22134=CARTESIAN_POINT('Ctrl Pts',(0.00631176444456456,-0.139064040754811,
0.595424222797929));
#22135=CARTESIAN_POINT('Ctrl Pts',(0.120263693490807,-0.0701091280034811,
0.603363212435234));
#22136=CARTESIAN_POINT('Ctrl Pts',(0.124122453355413,0.0630258865426945,
0.611302202072541));
#22137=CARTESIAN_POINT('Ctrl Pts',(0.0143556138404206,0.138465021405133,
0.619241191709845));
#22138=CARTESIAN_POINT('Ctrl Pts',(-0.108552806291007,0.0871489187988374,
0.627180181347153));
#22139=CARTESIAN_POINT('Ctrl Pts',(-0.132088571872698,-0.043946046262323,
0.635119170984457));
#22140=CARTESIAN_POINT('Ctrl Pts',(-0.0347063025259737,-0.134811417789573,
0.643058160621763));
#22141=CARTESIAN_POINT('Ctrl Pts',(0.0944472082050275,-0.102266175560326,
0.65099715025907));
#22142=CARTESIAN_POINT('Ctrl Pts',(0.137140772714236,0.0238967416356601,
0.658936139896373));
#22143=CARTESIAN_POINT('Ctrl Pts',(0.054291358674537,0.128183829614862,
0.666875129533682));
#22144=CARTESIAN_POINT('Ctrl Pts',(-0.0782580734018908,0.115127406593233,
0.674814119170985));
#22145=CARTESIAN_POINT('Ctrl Pts',(-0.139167602654929,-0.00332026696803425,
0.682753108808293));
#22146=CARTESIAN_POINT('Ctrl Pts',(-0.0726787294560835,-0.118728463672822,
0.690692098445597));
#22147=CARTESIAN_POINT('Ctrl Pts',(0.0603425395611779,-0.125448888878168,
0.698631088082904));
#22148=CARTESIAN_POINT('Ctrl Pts',(0.138124349154501,-0.0173294538893964,
0.706570077720209));
#22149=CARTESIAN_POINT('Ctrl Pts',(0.0894627833767505,0.106653908470079,
0.714509067357515));
#22150=CARTESIAN_POINT('Ctrl Pts',(-0.0410958292974484,0.133002927094911,
0.72244805699482));
#22151=CARTESIAN_POINT('Ctrl Pts',(-0.134034026730954,0.0375968812502473,
0.730387046632127));
#22152=CARTESIAN_POINT('Ctrl Pts',(-0.104273258644039,-0.0922265326964679,
0.738326036269432));
#22153=CARTESIAN_POINT('Ctrl Pts',(0.0209425314183671,-0.137622876656644,
0.746265025906738));
#22154=CARTESIAN_POINT('Ctrl Pts',(0.126986869252672,-0.0570349089493802,
0.754204015544043));
#22155=CARTESIAN_POINT('Ctrl Pts',(0.11678343126468,0.0757646090434518,
0.762143005181349));
#22156=CARTESIAN_POINT('Ctrl Pts',(-0.000327234354877375,0.139206819944772,
0.770081994818654));
#22157=CARTESIAN_POINT('Ctrl Pts',(-0.117138339349379,0.0752147276530931,
0.778020984455961));
#22158=CARTESIAN_POINT('Ctrl Pts',(-0.126717322684213,-0.0576312930030564,
0.785959974093266));
#22159=CARTESIAN_POINT('Ctrl Pts',(-0.0202952816069424,-0.137719814645367,
0.793898963730571));
#22160=CARTESIAN_POINT('Ctrl Pts',(0.104705698854998,-0.0917352845351548,
0.801837953367879));
#22161=CARTESIAN_POINT('Ctrl Pts',(0.133855787965376,0.0382266115373486,
0.809776943005182));
#22162=CARTESIAN_POINT('Ctrl Pts',(0.0404700769297216,0.133194664588195,
0.81771593264249));
#22163=CARTESIAN_POINT('Ctrl Pts',(-0.0899632159395838,0.106232130635072,
0.825654922279794));
#22164=CARTESIAN_POINT('Ctrl Pts',(-0.13804135019805,-0.0179786383510676,
0.833593911917101));
#22165=CARTESIAN_POINT('Ctrl Pts',(-0.059752088941783,-0.125731196083361,
0.841532901554406));
#22166=CARTESIAN_POINT('Ctrl Pts',(0.0732361146625898,-0.118385460722959,
0.849471891191712));
#22167=CARTESIAN_POINT('Ctrl Pts',(0.139181674492094,-0.00266594955618734,
0.857410880829018));
#22168=CARTESIAN_POINT('Ctrl Pts',(0.077715950067195,0.115494055719818,
0.865349870466323));
#22169=CARTESIAN_POINT('Ctrl Pts',(-0.0548934004223171,0.127927168308903,
0.87328886010363));
#22170=CARTESIAN_POINT('Ctrl Pts',(-0.137251604915624,0.0232517257326144,
0.881227849740934));
#22171=CARTESIAN_POINT('Ctrl Pts',(-0.0939653715754795,-0.102709078207047,
0.889166839378241));
#22172=CARTESIAN_POINT('Ctrl Pts',(0.0353397195745277,-0.134646760160997,
0.897105829015547));
#22173=CARTESIAN_POINT('Ctrl Pts',(0.132293719443212,-0.0433245611326863,
0.905044818652852));
#22174=CARTESIAN_POINT('Ctrl Pts',(0.108141885842356,0.0876583043865096,
0.912983808290157));
#22175=CARTESIAN_POINT('Ctrl Pts',(-0.0150064327997127,0.138395999855801,
0.920922797927463));
#22176=CARTESIAN_POINT('Ctrl Pts',(-0.124417390671652,0.0624416423544169,
0.928861787564769));
#22177=CARTESIAN_POINT('Ctrl Pts',(-0.119932754264349,-0.0706737593172073,
0.936800777202075));
#22178=CARTESIAN_POINT('Ctrl Pts',(-0.00565790085648466,-0.139092177922979,
0.944739766839381));
#22179=CARTESIAN_POINT('Ctrl Pts',(0.113796373024222,-0.0801812402497705,
0.952678756476687));
#22180=CARTESIAN_POINT('Ctrl Pts',(0.129077866376032,0.0521301276928276,
0.960617746113992));
#22181=CARTESIAN_POINT('Ctrl Pts',(0.026197419344502,0.13671993644362,0.968556735751298));
#22182=CARTESIAN_POINT('Ctrl Pts',(-0.100664969670515,0.0961520134094621,
0.976495725388603));
#22183=CARTESIAN_POINT('Ctrl Pts',(-0.13537547797311,-0.0324364881732178,
0.98443471502591));
#22184=CARTESIAN_POINT('Ctrl Pts',(-0.0461590140787468,-0.131331607851033,
0.992373704663214));
#22185=CARTESIAN_POINT('Ctrl Pts',(0.0853128637208732,-0.110001641284132,
1.00031269430052));
#22186=CARTESIAN_POINT('Ctrl Pts',(0.138686661656432,0.0120272889735618,
1.00825168393783));
#22187=CARTESIAN_POINT('Ctrl Pts',(0.0651023256631918,0.123046060459907,
1.01619067357513));
#22188=CARTESIAN_POINT('Ctrl Pts',(-0.0680787277209358,0.121424596492465,
1.02412966321244));
#22189=CARTESIAN_POINT('Ctrl Pts',(-0.138938371616466,0.00864723620724691,
1.03206865284975));
#22190=CARTESIAN_POINT('Ctrl Pts',(-0.0826094583655966,-0.112046076191904,
1.04000764248705));
#22191=CARTESIAN_POINT('Ctrl Pts',(0.0493427524230464,-0.130168884856471,
1.04794663212436));
#22192=CARTESIAN_POINT('Ctrl Pts',(0.136125055048066,-0.0291310004912345,
1.05588562176166));
#22193=CARTESIAN_POINT('Ctrl Pts',(0.0982941990358779,0.0985743183458784,
1.06382461139897));
#22194=CARTESIAN_POINT('Ctrl Pts',(-0.0295182596522469,0.136041604476578,
1.07176360103627));
#22195=CARTESIAN_POINT('Ctrl Pts',(-0.130308774647192,0.0489721252490281,
1.07970259067358));
#22196=CARTESIAN_POINT('Ctrl Pts',(-0.111810537096203,-0.0829279783650712,
1.08764158031088));
#22197=CARTESIAN_POINT('Ctrl Pts',(0.00904258428980543,-0.13891320121148,
1.09558056994819));
#22198=CARTESIAN_POINT('Ctrl Pts',(0.121617839487272,-0.067732908692211,
1.1035195595855));
#22199=CARTESIAN_POINT('Ctrl Pts',(0.122860297649024,0.0654522196953821,
1.1114585492228));
#22200=CARTESIAN_POINT('Ctrl Pts',(0.0116325734791967,0.138720326685422,
1.11939753886011));
#22201=CARTESIAN_POINT('Ctrl Pts',(-0.110243974478508,0.0849994817198388,
1.12733652849741));
#22202=CARTESIAN_POINT('Ctrl Pts',(-0.131199719314147,-0.0465325633653302,
1.13527551813472));
#22203=CARTESIAN_POINT('Ctrl Pts',(-0.0320511128216771,-0.13546723577438,
1.14321450777202));
#22204=CARTESIAN_POINT('Ctrl Pts',(0.0964380908528195,-0.100390938007982,
1.15115349740933));
#22205=CARTESIAN_POINT('Ctrl Pts',(0.136644831685568,0.0265863832644056,
1.15909248704664));
#22206=CARTESIAN_POINT('Ctrl Pts',(0.0517625939920979,0.129225692742072,
1.16703147668394));
#22207=CARTESIAN_POINT('Ctrl Pts',(-0.0805047509788913,0.113567736929491,
1.17497046632125));
#22208=CARTESIAN_POINT('Ctrl Pts',(-0.139075513779617,-0.00605369873671642,
1.18290945595855));
#22209=CARTESIAN_POINT('Ctrl Pts',(-0.0703321751825429,-0.12013338809653,
1.19084844559586));
#22210=CARTESIAN_POINT('Ctrl Pts',(0.0627954496153871,-0.124239193932754,
1.19878743523316));
#22211=CARTESIAN_POINT('Ctrl Pts',(0.138438143943654,-0.0146125323915816,
1.20672642487047));
#22212=CARTESIAN_POINT('Ctrl Pts',(0.0873502052771435,0.108390901091839,
1.21466541450777));
#22213=CARTESIAN_POINT('Ctrl Pts',(-0.043700859820065,0.132169893139269,
1.22260440414508));
#22214=CARTESIAN_POINT('Ctrl Pts',(-0.134746782767514,0.0349564062120582,
1.23054339378239));
#22215=CARTESIAN_POINT('Ctrl Pts',(-0.102441260891455,-0.0942572748833364,
1.23848238341969));
#22216=CARTESIAN_POINT('Ctrl Pts',(0.0236422145726536,-0.137184880695923,
1.246421373057));
#22217=CARTESIAN_POINT('Ctrl Pts',(0.128082862902196,-0.0545291301253663,
1.2543603626943));
#22218=CARTESIAN_POINT('Ctrl Pts',(0.115272428336817,0.0780443019497631,
1.26229935233161));
#22219=CARTESIAN_POINT('Ctrl Pts',(-0.00306201423577413,0.139173524314926,
1.27023834196891));
#22220=CARTESIAN_POINT('Ctrl Pts',(-0.118593392628464,0.0728989233548558,
1.27817733160622));
#22221=CARTESIAN_POINT('Ctrl Pts',(-0.125560647806918,-0.06010964584811,
1.28611632124353));
#22222=CARTESIAN_POINT('Ctrl Pts',(-0.0175857351491984,-0.138091953858251,
1.29405531088083));
#22223=CARTESIAN_POINT('Ctrl Pts',(0.106487712804436,-0.089660542174548,
1.30199430051814));
#22224=CARTESIAN_POINT('Ctrl Pts',(0.133078957772855,0.0408489510387311,
1.30993329015544));
#22225=CARTESIAN_POINT('Ctrl Pts',(0.0378455373822902,0.133964029124136,
1.31787227979275));
#22226=CARTESIAN_POINT('Ctrl Pts',(-0.0920328787300654,0.104444219726284,
1.32581126943006));
#22227=CARTESIAN_POINT('Ctrl Pts',(-0.137661501842601,-0.0206871148492911,
1.33375025906736));
#22228=CARTESIAN_POINT('Ctrl Pts',(-0.0572704544775333,-0.126880813469472,
1.34168924870467));
#22229=CARTESIAN_POINT('Ctrl Pts',(0.0755477687720905,-0.116923823242002,
1.34962823834197));
#22230=CARTESIAN_POINT('Ctrl Pts',(0.13920718769651,6.89141801743488E-5,
1.35756722797928));
#22231=CARTESIAN_POINT('Ctrl Pts',(0.0754319660950179,0.116998564767658,
1.36550621761658));
#22232=CARTESIAN_POINT('Ctrl Pts',(-0.0573960494825499,0.126824048933643,
1.37344520725389));
#22233=CARTESIAN_POINT('Ctrl Pts',(-0.13768191782304,0.0205508058651932,
1.38138419689119));
#22234=CARTESIAN_POINT('Ctrl Pts',(-0.0919294216917856,-0.104535287252199,
1.3893231865285));
#22235=CARTESIAN_POINT('Ctrl Pts',(0.0379781508110965,-0.133926497290667,
1.39726217616581));
#22236=CARTESIAN_POINT('Ctrl Pts',(0.133119345865688,-0.0407171622080862,
1.40520116580311));
#22237=CARTESIAN_POINT('Ctrl Pts',(0.106398871137127,0.0897659150453452,
1.41314015544042));
#22238=CARTESIAN_POINT('Ctrl Pts',(-0.0177224175491345,0.138074504763813,
1.42107914507772));
#22239=CARTESIAN_POINT('Ctrl Pts',(-0.125620162573399,0.0599852426217579,
1.42901813471503));
#22240=CARTESIAN_POINT('Ctrl Pts',(-0.118521039729242,-0.0730161975746823,
1.43695712435233));
#22241=CARTESIAN_POINT('Ctrl Pts',(-0.00292444232197888,-0.139176693688359,
1.44489611398964));
#22242=CARTESIAN_POINT('Ctrl Pts',(0.115350068603298,-0.0779297424218237,
1.45283510362695));
#22243=CARTESIAN_POINT('Ctrl Pts',(0.128028003046829,0.0546551750765237,
1.46077409326425));
#22244=CARTESIAN_POINT('Ctrl Pts',(0.0235079116789307,0.137209630484779,
1.46871308290156));
#22245=CARTESIAN_POINT('Ctrl Pts',(-0.102537447198224,0.0941531272373115,
1.47665207253886));
#22246=CARTESIAN_POINT('Ctrl Pts',(-0.134706575776555,-0.0350847218495708,
1.48459106217617));
#22247=CARTESIAN_POINT('Ctrl Pts',(-0.0435804807853106,-0.132222740314769,
1.49253005181348));
#22248=CARTESIAN_POINT('Ctrl Pts',(0.0874774386997331,-0.108286040948335,
1.50046904145078));
#22249=CARTESIAN_POINT('Ctrl Pts',(0.138385550162814,0.0147146982980264,
1.50840803108809));
#22250=CARTESIAN_POINT('Ctrl Pts',(0.0627460642121078,0.124368470664037,
1.51634702072539));
#22251=CARTESIAN_POINT('Ctrl Pts',(-0.0706026869052757,0.119928391791904,
1.5242860103627));
#22252=CARTESIAN_POINT('Ctrl Pts',(-0.116004137797729,0.0441355889673283,
1.5295786701209));
#22253=CARTESIAN_POINT('Ctrl Pts',(-0.117668597464313,0.00500517689812487,
1.532225));
#22254=CARTESIAN_POINT('',(0.0684664424539461,-0.0958295198918396,0.));
#22255=CARTESIAN_POINT('Ctrl Pts',(0.0684664424539414,-0.095829519891843,
-1.38777878078145E-17));
#22256=CARTESIAN_POINT('Ctrl Pts',(0.100334321247169,-0.0730611673843044,
0.00264632987910189));
#22257=CARTESIAN_POINT('Ctrl Pts',(0.139021564822767,0.00636891437108143,
0.00793898963730573));
#22258=CARTESIAN_POINT('Ctrl Pts',(0.0699018669780613,0.120491966796142,
0.0158779792746114));
#22259=CARTESIAN_POINT('Ctrl Pts',(-0.0632645460347191,0.123954346655885,
0.0238169689119172));
#22260=CARTESIAN_POINT('Ctrl Pts',(-0.11596266760442,0.0470121293552651,
0.0293787386625077));
#22261=CARTESIAN_POINT('Ctrl Pts',(-0.117944740497024,0.00404481602818191,
0.0322941785339964));
#22262=CARTESIAN_POINT('Ctrl Pts',(-0.117917485785546,7.60014832213644E-5,
0.0325632885263832));
#22263=CARTESIAN_POINT('Ctrl Pts',(0.0635546915223951,0.132092229195826,
-2.16840434497101E-19));
#22264=CARTESIAN_POINT('Ctrl Pts',(0.0668114782730532,0.13015255741457,
-1.00603861447787E-18));
#22265=CARTESIAN_POINT('Ctrl Pts',(0.0699821360194518,0.12808121947321,
-2.9262196004085E-17));
#22266=CARTESIAN_POINT('Ctrl Pts',(0.0730575207853233,0.125877721325919,
-2.71050543121376E-17));
#22267=CARTESIAN_POINT('Ctrl Pts',(0.0789281193465506,0.121671466161783,
-2.36378102375718E-17));
#22268=CARTESIAN_POINT('Ctrl Pts',(0.0844522091809674,0.11698398814956,
1.43782932504085E-18));
#22269=CARTESIAN_POINT('Ctrl Pts',(0.0895990070394484,0.111875963994554,
9.97465998686664E-18));
#22270=CARTESIAN_POINT('Ctrl Pts',(0.0928865546640729,0.108613183302742,
1.54276111490851E-17));
#22271=CARTESIAN_POINT('Ctrl Pts',(0.0960206821069302,0.105176950779614,
-2.53636710091701E-17));
#22272=CARTESIAN_POINT('Ctrl Pts',(0.098978417360439,0.101599719103904,
-1.56125112837913E-17));
#22273=CARTESIAN_POINT('Ctrl Pts',(0.103148772110026,0.0965558852815647,
-1.86354736740503E-18));
#22274=CARTESIAN_POINT('Ctrl Pts',(0.106976174326278,0.0912251680483688,
1.1337629845105E-17));
#22275=CARTESIAN_POINT('Ctrl Pts',(0.110435561611279,0.0856523061447448,
2.03830008427275E-17));
#22276=CARTESIAN_POINT('Ctrl Pts',(0.112407683932559,0.0824753373788608,
2.55395723911076E-17));
#22277=CARTESIAN_POINT('Ctrl Pts',(0.114261188142284,0.0792174064057451,
2.29308760465575E-17));
#22278=CARTESIAN_POINT('Ctrl Pts',(0.115986535786665,0.0758936579718971,
2.08166817117217E-17));
#22279=CARTESIAN_POINT('Ctrl Pts',(0.120573220307724,0.0670577659456877,
1.51962825639422E-17));
#22280=CARTESIAN_POINT('Ctrl Pts',(0.124235263225439,0.0578042025119142,
2.52358375750583E-18));
#22281=CARTESIAN_POINT('Ctrl Pts',(0.126883306113679,0.0482911783993335,
1.30104260698261E-17));
#22282=CARTESIAN_POINT('Ctrl Pts',(0.128478610866444,0.0425600882242624,
1.93281898253259E-17));
#22283=CARTESIAN_POINT('Ctrl Pts',(0.129704960854084,0.0367345196138549,
-5.78096029915021E-19));
#22284=CARTESIAN_POINT('Ctrl Pts',(0.130533291754837,0.0308494671050701,
0.));
#22285=CARTESIAN_POINT('Ctrl Pts',(0.131003715791213,0.0275072397983871,
3.2831114661813E-19));
#22286=CARTESIAN_POINT('Ctrl Pts',(0.131345346899704,0.0241444941465381,
-1.7128612844445E-18));
#22287=CARTESIAN_POINT('Ctrl Pts',(0.131551728167405,0.0207857616715298,
2.60208521396521E-18));
#22288=CARTESIAN_POINT('Ctrl Pts',(0.131851321606701,0.0159100565018035,
8.86587880453295E-18));
#22289=CARTESIAN_POINT('Ctrl Pts',(0.131867617692795,0.0110341713389591,
-1.68111772803455E-17));
#22290=CARTESIAN_POINT('Ctrl Pts',(0.131586936334964,0.0061777758930637,
-6.93889390390723E-18));
#22291=CARTESIAN_POINT('Ctrl Pts',(0.131099036368572,-0.00226395031615145,
9.98510028643051E-18));
#22292=CARTESIAN_POINT('Ctrl Pts',(0.129715139118287,-0.0106479390144509,
1.03491660509995E-17));
#22293=CARTESIAN_POINT('Ctrl Pts',(0.127493709984164,-0.018859987399606,
1.04083408558608E-17));
#22294=CARTESIAN_POINT('Ctrl Pts',(0.126553994220251,-0.0223338732882013,
1.04333731632617E-17));
#22295=CARTESIAN_POINT('Ctrl Pts',(0.125463061762623,-0.0257782540966497,
1.75224609115742E-17));
#22296=CARTESIAN_POINT('Ctrl Pts',(0.124232565886791,-0.0291638780753137,
1.73472347597681E-17));
#22297=CARTESIAN_POINT('Ctrl Pts',(0.12170396813588,-0.0361211392462112,
1.69871551674183E-17));
#22298=CARTESIAN_POINT('Ctrl Pts',(0.118582485980247,-0.0428512226170345,
-6.45748389186585E-19));
#22299=CARTESIAN_POINT('Ctrl Pts',(0.114911168983798,-0.0492778939609075,
3.46944695195361E-18));
#22300=CARTESIAN_POINT('Ctrl Pts',(0.112347970921096,-0.0537647937721124,
6.34254691478841E-18));
#22301=CARTESIAN_POINT('Ctrl Pts',(0.109516356061708,-0.0581036184196785,
-1.05628593522785E-17));
#22302=CARTESIAN_POINT('Ctrl Pts',(0.106427098863261,-0.0622637901458048,
-1.21430643318376E-17));
#22303=CARTESIAN_POINT('Ctrl Pts',(0.104287070791936,-0.0651456752410043,
-1.32377232732828E-17));
#22304=CARTESIAN_POINT('Ctrl Pts',(0.102021590876101,-0.067943056099314,
-1.03088264066386E-17));
#22305=CARTESIAN_POINT('Ctrl Pts',(0.0996491962474235,-0.0706287444932102,
-1.04083408558608E-17));
#22306=CARTESIAN_POINT('Ctrl Pts',(0.0938611946766418,-0.0771810981592459,
-1.06511292104842E-17));
#22307=CARTESIAN_POINT('Ctrl Pts',(0.0874218747326319,-0.0830961188460978,
9.460259835177E-18));
#22308=CARTESIAN_POINT('Ctrl Pts',(0.0803902102994179,-0.0882260767030795,
2.94902990916057E-17));
#22309=CARTESIAN_POINT('Ctrl Pts',(0.0765868618375105,-0.091000813397402,
4.03243227742548E-17));
#22310=CARTESIAN_POINT('Ctrl Pts',(0.0726097989303321,-0.0935451549285004,
-2.49510848448888E-18));
#22311=CARTESIAN_POINT('Ctrl Pts',(0.0684664424539416,-0.0958295198918429,
0.));
#22312=CARTESIAN_POINT('Ctrl Pts',(-0.00156962371674571,0.146072546381438,
1.50365));
#22313=CARTESIAN_POINT('Ctrl Pts',(0.0218361081466035,0.146362061217761,
1.50238307892777));
#22314=CARTESIAN_POINT('Ctrl Pts',(0.0452966847593804,0.141345883428421,
1.50111615785553));
#22315=CARTESIAN_POINT('Ctrl Pts',(0.0660179268768178,0.130913916311315,
1.4998492367833));
#22316=CARTESIAN_POINT('Ctrl Pts',(0.109300214423576,0.109123745727819,
1.4972029069042));
#22317=CARTESIAN_POINT('Ctrl Pts',(0.140630685714559,0.0637042888941242,
1.49455657702509));
#22318=CARTESIAN_POINT('Ctrl Pts',(0.145752650840527,0.0155206226173656,
1.49191024714599));
#22319=CARTESIAN_POINT('Ctrl Pts',(0.150874615966495,-0.0326630436593903,
1.48926391726689));
#22320=CARTESIAN_POINT('Ctrl Pts',(0.129788074927449,-0.0836109193792113,
1.48661758738779));
#22321=CARTESIAN_POINT('Ctrl Pts',(0.0921021927661857,-0.114042242015571,
1.48397125750869));
#22322=CARTESIAN_POINT('Ctrl Pts',(0.0544163106049216,-0.144473564651931,
1.48132492762959));
#22323=CARTESIAN_POINT('Ctrl Pts',(0.000131087321441313,-0.154388334204831,
1.47867859775048));
#22324=CARTESIAN_POINT('Ctrl Pts',(-0.0458840977328367,-0.139228052523514,
1.47603226787138));
#22325=CARTESIAN_POINT('Ctrl Pts',(-0.0918992827871148,-0.124067770842196,
1.47338593799228));
#22326=CARTESIAN_POINT('Ctrl Pts',(-0.129644429612189,-0.0838324379266627,
1.47073960811318));
#22327=CARTESIAN_POINT('Ctrl Pts',(-0.141854649713415,-0.0369491035797489,
1.46809327823408));
#22328=CARTESIAN_POINT('Ctrl Pts',(-0.14497337938942,-0.0249741805295802,
1.46741735368415));
#22329=CARTESIAN_POINT('Ctrl Pts',(-0.146426231435716,-0.0125655473306973,
1.46674142913422));
#22330=CARTESIAN_POINT('Ctrl Pts',(-0.14631473222987,-0.000131398079681141,
1.46606550458429));
#22331=CARTESIAN_POINT('Origin',(0.,0.,-0.0924367114736175));
#22332=CARTESIAN_POINT('',(-0.0684664424539507,-0.0958295198918364,0.));
#22333=CARTESIAN_POINT('Ctrl Pts',(-0.0686146973663072,-0.0959584553529141,
8.16675286424706E-17));
#22334=CARTESIAN_POINT('Ctrl Pts',(-0.0391968190522335,-0.116741470120209,
0.00244290680874874));
#22335=CARTESIAN_POINT('Ctrl Pts',(0.0436301113039178,-0.130476273073809,
0.0075332029917574));
#22336=CARTESIAN_POINT('Ctrl Pts',(0.134092250525203,-0.0374520209666004,
0.0152708885490261));
#22337=CARTESIAN_POINT('Ctrl Pts',(0.104134301645602,0.0924305194826295,
0.023213056671806));
#22338=CARTESIAN_POINT('Ctrl Pts',(-0.0212379681243542,0.137589894578696,
0.0311552247945861));
#22339=CARTESIAN_POINT('Ctrl Pts',(-0.106685947947232,0.0723488109778776,
0.0375631097285225));
#22340=CARTESIAN_POINT('Ctrl Pts',(-0.117663533972591,0.0165813593984342,
0.041323605288199));
#22341=CARTESIAN_POINT('Ctrl Pts',(-0.117600989619072,5.04992496179954E-5,
0.0424367114736154));
#22342=CARTESIAN_POINT('Origin',(0.,0.,0.));
#22343=CARTESIAN_POINT('Ctrl Pts',(-0.0510216505388318,0.106149619882943,
-0.0164977839420939));
#22344=CARTESIAN_POINT('Ctrl Pts',(-0.0863355867949722,0.0891756983861136,
-0.0138503945678339));
#22345=CARTESIAN_POINT('Ctrl Pts',(-0.13808023131828,0.0175094743621551,
-0.00855561581931395));
#22346=CARTESIAN_POINT('Ctrl Pts',(-0.0894531427980795,-0.106808298616542,
-0.000613447696533924));
#22347=CARTESIAN_POINT('Ctrl Pts',(0.0412394829729132,-0.132934609947913,
0.00732872042624606));
#22348=CARTESIAN_POINT('Ctrl Pts',(0.134092250525203,-0.0374520209666004,
0.0152708885490261));
#22349=CARTESIAN_POINT('Ctrl Pts',(0.104134301645602,0.0924305194826295,
0.023213056671806));
#22350=CARTESIAN_POINT('Ctrl Pts',(-0.0212379681243542,0.137589894578696,
0.0311552247945861));
#22351=CARTESIAN_POINT('Ctrl Pts',(-0.127145335141994,0.0567276974868182,
0.039097392917366));
#22352=CARTESIAN_POINT('Ctrl Pts',(-0.116579117211717,-0.0761160149501382,
0.0470395610401461));
#22353=CARTESIAN_POINT('Ctrl Pts',(0.000787973702835166,-0.139222729671589,
0.054981729162926));
#22354=CARTESIAN_POINT('Ctrl Pts',(0.117431922513572,-0.0747907597173192,
0.0629238972857061));
#22355=CARTESIAN_POINT('Ctrl Pts',(0.126496838785129,0.0581591461343325,
0.070866065408486));
#22356=CARTESIAN_POINT('Ctrl Pts',(0.0196773008918215,0.137828289815661,
0.0788082335312661));
#22357=CARTESIAN_POINT('Ctrl Pts',(-0.105168479521776,0.0912330920368172,
0.0867504016540459));
#22358=CARTESIAN_POINT('Ctrl Pts',(-0.133669226619255,-0.0389412707994331,
0.0946925697768262));
#22359=CARTESIAN_POINT('Ctrl Pts',(-0.0397151780004399,-0.133441281507892,
0.102634737899606));
#22360=CARTESIAN_POINT('Ctrl Pts',(0.0906220264938673,-0.105695447092796,
0.110576906022386));
#22361=CARTESIAN_POINT('Ctrl Pts',(0.137940159127448,0.0188783162799928,
0.118519074145166));
#22362=CARTESIAN_POINT('Ctrl Pts',(0.0588909273047484,0.126157580947307,
0.126461242267946));
#22363=CARTESIAN_POINT('Ctrl Pts',(-0.074108440039672,0.117863552156501,
0.134403410390726));
#22364=CARTESIAN_POINT('Ctrl Pts',(-0.139216864956951,0.00159439502933392,
0.142345578513506));
#22365=CARTESIAN_POINT('Ctrl Pts',(-0.0767883381764272,-0.116135388594389,
0.150287746636286));
#22366=CARTESIAN_POINT('Ctrl Pts',(0.0559861945572589,-0.127473226882309,
0.158229914759066));
#22367=CARTESIAN_POINT('Ctrl Pts',(0.137471621702818,-0.0220324926503626,
0.166172082881846));
#22368=CARTESIAN_POINT('Ctrl Pts',(0.0930189202108026,0.103592267873211,
0.174114251004626));
#22369=CARTESIAN_POINT('Ctrl Pts',(-0.0366486683060043,0.134315868829211,
0.182056419127406));
#22370=CARTESIAN_POINT('Ctrl Pts',(-0.132742311638566,0.0419923350165386,
0.189998587250186));
#22371=CARTESIAN_POINT('Ctrl Pts',(-0.107230360350792,-0.0888004916405464,
0.197940755372966));
#22372=CARTESIAN_POINT('Ctrl Pts',(0.0165156171993534,-0.138242945169174,
0.205882923495746));
#22373=CARTESIAN_POINT('Ctrl Pts',(0.125131592687617,-0.061040658666823,
0.213825091618526));
#22374=CARTESIAN_POINT('Ctrl Pts',(0.119114174013628,0.0720811421096423,
0.221767259741306));
#22375=CARTESIAN_POINT('Ctrl Pts',(0.0039759348809324,0.139169211541763,
0.229709427864086));
#22376=CARTESIAN_POINT('Ctrl Pts',(-0.114804669066963,0.0787639858025777,
0.237651595986866));
#22377=CARTESIAN_POINT('Ctrl Pts',(-0.128412401817242,-0.0537971426620367,
0.245593764109646));
#22378=CARTESIAN_POINT('Ctrl Pts',(-0.024381182195918,-0.137074561658528,
0.253535932232426));
#22379=CARTESIAN_POINT('Ctrl Pts',(0.101985705091022,-0.094777599970642,
0.261478100355206));
#22380=CARTESIAN_POINT('Ctrl Pts',(0.134923209124943,0.0343453801629359,
0.269420268477986));
#22381=CARTESIAN_POINT('Ctrl Pts',(0.0442571924125319,0.132004463632409,
0.277362436600766));
#22382=CARTESIAN_POINT('Ctrl Pts',(-0.0869529592639067,0.108733897080731,
0.285304604723546));
#22383=CARTESIAN_POINT('Ctrl Pts',(-0.138505267237684,-0.0141480898545381,
0.293246772846326));
#22384=CARTESIAN_POINT('Ctrl Pts',(-0.0631725212350128,-0.124068972994571,
0.301188940969106));
#22385=CARTESIAN_POINT('Ctrl Pts',(0.0700327441786229,-0.12032993078169,
0.309131109091886));
#22386=CARTESIAN_POINT('Ctrl Pts',(0.139080821187468,-0.00635631000930847,
0.317073277214666));
#22387=CARTESIAN_POINT('Ctrl Pts',(0.0807165776729536,0.11344034374014,
0.325015445337446));
#22388=CARTESIAN_POINT('Ctrl Pts',(-0.0515923433190751,0.129313988454311,
0.332957613460226));
#22389=CARTESIAN_POINT('Ctrl Pts',(-0.136637377548019,0.026722734813544,
0.340899781583006));
#22390=CARTESIAN_POINT('Ctrl Pts',(-0.0965085366518414,-0.100349289247285,
0.348841949705786));
#22391=CARTESIAN_POINT('Ctrl Pts',(0.0320320385160992,-0.135491055083419,
0.356784117828566));
#22392=CARTESIAN_POINT('Ctrl Pts',(0.131227975626944,-0.0465090949381858,
0.364726285951346));
#22393=CARTESIAN_POINT('Ctrl Pts',(0.110205605501345,0.0850799742312894,
0.372668454074126));
#22394=CARTESIAN_POINT('Ctrl Pts',(-0.0117764211155082,0.138727046407055,
0.380610622196906));
#22395=CARTESIAN_POINT('Ctrl Pts',(-0.122970036152848,0.065285892102983,
0.388552790319686));
#22396=CARTESIAN_POINT('Ctrl Pts',(-0.121510464882371,-0.0679638464419502,
0.396494958442466));
#22397=CARTESIAN_POINT('Ctrl Pts',(-0.00873482453528946,-0.138951719454826,
0.404437126565246));
#22398=CARTESIAN_POINT('Ctrl Pts',(0.112042812448737,-0.0826455423945668,
0.412379294688026));
#22399=CARTESIAN_POINT('Ctrl Pts',(0.130177722634257,0.049372441998279,
0.420321462810806));
#22400=CARTESIAN_POINT('Ctrl Pts',(0.0290564652212241,0.136160197297018,
0.428263630933586));
#22401=CARTESIAN_POINT('Ctrl Pts',(-0.098683499418539,0.098211223603141,
0.436205799056366));
#22402=CARTESIAN_POINT('Ctrl Pts',(-0.136019240449831,-0.0297093205335648,
0.444147967179146));
#22403=CARTESIAN_POINT('Ctrl Pts',(-0.0487473834415776,-0.130413074907061,
0.452090135301926));
#22404=CARTESIAN_POINT('Ctrl Pts',(0.0831820848081396,-0.111645054821459,
0.460032303424706));
#22405=CARTESIAN_POINT('Ctrl Pts',(0.138908217753341,0.00940130521287039,
0.467974471547486));
#22406=CARTESIAN_POINT('Ctrl Pts',(0.0673801526530663,0.121835103839429,
0.475916639670265));
#22407=CARTESIAN_POINT('Ctrl Pts',(-0.0658750545035054,0.12265543075329,
0.483858807793047));
#22408=CARTESIAN_POINT('Ctrl Pts',(-0.138781944133385,0.0111107822259715,
0.491800975915825));
#22409=CARTESIAN_POINT('Ctrl Pts',(-0.084550315326251,-0.110612484274364,
0.499743144038607));
#22410=CARTESIAN_POINT('Ctrl Pts',(0.0471380885036503,-0.131003351527116,
0.507685312161385));
#22411=CARTESIAN_POINT('Ctrl Pts',(0.135643160584381,-0.031381690295376,
0.515627480284167));
#22412=CARTESIAN_POINT('Ctrl Pts',(0.0998851624184703,0.0969888232104648,
0.523569648406945));
#22413=CARTESIAN_POINT('Ctrl Pts',(-0.0273779061153799,0.136507610615132,
0.531511816529727));
#22414=CARTESIAN_POINT('Ctrl Pts',(-0.129560000008381,0.0509714027366644,
0.539453984652505));
#22415=CARTESIAN_POINT('Ctrl Pts',(-0.113051823689188,-0.0812598465397498,
0.547396152775286));
#22416=CARTESIAN_POINT('Ctrl Pts',(0.00702343738442799,-0.139048728244533,
0.555338320898066));
#22417=CARTESIAN_POINT('Ctrl Pts',(0.12066450826877,-0.0694546898587181,
0.563280489020846));
#22418=CARTESIAN_POINT('Ctrl Pts',(0.123764493242992,0.063766979789076,
0.571222657143626));
#22419=CARTESIAN_POINT('Ctrl Pts',(0.0134834875971477,0.13857154491934,
0.579164825266405));
#22420=CARTESIAN_POINT('Ctrl Pts',(-0.109149777898995,0.0864303389077871,
0.587106993389186));
#22421=CARTESIAN_POINT('Ctrl Pts',(-0.131790633456927,-0.0448899368693808,
0.595049161511966));
#22422=CARTESIAN_POINT('Ctrl Pts',(-0.0336977294021144,-0.135086418755761,
0.602991329634746));
#22423=CARTESIAN_POINT('Ctrl Pts',(0.0952657566843092,-0.101529863106778,
0.610933497757526));
#22424=CARTESIAN_POINT('Ctrl Pts',(0.136956022624868,0.025038477707157,
0.618875665880307));
#22425=CARTESIAN_POINT('Ctrl Pts',(0.0531805018142573,0.128669000640787,
0.626817834003085));
#22426=CARTESIAN_POINT('Ctrl Pts',(-0.0793138220987445,0.114425500318782,
0.634760002125867));
#22427=CARTESIAN_POINT('Ctrl Pts',(-0.139148536750765,-0.00464351367351466,
0.642702170248646));
#22428=CARTESIAN_POINT('Ctrl Pts',(-0.0715088964667609,-0.119458592094588,
0.650644338371427));
#22429=CARTESIAN_POINT('Ctrl Pts',(0.0616402393688536,-0.124837327709565,
0.658586506494205));
#22430=CARTESIAN_POINT('Ctrl Pts',(0.138320583400205,-0.0158522461166236,
0.666528674616987));
#22431=CARTESIAN_POINT('Ctrl Pts',(0.0882850628235238,0.107655121482266,
0.674470842739765));
#22432=CARTESIAN_POINT('Ctrl Pts',(-0.0426286451686149,0.132539337972556,
0.682413010862546));
#22433=CARTESIAN_POINT('Ctrl Pts',(-0.13449013477919,0.0360039045964495,
0.690355178985326));
#22434=CARTESIAN_POINT('Ctrl Pts',(-0.103144844235522,-0.0935148042116587,
0.698297347108106));
#22435=CARTESIAN_POINT('Ctrl Pts',(0.022691720100341,-0.137364345221032,
0.706239515230886));
#22436=CARTESIAN_POINT('Ctrl Pts',(0.127740337615313,-0.0553740340325759,
0.714181683353665));
#22437=CARTESIAN_POINT('Ctrl Pts',(0.115765682611161,0.077344581120379,
0.722123851476446));
#22438=CARTESIAN_POINT('Ctrl Pts',(-0.00226223072526165,0.139207614056346,
0.730066019599226));
#22439=CARTESIAN_POINT('Ctrl Pts',(-0.118217708309552,0.0735421711751344,
0.738008187722006));
#22440=CARTESIAN_POINT('Ctrl Pts',(-0.125873620115675,-0.059495455776806,
0.745950355844786));
#22441=CARTESIAN_POINT('Ctrl Pts',(-0.0182163644075178,-0.138029133036789,
0.753892523967566));
#22442=CARTESIAN_POINT('Ctrl Pts',(0.106128952536144,-0.0901139441634624,
0.761834692090347));
#22443=CARTESIAN_POINT('Ctrl Pts',(0.133249245915149,0.0403548753208232,
0.769776860213125));
#22444=CARTESIAN_POINT('Ctrl Pts',(0.0382995408207276,0.133854483197375,
0.777719028335907));
#22445=CARTESIAN_POINT('Ctrl Pts',(-0.0917364783268051,0.104729633071593,
0.785661196458685));
#22446=CARTESIAN_POINT('Ctrl Pts',(-0.137732458880487,-0.0203383202317681,
0.793603364581467));
#22447=CARTESIAN_POINT('Ctrl Pts',(-0.0575513573065257,-0.126774282767806,
0.801545532704245));
#22448=CARTESIAN_POINT('Ctrl Pts',(0.0753527000357912,-0.117071978271622,
0.809487700827026));
#22449=CARTESIAN_POINT('Ctrl Pts',(0.139225942868322,-0.000119714417332432,
0.817429868949805));
#22450=CARTESIAN_POINT('Ctrl Pts',(0.0755539188089132,0.116942220141962,
0.825372037072586));
#22451=CARTESIAN_POINT('Ctrl Pts',(-0.0573332568284509,0.12687306712048,
0.833314205195366));
#22452=CARTESIAN_POINT('Ctrl Pts',(-0.13769727914169,0.0205751504512258,
0.841256373318145));
#22453=CARTESIAN_POINT('Ctrl Pts',(-0.0919164475821765,-0.104571717796869,
0.849198541440926));
#22454=CARTESIAN_POINT('Ctrl Pts',(0.0380692928980519,-0.133920149482284,
0.857140709563706));
#22455=CARTESIAN_POINT('Ctrl Pts',(0.133179650076608,-0.0405839661022353,
0.865082877686486));
#22456=CARTESIAN_POINT('Ctrl Pts',(0.106283765719693,0.0899312995767124,
0.873025045809266));
#22457=CARTESIAN_POINT('Ctrl Pts',(-0.0179789669825735,0.138060255849953,
0.880967213932046));
#22458=CARTESIAN_POINT('Ctrl Pts',(-0.125771118879347,0.0597118342956578,
0.888909382054826));
#22459=CARTESIAN_POINT('Ctrl Pts',(-0.118344004924669,-0.0733387619032726,
0.896851550177606));
#22460=CARTESIAN_POINT('Ctrl Pts',(-0.00250162451743248,-0.139203517821528,
0.904793718300386));
#22461=CARTESIAN_POINT('Ctrl Pts',(0.115632500949424,-0.0775435504945224,
0.912735886423165));
#22462=CARTESIAN_POINT('Ctrl Pts',(0.127835376168433,0.0551542754370876,
0.920678054545947));
#22463=CARTESIAN_POINT('Ctrl Pts',(0.0229279137899797,0.137325118854324,
0.928620222668725));
#22464=CARTESIAN_POINT('Ctrl Pts',(-0.102983873094174,0.0936920454555137,
0.936562390791507));
#22465=CARTESIAN_POINT('Ctrl Pts',(-0.134551852288801,-0.0357725669300891,
0.944504558914285));
#22466=CARTESIAN_POINT('Ctrl Pts',(-0.0428565117498991,-0.132465832952297,
0.952446727037066));
#22467=CARTESIAN_POINT('Ctrl Pts',(0.0880997963686447,-0.107806787258123,
0.960388895159846));
#22468=CARTESIAN_POINT('Ctrl Pts',(0.138347640177547,0.0156143509765511,
0.968331063282625));
#22469=CARTESIAN_POINT('Ctrl Pts',(0.061854832590724,0.124731139593481,
0.976273231405407));
#22470=CARTESIAN_POINT('Ctrl Pts',(-0.0713033562375951,0.119581390225944,
0.984215399528185));
#22471=CARTESIAN_POINT('Ctrl Pts',(-0.139140345480169,0.00488280234845834,
0.992157567650966));
#22472=CARTESIAN_POINT('Ctrl Pts',(-0.0795104838321055,-0.114288934109561,
1.00009973577375));
#22473=CARTESIAN_POINT('Ctrl Pts',(0.0529591494285269,-0.128760265574912,
1.00804190389653));
#22474=CARTESIAN_POINT('Ctrl Pts',(0.136912761112491,-0.0252739657289669,
1.0159840720193));
#22475=CARTESIAN_POINT('Ctrl Pts',(0.0954402180350474,0.101365883217864,
1.02392624014209));
#22476=CARTESIAN_POINT('Ctrl Pts',(-0.0334653697086341,0.135144169424284,
1.03186840826486));
#22477=CARTESIAN_POINT('Ctrl Pts',(-0.131713240771149,0.0451165125500212,
1.03981057638765));
#22478=CARTESIAN_POINT('Ctrl Pts',(-0.109298251871946,-0.0862425048155002,
1.04775274451043));
#22479=CARTESIAN_POINT('Ctrl Pts',(0.0132451643780021,-0.13859452774087,
1.05569491263321));
#22480=CARTESIAN_POINT('Ctrl Pts',(0.123654649330263,-0.0639797248987874,
1.06363708075599));
#22481=CARTESIAN_POINT('Ctrl Pts',(0.120783771971213,0.0692470788374567,
1.07157924887876));
#22482=CARTESIAN_POINT('Ctrl Pts',(0.00726255089817806,0.139036444335888,
1.07952141700155));
#22483=CARTESIAN_POINT('Ctrl Pts',(-0.112911912907791,0.0814541430660127,
1.08746358512433));
#22484=CARTESIAN_POINT('Ctrl Pts',(-0.129647464608677,-0.0507485213543897,
1.09540575324711));
#22485=CARTESIAN_POINT('Ctrl Pts',(-0.0276126195379174,-0.136460326620484,
1.10334792136989));
#22486=CARTESIAN_POINT('Ctrl Pts',(0.0997182217817603,-0.0971604536002107,
1.11129008949267));
#22487=CARTESIAN_POINT('Ctrl Pts',(0.135696927507188,0.0311483765905046,
1.11923225761545));
#22488=CARTESIAN_POINT('Ctrl Pts',(0.0473633069609982,0.130922093830007,
1.12717442573822));
#22489=CARTESIAN_POINT('Ctrl Pts',(-0.0843599685788644,0.110757722983492,
1.13511659386101));
#22490=CARTESIAN_POINT('Ctrl Pts',(-0.138800846271631,-0.0108721006891078,
1.14305876198379));
#22491=CARTESIAN_POINT('Ctrl Pts',(-0.0660858892268601,-0.122541963197144,
1.15100093010657));
#22492=CARTESIAN_POINT('Ctrl Pts',(0.0671705316110708,-0.121950798202395,
1.15894309822935));
#22493=CARTESIAN_POINT('Ctrl Pts',(0.138891844802359,-0.00964017357273747,
1.16688526635212));
#22494=CARTESIAN_POINT('Ctrl Pts',(0.0833739592533277,0.111501840422208,
1.17482743447491));
#22495=CARTESIAN_POINT('Ctrl Pts',(-0.0485230383040216,0.130496713571114,
1.18276960259768));
#22496=CARTESIAN_POINT('Ctrl Pts',(-0.135967947813762,0.0299431906521225,
1.19071177072047));
#22497=CARTESIAN_POINT('Ctrl Pts',(-0.0988522486080867,-0.0980413710850678,
1.19865393884324));
#22498=CARTESIAN_POINT('Ctrl Pts',(0.0288222657999454,-0.136209964735594,
1.20659610696603));
#22499=CARTESIAN_POINT('Ctrl Pts',(0.130092623711363,-0.0495962373069701,
1.21453827508881));
#22500=CARTESIAN_POINT('Ctrl Pts',(0.112184773380136,0.082452738709893,
1.22248044321158));
#22501=CARTESIAN_POINT('Ctrl Pts',(-0.00849585454694533,0.138966535376798,
1.23042261133437));
#22502=CARTESIAN_POINT('Ctrl Pts',(-0.121393406896754,0.0681727090639588,
1.23836477945715));
#22503=CARTESIAN_POINT('Ctrl Pts',(-0.123082127310551,-0.0650743223999996,
1.24630694757992));
#22504=CARTESIAN_POINT('Ctrl Pts',(-0.0120149744006178,-0.138706589206355,
1.25424911570271));
#22505=CARTESIAN_POINT('Ctrl Pts',(0.110059129405696,-0.0852693704304675,
1.26219128382548));
#22506=CARTESIAN_POINT('Ctrl Pts',(0.13130776387206,0.0462833517151888,
1.27013345194827));
#22507=CARTESIAN_POINT('Ctrl Pts',(0.0322649968732001,0.135435768819968,
1.27807562007105));
#22508=CARTESIAN_POINT('Ctrl Pts',(-0.0963358219719167,0.100515107841202,
1.28601778819382));
#22509=CARTESIAN_POINT('Ctrl Pts',(-0.136683130933199,-0.0264877182308561,
1.29395995631661));
#22510=CARTESIAN_POINT('Ctrl Pts',(-0.0518146499729274,-0.129225073214149,
1.30190212443939));
#22511=CARTESIAN_POINT('Ctrl Pts',(0.0805213734929343,-0.11357898534207,
1.30984429256217));
#22512=CARTESIAN_POINT('Ctrl Pts',(0.1390915465469,0.0061171215252809,1.31778646068495));
#22513=CARTESIAN_POINT('Ctrl Pts',(0.0702395735793815,0.120209316621791,
1.32572862880773));
#22514=CARTESIAN_POINT('Ctrl Pts',(-0.0629590648350173,0.124177428154433,
1.33367079693051));
#22515=CARTESIAN_POINT('Ctrl Pts',(-0.138480731711197,0.0143862582011507,
1.34161296505328));
#22516=CARTESIAN_POINT('Ctrl Pts',(-0.0871398218994898,-0.108584202098263,
1.34955513317607));
#22517=CARTESIAN_POINT('Ctrl Pts',(0.0440301174146577,-0.132080378229483,
1.35749730129884));
#22518=CARTESIAN_POINT('Ctrl Pts',(0.13486394497766,-0.0345773583278084,
1.36543946942163));
#22519=CARTESIAN_POINT('Ctrl Pts',(0.102148545386143,0.0946020732301706,
1.3733816375444));
#22520=CARTESIAN_POINT('Ctrl Pts',(-0.0241454188302812,0.137116288461919,
1.38132380566719));
#22521=CARTESIAN_POINT('Ctrl Pts',(-0.128319693277533,0.0540178939468163,
1.38926597378996));
#22522=CARTESIAN_POINT('Ctrl Pts',(-0.114939956470138,-0.0785664351508689,
1.39720814191275));
#22523=CARTESIAN_POINT('Ctrl Pts',(0.00373660876362508,-0.139175849115243,
1.40515031003553));
#22524=CARTESIAN_POINT('Ctrl Pts',(0.118990018389619,-0.0722858665142316,
1.41309247815831));
#22525=CARTESIAN_POINT('Ctrl Pts',(0.125236419206141,0.0608253567263532,
1.42103464628109));
#22526=CARTESIAN_POINT('Ctrl Pts',(0.0167532566496359,0.13821437898841,
1.42897681440387));
#22527=CARTESIAN_POINT('Ctrl Pts',(-0.107077349343502,0.0889846891406984,
1.43691898252665));
#22528=CARTESIAN_POINT('Ctrl Pts',(-0.132814597987359,-0.0417638487589672,
1.44486115064943));
#22529=CARTESIAN_POINT('Ctrl Pts',(-0.0368790902657646,-0.134252921254984,
1.45280331877221));
#22530=CARTESIAN_POINT('Ctrl Pts',(0.0928396680879532,-0.103751556080299,
1.46074548689499));
#22531=CARTESIAN_POINT('Ctrl Pts',(0.137511141307062,0.0217950526079239,
1.46868765501776));
#22532=CARTESIAN_POINT('Ctrl Pts',(0.0562018483347667,0.127378648737854,
1.47662982314055));
#22533=CARTESIAN_POINT('Ctrl Pts',(-0.0765818961642769,0.116263681173923,
1.48457199126332));
#22534=CARTESIAN_POINT('Ctrl Pts',(-0.13923195096087,-0.00134816270381636,
1.49251415938611));
#22535=CARTESIAN_POINT('Ctrl Pts',(-0.0742871760264013,-0.117748889605885,
1.50045632750888));
#22536=CARTESIAN_POINT('Ctrl Pts',(0.0586284551779338,-0.126233948370975,
1.50839849563167));
#22537=CARTESIAN_POINT('Ctrl Pts',(0.137995068118234,-0.019163470063063,
1.51634066375444));
#22538=CARTESIAN_POINT('Ctrl Pts',(0.0906261803825392,0.105639137646141,
1.52428283187723));
#22539=CARTESIAN_POINT('Ctrl Pts',(0.00417072711528833,0.124051375507138,
1.52957761062575));
#22540=CARTESIAN_POINT('Ctrl Pts',(-0.0334019664627544,0.1129391839063,
1.53222500000001));
#22541=CARTESIAN_POINT('Ctrl Pts',(-0.0551480035117261,0.114734422509858,
-0.0109985226280628));
#22542=CARTESIAN_POINT('Ctrl Pts',(-0.093317938433455,0.0963877427684319,
-0.00835113325380276));
#22543=CARTESIAN_POINT('Ctrl Pts',(-0.149247407742026,0.0189255452031589,
-0.00305635450528277));
#22544=CARTESIAN_POINT('Ctrl Pts',(-0.0966876253720675,-0.115446371588928,
0.00488581361749726));
#22545=CARTESIAN_POINT('Ctrl Pts',(0.0445747075563756,-0.143685636564375,
0.0128279817402772));
#22546=CARTESIAN_POINT('Ctrl Pts',(0.144936900801175,-0.0404809362687151,
0.0207701498630572));
#22547=CARTESIAN_POINT('Ctrl Pts',(0.112556116319125,0.0999057960529736,
0.0287123179858373));
#22548=CARTESIAN_POINT('Ctrl Pts',(-0.0229555792165621,0.148717415239805,
0.0366544861086172));
#22549=CARTESIAN_POINT('Ctrl Pts',(-0.137428156769908,0.0613155244327884,
0.0445966542313972));
#22550=CARTESIAN_POINT('Ctrl Pts',(-0.126007400730642,-0.0822718633254329,
0.0525388223541772));
#22551=CARTESIAN_POINT('Ctrl Pts',(0.000851700720621877,-0.150482305134309,
0.0604809904769572));
#22552=CARTESIAN_POINT('Ctrl Pts',(0.126929176276611,-0.0808394286734405,
0.0684231585997372));
#22553=CARTESIAN_POINT('Ctrl Pts',(0.136727213562698,0.0628627408439891,
0.0763653267225173));
#22554=CARTESIAN_POINT('Ctrl Pts',(0.0212686937255662,0.148975090584026,
0.0843074948452972));
#22555=CARTESIAN_POINT('Ctrl Pts',(-0.113673932864549,0.0986115272026031,
0.0922496629680772));
#22556=CARTESIAN_POINT('Ctrl Pts',(-0.144479665027646,-0.0420906285100245,
0.100191831090857));
#22557=CARTESIAN_POINT('Ctrl Pts',(-0.0429271251068198,-0.144233284958223,
0.108133999213637));
#22558=CARTESIAN_POINT('Ctrl Pts',(0.0979510420095061,-0.114243518700172,
0.116076167336417));
#22559=CARTESIAN_POINT('Ctrl Pts',(0.149096007275942,0.0204050915936607,
0.124018335459197));
#22560=CARTESIAN_POINT('Ctrl Pts',(0.0636537044864716,0.136360518400275,
0.131960503581977));
#22561=CARTESIAN_POINT('Ctrl Pts',(-0.0801019266996435,0.127395713772213,
0.139902671704757));
#22562=CARTESIAN_POINT('Ctrl Pts',(-0.15047596611352,0.00172334100814176,
0.147844839827537));
#22563=CARTESIAN_POINT('Ctrl Pts',(-0.0829985603893774,-0.125527785761544,
0.155787007950317));
#22564=CARTESIAN_POINT('Ctrl Pts',(0.0605140527882773,-0.137782566606816,
0.163729176073097));
#22565=CARTESIAN_POINT('Ctrl Pts',(0.148589577098441,-0.0238143605552183,
0.171671344195877));
#22566=CARTESIAN_POINT('Ctrl Pts',(0.100541783424623,0.111970245809892,
0.179613512318657));
#22567=CARTESIAN_POINT('Ctrl Pts',(-0.0396126128240685,0.145178604134651,
0.187555680441437));
#22568=CARTESIAN_POINT('Ctrl Pts',(-0.143477786216001,0.0453884461694337,
0.195497848564217));
#22569=CARTESIAN_POINT('Ctrl Pts',(-0.115902567375552,-0.095982191346566,
0.203440016686997));
#22570=CARTESIAN_POINT('Ctrl Pts',(0.0178513102906219,-0.149423281002214,
0.211382184809777));
#22571=CARTESIAN_POINT('Ctrl Pts',(0.135251553802876,-0.0659772944027704,
0.219324352932557));
#22572=CARTESIAN_POINT('Ctrl Pts',(0.128747479107914,0.07791067196398,0.227266521055337));
#22573=CARTESIAN_POINT('Ctrl Pts',(0.00429748682099232,0.150424458749874,
0.235208689178117));
#22574=CARTESIAN_POINT('Ctrl Pts',(-0.124089444892588,0.0851339876261335,
0.243150857300897));
#22575=CARTESIAN_POINT('Ctrl Pts',(-0.138797696890977,-0.0581479623084488,
0.251093025423677));
#22576=CARTESIAN_POINT('Ctrl Pts',(-0.0263529993083425,-0.148160405002171,
0.259035193546457));
#22577=CARTESIAN_POINT('Ctrl Pts',(0.110233752987369,-0.102442695616748,
0.266977361669237));
#22578=CARTESIAN_POINT('Ctrl Pts',(0.145835062802846,0.0371230472913779,
0.274919529792017));
#22579=CARTESIAN_POINT('Ctrl Pts',(0.0478364728857143,0.142680265085169,
0.282861697914797));
#22580=CARTESIAN_POINT('Ctrl Pts',(-0.0939852406223356,0.117527701960322,
0.290803866037577));
#22581=CARTESIAN_POINT('Ctrl Pts',(-0.14970681824969,-0.01529231023972,
0.298746034160357));
#22582=CARTESIAN_POINT('Ctrl Pts',(-0.0682815703945392,-0.134102995221473,
0.306688202283137));
#22583=CARTESIAN_POINT('Ctrl Pts',(0.0756966107742644,-0.1300615596562,
0.314630370405917));
#22584=CARTESIAN_POINT('Ctrl Pts',(0.150328919865546,-0.00687037371415525,
0.322572538528697));
#22585=CARTESIAN_POINT('Ctrl Pts',(0.0872444944832666,0.122614780370367,
0.330514706651477));
#22586=CARTESIAN_POINT('Ctrl Pts',(-0.0557648508131485,0.139772198940638,
0.338456874774257));
#22587=CARTESIAN_POINT('Ctrl Pts',(-0.147687863823926,0.0288839239377102,
0.346399042897038));
#22588=CARTESIAN_POINT('Ctrl Pts',(-0.104313621021262,-0.10846499275041,
0.354341211019817));
#22589=CARTESIAN_POINT('Ctrl Pts',(0.0346226151823369,-0.146448833047075,
0.362283379142597));
#22590=CARTESIAN_POINT('Ctrl Pts',(0.141840978962514,-0.0502704970123603,
0.370225547265377));
#22591=CARTESIAN_POINT('Ctrl Pts',(0.119118434135606,0.0919607787700563,
0.378167715388157));
#22592=CARTESIAN_POINT('Ctrl Pts',(-0.0127288338612142,0.149946533709345,
0.386109883510937));
#22593=CARTESIAN_POINT('Ctrl Pts',(-0.132915182358376,0.070565859178174,
0.394052051633717));
#22594=CARTESIAN_POINT('Ctrl Pts',(-0.131337568919768,-0.0734603918663599,
0.401994219756497));
#22595=CARTESIAN_POINT('Ctrl Pts',(-0.00944124952954395,-0.150189377088511,
0.409936387879277));
#22596=CARTESIAN_POINT('Ctrl Pts',(0.121104224366159,-0.0893294633566384,
0.417878556002057));
#22597=CARTESIAN_POINT('Ctrl Pts',(0.140705787232781,0.0533654159743681,
0.425820724124838));
#22598=CARTESIAN_POINT('Ctrl Pts',(0.0314063937394313,0.147172091835368,
0.433762892247617));
#22599=CARTESIAN_POINT('Ctrl Pts',(-0.106664482920656,0.106154012011714,
0.441705060370398));
#22600=CARTESIAN_POINT('Ctrl Pts',(-0.147019735166745,-0.032112048430678,
0.449647228493177));
#22601=CARTESIAN_POINT('Ctrl Pts',(-0.052689806088835,-0.14096017351449,
0.457589396615958));
#22602=CARTESIAN_POINT('Ctrl Pts',(0.0899093983958942,-0.120674298270189,
0.465531564738737));
#22603=CARTESIAN_POINT('Ctrl Pts',(0.15014235720654,0.0101616315312987,
0.473473732861518));
#22604=CARTESIAN_POINT('Ctrl Pts',(0.0728294921055832,0.131688462906045,
0.481415900984297));
#22605=CARTESIAN_POINT('Ctrl Pts',(-0.071202669822089,0.132575133389036,
0.489358069107078));
#22606=CARTESIAN_POINT('Ctrl Pts',(-0.150005871264529,0.012009361726732,
0.497300237229857));
#22607=CARTESIAN_POINT('Ctrl Pts',(-0.0913882839399832,-0.119558219045865,
0.505242405352637));
#22608=CARTESIAN_POINT('Ctrl Pts',(0.0509503601487159,-0.141598188489932,
0.513184573475417));
#22609=CARTESIAN_POINT('Ctrl Pts',(0.146613240011817,-0.0339196703426114,
0.521126741598197));
#22610=CARTESIAN_POINT('Ctrl Pts',(0.107963329873666,0.104832750538675,
0.529068909720978));
#22611=CARTESIAN_POINT('Ctrl Pts',(-0.0295920819230583,0.147547602048875,
0.537011077843756));
#22612=CARTESIAN_POINT('Ctrl Pts',(-0.140038106568177,0.055093691941219,
0.544953245966537));
#22613=CARTESIAN_POINT('Ctrl Pts',(-0.122194838935542,-0.0878316999746162,
0.552895414089317));
#22614=CARTESIAN_POINT('Ctrl Pts',(0.00759145471482065,-0.150294231420327,
0.560837582212097));
#22615=CARTESIAN_POINT('Ctrl Pts',(0.130423195946632,-0.0750718065719766,
0.568779750334878));
#22616=CARTESIAN_POINT('Ctrl Pts',(0.133773890807325,0.0689241055160235,
0.576721918457657));
#22617=CARTESIAN_POINT('Ctrl Pts',(0.0145739585745413,0.149778456108953,
0.584664086580438));
#22618=CARTESIAN_POINT('Ctrl Pts',(-0.117977216952174,0.0934203535806499,
0.592606254703216));
#22619=CARTESIAN_POINT('Ctrl Pts',(-0.142449141490696,-0.0485203902651028,
0.600548422825998));
#22620=CARTESIAN_POINT('Ctrl Pts',(-0.036423018067407,-0.146011471938939,
0.608490590948776));
#22621=CARTESIAN_POINT('Ctrl Pts',(0.102970331784443,-0.109741044988262,
0.616432759071558));
#22622=CARTESIAN_POINT('Ctrl Pts',(0.148032279177632,0.0270634532975707,
0.624374927194337));
#22623=CARTESIAN_POINT('Ctrl Pts',(0.0574814509102497,0.139075048028633,
0.632317095317117));
#22624=CARTESIAN_POINT('Ctrl Pts',(-0.0857282916847416,0.123679611042927,
0.640259263439898));
#22625=CARTESIAN_POINT('Ctrl Pts',(-0.150402111894479,-0.00501905574730406,
0.648201431562677));
#22626=CARTESIAN_POINT('Ctrl Pts',(-0.0772921462128499,-0.129119751845818,
0.656143599685457));
#22627=CARTESIAN_POINT('Ctrl Pts',(0.0666253659236285,-0.134933490277457,
0.664085767808237));
#22628=CARTESIAN_POINT('Ctrl Pts',(0.14950719819016,-0.0171342893707992,
0.672027935931017));
#22629=CARTESIAN_POINT('Ctrl Pts',(0.0954250774564579,0.11636168087194,
0.679970104053797));
#22630=CARTESIAN_POINT('Ctrl Pts',(-0.0460762176180427,0.143258397146306,
0.687912272176577));
#22631=CARTESIAN_POINT('Ctrl Pts',(-0.145366963764729,0.0389157041403328,
0.695854440299358));
#22632=CARTESIAN_POINT('Ctrl Pts',(-0.111486636987321,-0.101077771820372,
0.703796608422136));
#22633=CARTESIAN_POINT('Ctrl Pts',(0.02452690272786,-0.148473624679578,
0.711738776544918));
#22634=CARTESIAN_POINT('Ctrl Pts',(0.138071279799868,-0.0598523840572839,
0.719680944667696));
#22635=CARTESIAN_POINT('Ctrl Pts',(0.125128179973684,0.0835997892305201,
0.727623112790477));
#22636=CARTESIAN_POINT('Ctrl Pts',(-0.00244518761474098,0.150465967050502,
0.735565280913257));
#22637=CARTESIAN_POINT('Ctrl Pts',(-0.127778512144395,0.0794898610961098,
0.743507449036036));
#22638=CARTESIAN_POINT('Ctrl Pts',(-0.136053592364468,-0.0643071239260258,
0.751449617158818));
#22639=CARTESIAN_POINT('Ctrl Pts',(-0.019689604662082,-0.149192176910068,
0.759391785281597));
#22640=CARTESIAN_POINT('Ctrl Pts',(0.114712083700712,-0.0974018687498071,
0.767333953404378));
#22641=CARTESIAN_POINT('Ctrl Pts',(0.144025718573537,0.0436185576594447,
0.775276121527157));
#22642=CARTESIAN_POINT('Ctrl Pts',(0.0413969989087525,0.14467990414796,
0.783218289649938));
#22643=CARTESIAN_POINT('Ctrl Pts',(-0.0991556246317344,0.113199594905656,
0.791160457772717));
#22644=CARTESIAN_POINT('Ctrl Pts',(-0.148871509365196,-0.021983172706469,
0.799102625895497));
#22645=CARTESIAN_POINT('Ctrl Pts',(-0.062205797368885,-0.137027095702329,
0.807044794018277));
#22646=CARTESIAN_POINT('Ctrl Pts',(0.081446815661698,-0.126540121706451,
0.814986962141057));
#22647=CARTESIAN_POINT('Ctrl Pts',(0.150485778196879,-0.000129396266831759,
0.822929130263837));
#22648=CARTESIAN_POINT('Ctrl Pts',(0.0816643079123276,0.126399869446589,
0.830871298386618));
#22649=CARTESIAN_POINT('Ctrl Pts',(-0.0619700581130299,0.137133869194964,
0.838813466509397));
#22650=CARTESIAN_POINT('Ctrl Pts',(-0.148833484480893,0.0222391564630926,
0.846755634632177));
#22651=CARTESIAN_POINT('Ctrl Pts',(-0.0993501488194509,-0.113028908304323,
0.854697802754957));
#22652=CARTESIAN_POINT('Ctrl Pts',(0.041148129789194,-0.144750881164039,
0.862639970877736));
#22653=CARTESIAN_POINT('Ctrl Pts',(0.143950494202948,-0.0438661760544617,
0.870582139000517));
#22654=CARTESIAN_POINT('Ctrl Pts',(0.114879417330645,0.0972044528644933,
0.878524307123298));
#22655=CARTESIAN_POINT('Ctrl Pts',(-0.0194330078274841,0.149225816766708,
0.886466475246077));
#22656=CARTESIAN_POINT('Ctrl Pts',(-0.135942801386891,0.0645410019599824,
0.894408643368857));
#22657=CARTESIAN_POINT('Ctrl Pts',(-0.127915022941288,-0.0792700011911429,
0.902350811491637));
#22658=CARTESIAN_POINT('Ctrl Pts',(-0.00270394227186439,-0.150461539534541,
0.910292979614417));
#22659=CARTESIAN_POINT('Ctrl Pts',(0.124984227305131,-0.0838148501630433,
0.918235147737197));
#22660=CARTESIAN_POINT('Ctrl Pts',(0.138174004553101,0.0596148525845174,
0.926177315859977));
#22661=CARTESIAN_POINT('Ctrl Pts',(0.0247821984756025,0.148431225898158,
0.934119483982757));
#22662=CARTESIAN_POINT('Ctrl Pts',(-0.11131264737753,0.101269347369872,
0.942061652105537));
#22663=CARTESIAN_POINT('Ctrl Pts',(-0.145433672650089,-0.0386656571445607,
0.950003820228317));
#22664=CARTESIAN_POINT('Ctrl Pts',(-0.0463225128062989,-0.143178947440692,
0.957945988351097));
#22665=CARTESIAN_POINT('Ctrl Pts',(0.0952248276606132,-0.116525612549003,
0.965888156473877));
#22666=CARTESIAN_POINT('Ctrl Pts',(0.149536443172165,0.0168771545685866,
0.973830324596656));
#22667=CARTESIAN_POINT('Ctrl Pts',(0.0668573142755158,0.134818714245386,
0.981772492719438));
#22668=CARTESIAN_POINT('Ctrl Pts',(-0.0770699830103684,0.129252481220654,
0.989714660842216));
#22669=CARTESIAN_POINT('Ctrl Pts',(-0.15039325815857,0.00527769678589187,
0.997656828964997));
#22670=CARTESIAN_POINT('Ctrl Pts',(-0.0859408583470751,-0.123532000103139,
1.00559899708778));
#22671=CARTESIAN_POINT('Ctrl Pts',(0.0572421967501742,-0.139173693973137,
1.01354116521056));
#22672=CARTESIAN_POINT('Ctrl Pts',(0.147985518909957,-0.0273179863069172,
1.02148333333334));
#22673=CARTESIAN_POINT('Ctrl Pts',(0.103158902618224,0.109563803299803,
1.02942550145612));
#22674=CARTESIAN_POINT('Ctrl Pts',(-0.0361718663885326,0.146073893166727,
1.0373676695789));
#22675=CARTESIAN_POINT('Ctrl Pts',(-0.142365489706367,0.0487652901517079,
1.04530983770168));
#22676=CARTESIAN_POINT('Ctrl Pts',(-0.118137698690712,-0.0932173284908804,
1.05325200582446));
#22677=CARTESIAN_POINT('Ctrl Pts',(0.0143163610725534,-0.149803297655807,
1.06119417394724));
#22678=CARTESIAN_POINT('Ctrl Pts',(0.133655163317704,-0.0691540562905145,
1.06913634207002));
#22679=CARTESIAN_POINT('Ctrl Pts',(0.130552105047211,0.0748474051030229,
1.0770785101928));
#22680=CARTESIAN_POINT('Ctrl Pts',(0.0078499064261323,0.150280954056111,
1.08502067831558));
#22681=CARTESIAN_POINT('Ctrl Pts',(-0.122043612932812,0.0880417101447944,
1.09296284643836));
#22682=CARTESIAN_POINT('Ctrl Pts',(-0.140132644828567,-0.0548527851276936,
1.10090501456114));
#22683=CARTESIAN_POINT('Ctrl Pts',(-0.0298457776877653,-0.147496493982489,
1.10884718268392));
#22684=CARTESIAN_POINT('Ctrl Pts',(0.107782887988268,-0.10501826145877,
1.1167893508067));
#22685=CARTESIAN_POINT('Ctrl Pts',(0.146671355310253,0.033667487497105,
1.12473151892948));
#22686=CARTESIAN_POINT('Ctrl Pts',(0.0511937930472066,0.141510359113225,
1.13267368705226));
#22687=CARTESIAN_POINT('Ctrl Pts',(-0.0911825429852659,0.119715203870077,
1.14061585517504));
#22688=CARTESIAN_POINT('Ctrl Pts',(-0.150026302104679,-0.0117513769282424,
1.14855802329782));
#22689=CARTESIAN_POINT('Ctrl Pts',(-0.0714305557085884,-0.132452489195471,
1.1565001914206));
#22690=CARTESIAN_POINT('Ctrl Pts',(0.0726029180563751,-0.131813513998426,
1.16444235954338));
#22691=CARTESIAN_POINT('Ctrl Pts',(0.150124660100533,-0.010419818262018,
1.17238452766616));
#22692=CARTESIAN_POINT('Ctrl Pts',(0.0901167906002831,0.120519501471002,
1.18032669578894));
#22693=CARTESIAN_POINT('Ctrl Pts',(-0.0524473171394798,0.141050576417769,
1.18826886391172));
#22694=CARTESIAN_POINT('Ctrl Pts',(-0.146964294261872,0.0323648326895764,
1.1962110320345));
#22695=CARTESIAN_POINT('Ctrl Pts',(-0.106846879624786,-0.105970422747861,
1.20415320015727));
#22696=CARTESIAN_POINT('Ctrl Pts',(0.0311532535456026,-0.14722588419309,
1.21209536828006));
#22697=CARTESIAN_POINT('Ctrl Pts',(0.140613805972886,-0.0536073106276968,
1.22003753640283));
#22698=CARTESIAN_POINT('Ctrl Pts',(0.121257666323848,0.0891210667609394,
1.22797970452562));
#22699=CARTESIAN_POINT('Ctrl Pts',(-0.00918295295119051,0.150205391241489,
1.2359218726484));
#22700=CARTESIAN_POINT('Ctrl Pts',(-0.131211043922368,0.0736861461587066,
1.24386404077118));
#22701=CARTESIAN_POINT('Ctrl Pts',(-0.133036338837895,-0.0703371788708997,
1.25180620889396));
#22702=CARTESIAN_POINT('Ctrl Pts',(-0.0129866800356469,-0.149924422041766,
1.25974837701674));
#22703=CARTESIAN_POINT('Ctrl Pts',(0.118960111851797,-0.0921654923014072,
1.26769054513952));
#22704=CARTESIAN_POINT('Ctrl Pts',(0.141927220045961,0.050026496908035,
1.2756327132623));
#22705=CARTESIAN_POINT('Ctrl Pts',(0.0348744139414821,0.146389075532006,
1.28357488138508));
#22706=CARTESIAN_POINT('Ctrl Pts',(-0.104126938119509,0.108644221848311,
1.29151704950786));
#22707=CARTESIAN_POINT('Ctrl Pts',(-0.147737317493493,-0.0286299004949125,
1.29945921763064));
#22708=CARTESIAN_POINT('Ctrl Pts',(-0.0560051364173496,-0.139676092720537,
1.30740138575342));
#22709=CARTESIAN_POINT('Ctrl Pts',(0.0870335032532438,-0.122764634549313,
1.3153435538762));
#22710=CARTESIAN_POINT('Ctrl Pts',(0.150340512633584,0.00661184096937889,
1.32328572199898));
#22711=CARTESIAN_POINT('Ctrl Pts',(0.0759201674095095,0.129931190880528,
1.33122789012176));
#22712=CARTESIAN_POINT('Ctrl Pts',(-0.0680508508044829,0.134220221643466,
1.33917005824454));
#22713=CARTESIAN_POINT('Ctrl Pts',(-0.149680298423566,0.0155497403439283,
1.34711222636732));
#22714=CARTESIAN_POINT('Ctrl Pts',(-0.0941872156892785,-0.117365900463673,
1.3550543944901));
#22715=CARTESIAN_POINT('Ctrl Pts',(0.0475910332998192,-0.142762319241037,
1.36299656261288));
#22716=CARTESIAN_POINT('Ctrl Pts',(0.145771005694385,-0.0373737865856905,
1.37093873073566));
#22717=CARTESIAN_POINT('Ctrl Pts',(0.110409762917901,0.10225297323032,1.37888089885844));
#22718=CARTESIAN_POINT('Ctrl Pts',(-0.0260981686868614,0.148205506441964,
1.38682306698121));
#22719=CARTESIAN_POINT('Ctrl Pts',(-0.138697490589939,0.0583865667538053,
1.394765235104));
#22720=CARTESIAN_POINT('Ctrl Pts',(-0.124235673603468,-0.0849204601545819,
1.40270740322677));
#22721=CARTESIAN_POINT('Ctrl Pts',(0.0040388053119065,-0.150431633134115,
1.41064957134956));
#22722=CARTESIAN_POINT('Ctrl Pts',(0.12861328245382,-0.0781319533624403,
1.41859173947234));
#22723=CARTESIAN_POINT('Ctrl Pts',(0.1353648581188,0.0657445800149866,1.42653390759512));
#22724=CARTESIAN_POINT('Ctrl Pts',(0.0181081687242482,0.149392404544468,
1.43447607571789));
#22725=CARTESIAN_POINT('Ctrl Pts',(-0.115737181672069,0.0961812857364522,
1.44241824384068));
#22726=CARTESIAN_POINT('Ctrl Pts',(-0.143555918690644,-0.0451414811888502,
1.45036041196346));
#22727=CARTESIAN_POINT('Ctrl Pts',(-0.0398616700558823,-0.145110565703753,
1.45830258008624));
#22728=CARTESIAN_POINT('Ctrl Pts',(0.100348034367198,-0.112142416378873,
1.46624474820902));
#22729=CARTESIAN_POINT('Ctrl Pts',(0.14863229283285,0.0235577176564554,
1.4741869163318));
#22730=CARTESIAN_POINT('Ctrl Pts',(0.0607471474677608,0.137680339497592,
1.48212908445458));
#22731=CARTESIAN_POINT('Ctrl Pts',(-0.0827754224726193,0.125666453945577,
1.49007125257736));
#22732=CARTESIAN_POINT('Ctrl Pts',(-0.150492272191201,-0.00145719475437189,
1.49801342070014));
#22733=CARTESIAN_POINT('Ctrl Pts',(-0.0802951178786721,-0.12727177793954,
1.50595558882292));
#22734=CARTESIAN_POINT('Ctrl Pts',(0.0633700050447994,-0.136443062004882,
1.5138977569457));
#22735=CARTESIAN_POINT('Ctrl Pts',(0.149155357006591,-0.0207133070603065,
1.52183992506848));
#22736=CARTESIAN_POINT('Ctrl Pts',(0.0979555318420461,0.114182655252422,
1.52978209319126));
#22737=CARTESIAN_POINT('Ctrl Pts',(0.00450803278943675,0.134083974545181,
1.53507687193978));
#22738=CARTESIAN_POINT('Ctrl Pts',(-0.0361033354337414,0.122073089461022,
1.53772426131404));
#22739=CARTESIAN_POINT('Ctrl Pts',(-0.0592743564846203,0.123319225136773,
-0.00549926131403157));
#22740=CARTESIAN_POINT('Ctrl Pts',(-0.100300290071938,0.10359978715075,
-0.00285187193977157));
#22741=CARTESIAN_POINT('Ctrl Pts',(-0.160414584165772,0.0203416160441626,
0.00244290680874841));
#22742=CARTESIAN_POINT('Ctrl Pts',(-0.103922107946056,-0.124084444561314,
0.0103850749315284));
#22743=CARTESIAN_POINT('Ctrl Pts',(0.0479099321398382,-0.154436663180837,
0.0183272430543084));
#22744=CARTESIAN_POINT('Ctrl Pts',(0.155781551077148,-0.0435098515708298,
0.0262694111770884));
#22745=CARTESIAN_POINT('Ctrl Pts',(0.120977930992648,0.107381072623318,
0.0342115792998684));
#22746=CARTESIAN_POINT('Ctrl Pts',(-0.0246731903087699,0.159844935900913,
0.0421537474226484));
#22747=CARTESIAN_POINT('Ctrl Pts',(-0.147710978397823,0.0659033513787588,
0.0500959155454284));
#22748=CARTESIAN_POINT('Ctrl Pts',(-0.135435684249567,-0.0884277117007276,
0.0580380836682085));
#22749=CARTESIAN_POINT('Ctrl Pts',(0.000915427738408385,-0.16174188059703,
0.0659802517909884));
#22750=CARTESIAN_POINT('Ctrl Pts',(0.13642643003965,-0.0868880976295618,
0.0739224199137684));
#22751=CARTESIAN_POINT('Ctrl Pts',(0.146957588340267,0.0675663355536457,
0.0818645880365484));
#22752=CARTESIAN_POINT('Ctrl Pts',(0.0228600865593111,0.160121891352391,
0.0898067561593285));
#22753=CARTESIAN_POINT('Ctrl Pts',(-0.122179386207322,0.105989962368389,
0.0977489242821083));
#22754=CARTESIAN_POINT('Ctrl Pts',(-0.155290103436038,-0.0452399862206161,
0.105691092404888));
#22755=CARTESIAN_POINT('Ctrl Pts',(-0.0461390722131997,-0.155025288408554,
0.113633260527668));
#22756=CARTESIAN_POINT('Ctrl Pts',(0.105280057525145,-0.122791590307548,
0.121575428650448));
#22757=CARTESIAN_POINT('Ctrl Pts',(0.160251855424436,0.0219318669073289,
0.129517596773229));
#22758=CARTESIAN_POINT('Ctrl Pts',(0.0684164816681947,0.146563455853242,
0.137459764896008));
#22759=CARTESIAN_POINT('Ctrl Pts',(-0.086095413359615,0.136927875387926,
0.145401933018789));
#22760=CARTESIAN_POINT('Ctrl Pts',(-0.16173506727009,0.00185228698694943,
0.153344101141568));
#22761=CARTESIAN_POINT('Ctrl Pts',(-0.0892087826023274,-0.134920182928699,
0.161286269264348));
#22762=CARTESIAN_POINT('Ctrl Pts',(0.0650419110192955,-0.148091906331324,
0.169228437387128));
#22763=CARTESIAN_POINT('Ctrl Pts',(0.159707532494063,-0.025596228460074,
0.177170605509908));
#22764=CARTESIAN_POINT('Ctrl Pts',(0.108064646638443,0.120348223746572,
0.185112773632688));
#22765=CARTESIAN_POINT('Ctrl Pts',(-0.0425765573421325,0.156041339440091,
0.193054941755468));
#22766=CARTESIAN_POINT('Ctrl Pts',(-0.154213260793436,0.0487845573223287,
0.200997109878248));
#22767=CARTESIAN_POINT('Ctrl Pts',(-0.124574774400312,-0.103163891052585,
0.208939278001028));
#22768=CARTESIAN_POINT('Ctrl Pts',(0.0191870033818907,-0.160603616835255,
0.216881446123808));
#22769=CARTESIAN_POINT('Ctrl Pts',(0.145371514918136,-0.0709139301387177,
0.224823614246588));
#22770=CARTESIAN_POINT('Ctrl Pts',(0.138380784202201,0.0837402018183176,
0.232765782369368));
#22771=CARTESIAN_POINT('Ctrl Pts',(0.00461903876105218,0.161679705957985,
0.240707950492149));
#22772=CARTESIAN_POINT('Ctrl Pts',(-0.133374220718213,0.0915039894496894,
0.248650118614928));
#22773=CARTESIAN_POINT('Ctrl Pts',(-0.149182991964712,-0.0624987819548612,
0.256592286737709));
#22774=CARTESIAN_POINT('Ctrl Pts',(-0.0283248164207669,-0.159246248345813,
0.264534454860488));
#22775=CARTESIAN_POINT('Ctrl Pts',(0.118481800883715,-0.110107791262854,
0.272476622983269));
#22776=CARTESIAN_POINT('Ctrl Pts',(0.156746916480749,0.0399007144198201,
0.280418791106048));
#22777=CARTESIAN_POINT('Ctrl Pts',(0.0514157533588968,0.153356066537929,
0.288360959228829));
#22778=CARTESIAN_POINT('Ctrl Pts',(-0.101017521980764,0.126321506839912,
0.296303127351608));
#22779=CARTESIAN_POINT('Ctrl Pts',(-0.160908369261695,-0.0164365306249019,
0.304245295474388));
#22780=CARTESIAN_POINT('Ctrl Pts',(-0.0733906195540655,-0.144137017448375,
0.312187463597168));
#22781=CARTESIAN_POINT('Ctrl Pts',(0.0813604773699057,-0.13979318853071,
0.320129631719948));
#22782=CARTESIAN_POINT('Ctrl Pts',(0.161577018543625,-0.00738443741900211,
0.328071799842729));
#22783=CARTESIAN_POINT('Ctrl Pts',(0.0937724112935796,0.131789217000595,
0.336013967965508));
#22784=CARTESIAN_POINT('Ctrl Pts',(-0.0599373583072218,0.150230409426965,
0.343956136088289));
#22785=CARTESIAN_POINT('Ctrl Pts',(-0.158738350099833,0.0310451130618767,
0.351898304211068));
#22786=CARTESIAN_POINT('Ctrl Pts',(-0.112118705390683,-0.116580696253536,
0.359840472333849));
#22787=CARTESIAN_POINT('Ctrl Pts',(0.0372131918485748,-0.15740661101073,
0.367782640456628));
#22788=CARTESIAN_POINT('Ctrl Pts',(0.152453982298084,-0.0540318990865351,
0.375724808579408));
#22789=CARTESIAN_POINT('Ctrl Pts',(0.128031262769868,0.0988415833088236,
0.383666976702188));
#22790=CARTESIAN_POINT('Ctrl Pts',(-0.0136812466069205,0.161166021011634,
0.391609144824968));
#22791=CARTESIAN_POINT('Ctrl Pts',(-0.142860328563903,0.0758458262533652,
0.399551312947749));
#22792=CARTESIAN_POINT('Ctrl Pts',(-0.141164672957165,-0.0789569372907697,
0.407493481070528));
#22793=CARTESIAN_POINT('Ctrl Pts',(-0.0101476745237983,-0.161427034722196,
0.415435649193308));
#22794=CARTESIAN_POINT('Ctrl Pts',(0.130165636283581,-0.0960133843187101,
0.423377817316089));
#22795=CARTESIAN_POINT('Ctrl Pts',(0.151233851831306,0.0573583899504574,
0.431319985438868));
#22796=CARTESIAN_POINT('Ctrl Pts',(0.0337563222576384,0.158183986373718,
0.439262153561649));
#22797=CARTESIAN_POINT('Ctrl Pts',(-0.114645466422773,0.114096800420287,
0.447204321684428));
#22798=CARTESIAN_POINT('Ctrl Pts',(-0.158020229883659,-0.0345147763277912,
0.455146489807208));
#22799=CARTESIAN_POINT('Ctrl Pts',(-0.0566322287360923,-0.151507272121918,
0.463088657929988));
#22800=CARTESIAN_POINT('Ctrl Pts',(0.0966367119836487,-0.129703541718919,
0.471030826052768));
#22801=CARTESIAN_POINT('Ctrl Pts',(0.161376496659739,0.0109219578497271,
0.478972994175549));
#22802=CARTESIAN_POINT('Ctrl Pts',(0.0782788315581001,0.141541821972661,
0.486915162298328));
#22803=CARTESIAN_POINT('Ctrl Pts',(-0.0765302851406724,0.142494836024782,
0.494857330421108));
#22804=CARTESIAN_POINT('Ctrl Pts',(-0.161229798395673,0.0129079412274925,
0.502799498543889));
#22805=CARTESIAN_POINT('Ctrl Pts',(-0.0982262525537151,-0.128503953817366,
0.510741666666668));
#22806=CARTESIAN_POINT('Ctrl Pts',(0.0547626317937811,-0.152193025452748,
0.518683834789449));
#22807=CARTESIAN_POINT('Ctrl Pts',(0.157583319439253,-0.0364576503898468,
0.526626002912228));
#22808=CARTESIAN_POINT('Ctrl Pts',(0.116041497328862,0.112676677866884,
0.534568171035008));
#22809=CARTESIAN_POINT('Ctrl Pts',(-0.0318062577307366,0.158587593482618,
0.542510339157789));
#22810=CARTESIAN_POINT('Ctrl Pts',(-0.150516213127973,0.0592159811457737,
0.550452507280567));
#22811=CARTESIAN_POINT('Ctrl Pts',(-0.131337854181896,-0.0944035534094825,
0.558394675403349));
#22812=CARTESIAN_POINT('Ctrl Pts',(0.00815947204521347,-0.161539734596121,
0.566336843526128));
#22813=CARTESIAN_POINT('Ctrl Pts',(0.140181883624494,-0.080688923285235,
0.574279011648909));
#22814=CARTESIAN_POINT('Ctrl Pts',(0.143783288371658,0.0740812312429708,
0.582221179771688));
#22815=CARTESIAN_POINT('Ctrl Pts',(0.0156644295519346,0.160985367298567,
0.590163347894469));
#22816=CARTESIAN_POINT('Ctrl Pts',(-0.126804656005353,0.100410368253513,
0.598105516017247));
#22817=CARTESIAN_POINT('Ctrl Pts',(-0.153107649524464,-0.0521508436608248,
0.606047684140029));
#22818=CARTESIAN_POINT('Ctrl Pts',(-0.0391483067326994,-0.156936525122116,
0.613989852262808));
#22819=CARTESIAN_POINT('Ctrl Pts',(0.110674906884577,-0.117952226869747,
0.621932020385589));
#22820=CARTESIAN_POINT('Ctrl Pts',(0.159108535730396,0.0290884288879846,
0.629874188508368));
#22821=CARTESIAN_POINT('Ctrl Pts',(0.061782400006242,0.14948109541648,0.637816356631148));
#22822=CARTESIAN_POINT('Ctrl Pts',(-0.0921427612707386,0.132933721767072,
0.645758524753929));
#22823=CARTESIAN_POINT('Ctrl Pts',(-0.161655687038194,-0.0053945978210935,
0.653700692876707));
#22824=CARTESIAN_POINT('Ctrl Pts',(-0.0830753959589387,-0.138780911597048,
0.661642860999489));
#22825=CARTESIAN_POINT('Ctrl Pts',(0.0716104924784035,-0.145029652845349,
0.669585029122267));
#22826=CARTESIAN_POINT('Ctrl Pts',(0.160693812980115,-0.0184163326249747,
0.677527197245049));
#22827=CARTESIAN_POINT('Ctrl Pts',(0.102565092089392,0.125068240261613,
0.685469365367828));
#22828=CARTESIAN_POINT('Ctrl Pts',(-0.0495237900674707,0.153977456320057,
0.693411533490608));
#22829=CARTESIAN_POINT('Ctrl Pts',(-0.156243792750268,0.0418275036842162,
0.701353701613389));
#22830=CARTESIAN_POINT('Ctrl Pts',(-0.119828429739121,-0.108640739429086,
0.709295869736167));
#22831=CARTESIAN_POINT('Ctrl Pts',(0.0263620853553792,-0.159582904138124,
0.717238037858949));
#22832=CARTESIAN_POINT('Ctrl Pts',(0.148402221984423,-0.0643307340819919,
0.725180205981728));
#22833=CARTESIAN_POINT('Ctrl Pts',(0.134490677336207,0.0898549973406614,
0.733122374104509));
#22834=CARTESIAN_POINT('Ctrl Pts',(-0.00262814450422035,0.161724320044658,
0.741064542227287));
#22835=CARTESIAN_POINT('Ctrl Pts',(-0.137339315979238,0.0854375510170853,
0.749006710350069));
#22836=CARTESIAN_POINT('Ctrl Pts',(-0.146233564613262,-0.0691187920752458,
0.756948878472847));
#22837=CARTESIAN_POINT('Ctrl Pts',(-0.0211628449166461,-0.160355220783347,
0.764891046595629));
#22838=CARTESIAN_POINT('Ctrl Pts',(0.12329521486528,-0.104689793336152,
0.772833214718408));
#22839=CARTESIAN_POINT('Ctrl Pts',(0.154802191231926,0.0468822399980663,
0.780775382841188));
#22840=CARTESIAN_POINT('Ctrl Pts',(0.0444944569967772,0.155505325098544,
0.788717550963968));
#22841=CARTESIAN_POINT('Ctrl Pts',(-0.106574770936664,0.121669556739719,
0.796659719086747));
#22842=CARTESIAN_POINT('Ctrl Pts',(-0.160010559849905,-0.0236280251811701,
0.804601887209529));
#22843=CARTESIAN_POINT('Ctrl Pts',(-0.0668602374312443,-0.147279908636853,
0.812544055332307));
#22844=CARTESIAN_POINT('Ctrl Pts',(0.0875409312876049,-0.13600826514128,
0.820486223455089));
#22845=CARTESIAN_POINT('Ctrl Pts',(0.161745613525436,-0.000139078116330951,
0.828428391577867));
#22846=CARTESIAN_POINT('Ctrl Pts',(0.0877746970157421,0.135857518751215,
0.836370559700649));
#22847=CARTESIAN_POINT('Ctrl Pts',(-0.0666068593976089,0.147394671269449,
0.844312727823428));
#22848=CARTESIAN_POINT('Ctrl Pts',(-0.159969689820096,0.0239031624749592,
0.852254895946208));
#22849=CARTESIAN_POINT('Ctrl Pts',(-0.106783850056725,-0.121486098811777,
0.860197064068988));
#22850=CARTESIAN_POINT('Ctrl Pts',(0.0442269666803361,-0.155581612845794,
0.868139232191768));
#22851=CARTESIAN_POINT('Ctrl Pts',(0.154721338329289,-0.0471483860066884,
0.876081400314548));
#22852=CARTESIAN_POINT('Ctrl Pts',(0.123475068941597,0.104477606152275,
0.884023568437328));
#22853=CARTESIAN_POINT('Ctrl Pts',(-0.0208870486723946,0.160391377683462,
0.891965736560109));
#22854=CARTESIAN_POINT('Ctrl Pts',(-0.146114483894434,0.0693701696243073,
0.899907904682887));
#22855=CARTESIAN_POINT('Ctrl Pts',(-0.137486040957907,-0.0852012404790134,
0.907850072805669));
#22856=CARTESIAN_POINT('Ctrl Pts',(-0.00290626002629624,-0.161719561247554,
0.915792240928448));
#22857=CARTESIAN_POINT('Ctrl Pts',(0.134335953660838,-0.0900861498315643,
0.923734409051229));
#22858=CARTESIAN_POINT('Ctrl Pts',(0.148512632937768,0.0640754297319473,
0.931676577174007));
#22859=CARTESIAN_POINT('Ctrl Pts',(0.0266364831612253,0.159537332941991,
0.939618745296788));
#22860=CARTESIAN_POINT('Ctrl Pts',(-0.119641421660886,0.10884664928423,
0.947560913419568));
#22861=CARTESIAN_POINT('Ctrl Pts',(-0.156315493011378,-0.0415587473590326,
0.955503081542348));
#22862=CARTESIAN_POINT('Ctrl Pts',(-0.0497885138626987,-0.153892061929087,
0.963445249665127));
#22863=CARTESIAN_POINT('Ctrl Pts',(0.102349858952582,-0.125244437839883,
0.971387417787908));
#22864=CARTESIAN_POINT('Ctrl Pts',(0.160725246166783,0.018139958160622,
0.979329585910688));
#22865=CARTESIAN_POINT('Ctrl Pts',(0.0718597959603077,0.14490628889729,
0.987271754033468));
#22866=CARTESIAN_POINT('Ctrl Pts',(-0.0828366097831417,0.138923572215364,
0.995213922156248));
#22867=CARTESIAN_POINT('Ctrl Pts',(-0.161646170836971,0.00567259122332548,
1.00315609027903));
#22868=CARTESIAN_POINT('Ctrl Pts',(-0.0923712328620446,-0.132775066096718,
1.01109825840181));
#22869=CARTESIAN_POINT('Ctrl Pts',(0.0615252440718216,-0.149587122371362,
1.01904042652459));
#22870=CARTESIAN_POINT('Ctrl Pts',(0.159058276707423,-0.0293620068848675,
1.02698259464737));
#22871=CARTESIAN_POINT('Ctrl Pts',(0.1108775872014,0.117761723381742,1.03492476277015));
#22872=CARTESIAN_POINT('Ctrl Pts',(-0.0388783630684312,0.157003616909169,
1.04286693089293));
#22873=CARTESIAN_POINT('Ctrl Pts',(-0.153017738641585,0.0524140677533946,
1.05080909901571));
#22874=CARTESIAN_POINT('Ctrl Pts',(-0.126977145509477,-0.10019215216626,
1.05875126713849));
#22875=CARTESIAN_POINT('Ctrl Pts',(0.0153875577671049,-0.161012067570745,
1.06669343526127));
#22876=CARTESIAN_POINT('Ctrl Pts',(0.143655677305146,-0.0743283876822416,
1.07463560338405));
#22877=CARTESIAN_POINT('Ctrl Pts',(0.140320438123209,0.080447731368589,
1.08257777150683));
#22878=CARTESIAN_POINT('Ctrl Pts',(0.00843726195408678,0.161525463776335,
1.09051993962961));
#22879=CARTESIAN_POINT('Ctrl Pts',(-0.131175312957834,0.094629277223576,
1.09846210775239));
#22880=CARTESIAN_POINT('Ctrl Pts',(-0.150617825048456,-0.0589570489009974,
1.10640427587517));
#22881=CARTESIAN_POINT('Ctrl Pts',(-0.0320789358376135,-0.158532661344495,
1.11434644399795));
#22882=CARTESIAN_POINT('Ctrl Pts',(0.115847554194776,-0.112876069317329,
1.12228861212073));
#22883=CARTESIAN_POINT('Ctrl Pts',(0.157645783113317,0.0361865984037055,
1.13023078024351));
#22884=CARTESIAN_POINT('Ctrl Pts',(0.0550242791334153,0.152098624396442,
1.13817294836629));
#22885=CARTESIAN_POINT('Ctrl Pts',(-0.0980051173916675,0.128672684756662,
1.14611511648907));
#22886=CARTESIAN_POINT('Ctrl Pts',(-0.161251757937727,-0.0126306531673768,
1.15405728461185));
#22887=CARTESIAN_POINT('Ctrl Pts',(-0.0767752221903169,-0.142363015193798,
1.16199945273463));
#22888=CARTESIAN_POINT('Ctrl Pts',(0.0780353045016797,-0.141676229794458,
1.16994162085741));
#22889=CARTESIAN_POINT('Ctrl Pts',(0.161357475398708,-0.0111994629512984,
1.17788378898019));
#22890=CARTESIAN_POINT('Ctrl Pts',(0.0968596219472387,0.129537162519796,
1.18582595710297));
#22891=CARTESIAN_POINT('Ctrl Pts',(-0.0563715959749383,0.151604439264423,
1.19376812522575));
#22892=CARTESIAN_POINT('Ctrl Pts',(-0.157960640709981,0.0347864747270306,
1.20171029334853));
#22893=CARTESIAN_POINT('Ctrl Pts',(-0.114841510641486,-0.113899474410655,
1.20965246147131));
#22894=CARTESIAN_POINT('Ctrl Pts',(0.03348424129126,-0.158241803650584,
1.21759462959409));
#22895=CARTESIAN_POINT('Ctrl Pts',(0.151134988234409,-0.0576183839484237,
1.22553679771687));
#22896=CARTESIAN_POINT('Ctrl Pts',(0.130330559267559,0.0957893948119858,
1.23347896583965));
#22897=CARTESIAN_POINT('Ctrl Pts',(-0.0098700513554357,0.16144424710618,
1.24142113396243));
#22898=CARTESIAN_POINT('Ctrl Pts',(-0.141028680947982,0.0791995832534545,
1.24936330208521));
#22899=CARTESIAN_POINT('Ctrl Pts',(-0.142990550365238,-0.0756000353418,
1.25730547020799));
#22900=CARTESIAN_POINT('Ctrl Pts',(-0.013958385670676,-0.161142254877177,
1.26524763833077));
#22901=CARTESIAN_POINT('Ctrl Pts',(0.127861094297897,-0.0990616141723472,
1.27318980645355));
#22902=CARTESIAN_POINT('Ctrl Pts',(0.152546676219863,0.0537696421008814,
1.28113197457633));
#22903=CARTESIAN_POINT('Ctrl Pts',(0.0374838310097642,0.157342382244044,
1.28907414269911));
#22904=CARTESIAN_POINT('Ctrl Pts',(-0.111918054267102,0.116773335855419,
1.29701631082189));
#22905=CARTESIAN_POINT('Ctrl Pts',(-0.158791504053787,-0.0307720827589687,
1.30495847894467));
#22906=CARTESIAN_POINT('Ctrl Pts',(-0.060195622861772,-0.150127112226926,
1.31290064706745));
#22907=CARTESIAN_POINT('Ctrl Pts',(0.0935456330135535,-0.131950283756556,
1.32084281519023));
#22908=CARTESIAN_POINT('Ctrl Pts',(0.161589478720268,0.00710656041347678,
1.32878498331301));
#22909=CARTESIAN_POINT('Ctrl Pts',(0.0816007612396376,0.139653065139265,
1.33672715143579));
#22910=CARTESIAN_POINT('Ctrl Pts',(-0.0731426367739486,0.144263015132499,
1.34466931955857));
#22911=CARTESIAN_POINT('Ctrl Pts',(-0.160879865135934,0.0167132224867059,
1.35261148768135));
#22912=CARTESIAN_POINT('Ctrl Pts',(-0.101234609479067,-0.126147598829082,
1.36055365580413));
#22913=CARTESIAN_POINT('Ctrl Pts',(0.051151949184981,-0.153444260252591,
1.36849582392691));
#22914=CARTESIAN_POINT('Ctrl Pts',(0.15667806641111,-0.0401702148435725,
1.37643799204969));
#22915=CARTESIAN_POINT('Ctrl Pts',(0.118670980449659,0.10990387323047,1.38438016017247));
#22916=CARTESIAN_POINT('Ctrl Pts',(-0.0280509185434417,0.159294724422008,
1.39232232829525));
#22917=CARTESIAN_POINT('Ctrl Pts',(-0.149075287902345,0.0627552395607943,
1.40026449641803));
#22918=CARTESIAN_POINT('Ctrl Pts',(-0.133531390736797,-0.0912744851582948,
1.40820666454081));
#22919=CARTESIAN_POINT('Ctrl Pts',(0.00434100186018791,-0.161687417152987,
1.41614883266359));
#22920=CARTESIAN_POINT('Ctrl Pts',(0.138236546518021,-0.0839780402106489,
1.42409100078637));
#22921=CARTESIAN_POINT('Ctrl Pts',(0.145493297031458,0.07066380330362,1.43203316890915));
#22922=CARTESIAN_POINT('Ctrl Pts',(0.0194630807988606,0.160570430100525,
1.43997533703193));
#22923=CARTESIAN_POINT('Ctrl Pts',(-0.124397014000637,0.103377882332206,
1.44791750515471));
#22924=CARTESIAN_POINT('Ctrl Pts',(-0.15429723939393,-0.0485191136187331,
1.45585967327749));
#22925=CARTESIAN_POINT('Ctrl Pts',(-0.042844249846,-0.155968210152522,1.46380184140027));
#22926=CARTESIAN_POINT('Ctrl Pts',(0.107856400646442,-0.120533276677448,
1.47174400952305));
#22927=CARTESIAN_POINT('Ctrl Pts',(0.159753444358638,0.0253203827049868,
1.47968617764583));
#22928=CARTESIAN_POINT('Ctrl Pts',(0.0652924466007548,0.147982030257331,
1.48762834576861));
#22929=CARTESIAN_POINT('Ctrl Pts',(-0.0889689487809616,0.13506922671723,
1.49557051389139));
#22930=CARTESIAN_POINT('Ctrl Pts',(-0.161752593421533,-0.00156622680492735,
1.50351268201417));
#22931=CARTESIAN_POINT('Ctrl Pts',(-0.086303059730943,-0.136794666273195,
1.51145485013695));
#22932=CARTESIAN_POINT('Ctrl Pts',(0.0681115549116652,-0.14665217563879,
1.51939701825973));
#22933=CARTESIAN_POINT('Ctrl Pts',(0.160315645894948,-0.02226314405755,
1.52733918638251));
#22934=CARTESIAN_POINT('Ctrl Pts',(0.105284883301553,0.122726172858702,
1.53528135450529));
#22935=CARTESIAN_POINT('Ctrl Pts',(0.00484533846358528,0.144116573583224,
1.54057613325381));
#22936=CARTESIAN_POINT('Ctrl Pts',(-0.0388047044047284,0.131206995015745,
1.54322352262807));
#22937=CARTESIAN_POINT('Ctrl Pts',(-0.0634007094575145,0.131904027763688,
-3.88578058618805E-16));
#22938=CARTESIAN_POINT('Ctrl Pts',(-0.107282641710421,0.110811831533068,
0.00264738937425961));
#22939=CARTESIAN_POINT('Ctrl Pts',(-0.171581760589518,0.0217576868851663,
0.0079421681227796));
#22940=CARTESIAN_POINT('Ctrl Pts',(-0.111156590520044,-0.1327225175337,
0.0158843362455596));
#22941=CARTESIAN_POINT('Ctrl Pts',(0.0512451567233008,-0.165187689797298,
0.0238265043683396));
#22942=CARTESIAN_POINT('Ctrl Pts',(0.16662620135312,-0.0465387668729445,
0.0317686724911196));
#22943=CARTESIAN_POINT('Ctrl Pts',(0.129399745666171,0.114856349193662,
0.0397108406138996));
#22944=CARTESIAN_POINT('Ctrl Pts',(-0.026390801400978,0.170972456562021,
0.0476530087366796));
#22945=CARTESIAN_POINT('Ctrl Pts',(-0.157993800025737,0.070491178324729,
0.0555951768594596));
#22946=CARTESIAN_POINT('Ctrl Pts',(-0.144863967768493,-0.0945835600760224,
0.0635373449822396));
#22947=CARTESIAN_POINT('Ctrl Pts',(0.000979154756195248,-0.17300145605975,
0.0714795131050195));
#22948=CARTESIAN_POINT('Ctrl Pts',(0.145923683802689,-0.0929367665856833,
0.0794216812277997));
#22949=CARTESIAN_POINT('Ctrl Pts',(0.157187963117837,0.0722699302633024,
0.0873638493505794));
#22950=CARTESIAN_POINT('Ctrl Pts',(0.0244514793930555,0.171268692120756,
0.0953060174733598));
#22951=CARTESIAN_POINT('Ctrl Pts',(-0.130684839550095,0.113368397534175,
0.103248185596139));
#22952=CARTESIAN_POINT('Ctrl Pts',(-0.166100541844429,-0.0483893439312075,
0.11119035371892));
#22953=CARTESIAN_POINT('Ctrl Pts',(-0.0493510193195793,-0.165817291858885,
0.119132521841699));
#22954=CARTESIAN_POINT('Ctrl Pts',(0.112609073040783,-0.131339661914923,
0.12707468996448));
#22955=CARTESIAN_POINT('Ctrl Pts',(0.17140770357293,0.0234586422209967,
0.135016858087259));
#22956=CARTESIAN_POINT('Ctrl Pts',(0.0731792588499177,0.156766393306209,
0.14295902621004));
#22957=CARTESIAN_POINT('Ctrl Pts',(-0.0920889000195865,0.146460037003638,
0.150901194332819));
#22958=CARTESIAN_POINT('Ctrl Pts',(-0.172994168426659,0.00198123296575728,
0.1588433624556));
#22959=CARTESIAN_POINT('Ctrl Pts',(-0.0954190048152776,-0.144312580095855,
0.16678553057838));
#22960=CARTESIAN_POINT('Ctrl Pts',(0.0695697692503139,-0.158401246055831,
0.17472769870116));
#22961=CARTESIAN_POINT('Ctrl Pts',(0.170825487889685,-0.0273780963649298,
0.18266986682394));
#22962=CARTESIAN_POINT('Ctrl Pts',(0.115587509852263,0.128726201683253,
0.19061203494672));
#22963=CARTESIAN_POINT('Ctrl Pts',(-0.0455405018601966,0.16690407474553,
0.198554203069499));
#22964=CARTESIAN_POINT('Ctrl Pts',(-0.164948735370872,0.0521806684752238,
0.20649637119228));
#22965=CARTESIAN_POINT('Ctrl Pts',(-0.133246981425072,-0.110345590758605,
0.214438539315059));
#22966=CARTESIAN_POINT('Ctrl Pts',(0.0205226964731592,-0.171783952668295,
0.22238070743784));
#22967=CARTESIAN_POINT('Ctrl Pts',(0.155491476033395,-0.0758505658746651,
0.230322875560619));
#22968=CARTESIAN_POINT('Ctrl Pts',(0.148014089296488,0.0895697316726553,
0.2382650436834));
#22969=CARTESIAN_POINT('Ctrl Pts',(0.00494059070111224,0.172934953166096,
0.24620721180618));
#22970=CARTESIAN_POINT('Ctrl Pts',(-0.142658996543838,0.0978739912732451,
0.25414937992896));
#22971=CARTESIAN_POINT('Ctrl Pts',(-0.159568287038446,-0.0668496016012732,
0.262091548051739));
#22972=CARTESIAN_POINT('Ctrl Pts',(-0.0302966335331915,-0.170332091689456,
0.27003371617452));
#22973=CARTESIAN_POINT('Ctrl Pts',(0.126729848780061,-0.11777288690896,
0.2779758842973));
#22974=CARTESIAN_POINT('Ctrl Pts',(0.167658770158652,0.0426783815482623,
0.28591805242008));
#22975=CARTESIAN_POINT('Ctrl Pts',(0.0549950338320791,0.164031867990689,
0.293860220542859));
#22976=CARTESIAN_POINT('Ctrl Pts',(-0.108049803339193,0.135115311719503,
0.30180238866564));
#22977=CARTESIAN_POINT('Ctrl Pts',(-0.1721099202737,-0.0175807510100837,
0.309744556788419));
#22978=CARTESIAN_POINT('Ctrl Pts',(-0.0784996687135917,-0.154171039675278,
0.3176867249112));
#22979=CARTESIAN_POINT('Ctrl Pts',(0.087024343965547,-0.14952481740522,
0.325628893033979));
#22980=CARTESIAN_POINT('Ctrl Pts',(0.172825117221703,-0.00789850112384905,
0.33357106115676));
#22981=CARTESIAN_POINT('Ctrl Pts',(0.100300328103893,0.140963653630822,
0.341513229279539));
#22982=CARTESIAN_POINT('Ctrl Pts',(-0.0641098658012952,0.160688619913292,
0.349455397402319));
#22983=CARTESIAN_POINT('Ctrl Pts',(-0.16978883637574,0.033206302186043,
0.357397565525099));
#22984=CARTESIAN_POINT('Ctrl Pts',(-0.119923789760104,-0.124696399756661,
0.36533973364788));
#22985=CARTESIAN_POINT('Ctrl Pts',(0.0398037685148125,-0.168364388974385,
0.373281901770659));
#22986=CARTESIAN_POINT('Ctrl Pts',(0.163066985633654,-0.0577933011607096,
0.38122406989344));
#22987=CARTESIAN_POINT('Ctrl Pts',(0.136944091404129,0.10572238784759,0.38916623801622));
#22988=CARTESIAN_POINT('Ctrl Pts',(-0.0146336593526265,0.172385508313924,
0.397108406138999));
#22989=CARTESIAN_POINT('Ctrl Pts',(-0.152805474769431,0.0811257933285562,
0.40505057426178));
#22990=CARTESIAN_POINT('Ctrl Pts',(-0.150991776994562,-0.0844534827151793,
0.412992742384559));
#22991=CARTESIAN_POINT('Ctrl Pts',(-0.0108540995180527,-0.172664692355881,
0.42093491050734));
#22992=CARTESIAN_POINT('Ctrl Pts',(0.139227048201004,-0.102697305280782,
0.428877078630119));
#22993=CARTESIAN_POINT('Ctrl Pts',(0.16176191642983,0.0613513639265466,
0.4368192467529));
#22994=CARTESIAN_POINT('Ctrl Pts',(0.0361062507758455,0.169195880912067,
0.444761414875679));
#22995=CARTESIAN_POINT('Ctrl Pts',(-0.12262644992489,0.12203958882886,0.45270358299846));
#22996=CARTESIAN_POINT('Ctrl Pts',(-0.169020724600573,-0.0369175042249048,
0.460645751121239));
#22997=CARTESIAN_POINT('Ctrl Pts',(-0.0605746513833496,-0.162054370729346,
0.468587919244019));
#22998=CARTESIAN_POINT('Ctrl Pts',(0.103364025571403,-0.138732785167649,
0.4765300873668));
#22999=CARTESIAN_POINT('Ctrl Pts',(0.172610636112938,0.0116822841681558,
0.484472255489579));
#23000=CARTESIAN_POINT('Ctrl Pts',(0.083728171010617,0.151395181039277,
0.49241442361236));
#23001=CARTESIAN_POINT('Ctrl Pts',(-0.081857900459256,0.152414538660527,
0.500356591735139));
#23002=CARTESIAN_POINT('Ctrl Pts',(-0.172453725526818,0.0138065207282529,
0.50829875985792));
#23003=CARTESIAN_POINT('Ctrl Pts',(-0.105064221167447,-0.137449688588867,
0.516240927980699));
#23004=CARTESIAN_POINT('Ctrl Pts',(0.0585749034388466,-0.162787862415564,
0.52418309610348));
#23005=CARTESIAN_POINT('Ctrl Pts',(0.168553398866689,-0.0389956304370821,
0.532125264226259));
#23006=CARTESIAN_POINT('Ctrl Pts',(0.124119664784058,0.120520605195094,
0.54006743234904));
#23007=CARTESIAN_POINT('Ctrl Pts',(-0.0340204335384149,0.16962758491636,
0.548009600471819));
#23008=CARTESIAN_POINT('Ctrl Pts',(-0.160994319687769,0.0633382703503284,
0.5559517685946));
#23009=CARTESIAN_POINT('Ctrl Pts',(-0.14048086942825,-0.100975406844349,
0.563893936717379));
#23010=CARTESIAN_POINT('Ctrl Pts',(0.00872748937560605,-0.172785237771916,
0.57183610484016));
#23011=CARTESIAN_POINT('Ctrl Pts',(0.149940571302356,-0.0863060399984934,
0.579778272962939));
#23012=CARTESIAN_POINT('Ctrl Pts',(0.153792685935992,0.0792383569699183,
0.58772044108572));
#23013=CARTESIAN_POINT('Ctrl Pts',(0.0167549005293281,0.17219227848818,
0.595662609208499));
#23014=CARTESIAN_POINT('Ctrl Pts',(-0.135632095058532,0.107400382926376,
0.60360477733128));
#23015=CARTESIAN_POINT('Ctrl Pts',(-0.163766157558233,-0.0557812970565469,
0.611546945454059));
#23016=CARTESIAN_POINT('Ctrl Pts',(-0.0418735953979919,-0.167861578305293,
0.61948911357684));
#23017=CARTESIAN_POINT('Ctrl Pts',(0.118379481984711,-0.126163408751231,
0.627431281699619));
#23018=CARTESIAN_POINT('Ctrl Pts',(0.17018479228316,0.0311134044783985,
0.6353734498224));
#23019=CARTESIAN_POINT('Ctrl Pts',(0.0660833491022344,0.159887142804326,
0.643315617945179));
#23020=CARTESIAN_POINT('Ctrl Pts',(-0.0985572308567358,0.142187832491218,
0.651257786067961));
#23021=CARTESIAN_POINT('Ctrl Pts',(-0.172909262181909,-0.00577013989488307,
0.659199954190738));
#23022=CARTESIAN_POINT('Ctrl Pts',(-0.0888586457050277,-0.148442071348278,
0.667142122313521));
#23023=CARTESIAN_POINT('Ctrl Pts',(0.0765956190331784,-0.155125815413241,
0.675084290436298));
#23024=CARTESIAN_POINT('Ctrl Pts',(0.171880427770071,-0.0196983758791502,
0.683026458559081));
#23025=CARTESIAN_POINT('Ctrl Pts',(0.109705106722326,0.133774799651286,
0.690968626681858));
#23026=CARTESIAN_POINT('Ctrl Pts',(-0.0529713625168984,0.164696515493808,
0.698910794804641));
#23027=CARTESIAN_POINT('Ctrl Pts',(-0.167120621735807,0.0447393032280997,
0.706852962927418));
#23028=CARTESIAN_POINT('Ctrl Pts',(-0.12817022249092,-0.116203707037801,
0.7147951310502));
#23029=CARTESIAN_POINT('Ctrl Pts',(0.0281972679828983,-0.17069218359667,
0.722737299172979));
#23030=CARTESIAN_POINT('Ctrl Pts',(0.158733164168978,-0.0688090841067,0.73067946729576));
#23031=CARTESIAN_POINT('Ctrl Pts',(0.14385317469873,0.0961102054508026,
0.738621635418538));
#23032=CARTESIAN_POINT('Ctrl Pts',(-0.00281110139369983,0.172982673038814,
0.746563803541321));
#23033=CARTESIAN_POINT('Ctrl Pts',(-0.146900119814081,0.0913852409380608,
0.754505971664098));
#23034=CARTESIAN_POINT('Ctrl Pts',(-0.156413536862055,-0.0739304602244656,
0.762448139786881));
#23035=CARTESIAN_POINT('Ctrl Pts',(-0.0226360851712103,-0.171518264656626,
0.770390307909658));
#23036=CARTESIAN_POINT('Ctrl Pts',(0.131878346029848,-0.111977717922496,
0.778332476032441));
#23037=CARTESIAN_POINT('Ctrl Pts',(0.165578663890314,0.0501459223366878,
0.786274644155218));
#23038=CARTESIAN_POINT('Ctrl Pts',(0.047591915084802,0.166330746049129,
0.794216812278001));
#23039=CARTESIAN_POINT('Ctrl Pts',(-0.113993917241593,0.130139518573781,
0.802158980400778));
#23040=CARTESIAN_POINT('Ctrl Pts',(-0.171149610334614,-0.0252728776558711,
0.81010114852356));
#23041=CARTESIAN_POINT('Ctrl Pts',(-0.0715146774936035,-0.157532721571376,
0.818043316646339));
#23042=CARTESIAN_POINT('Ctrl Pts',(0.0936350469135118,-0.14547640857611,
0.825985484769119));
#23043=CARTESIAN_POINT('Ctrl Pts',(0.173005448853992,-0.000148759965830227,
0.8339276528919));
#23044=CARTESIAN_POINT('Ctrl Pts',(0.0938850861191564,0.145315168055841,
0.841869821014678));
#23045=CARTESIAN_POINT('Ctrl Pts',(-0.0712436606821878,0.157655473343934,
0.849811989137461));
#23046=CARTESIAN_POINT('Ctrl Pts',(-0.171105895159299,0.0255671684868261,
0.857754157260238));
#23047=CARTESIAN_POINT('Ctrl Pts',(-0.114217551294,-0.129943289319231,0.86569632538302));
#23048=CARTESIAN_POINT('Ctrl Pts',(0.0473058035714782,-0.166412344527548,
0.873638493505798));
#23049=CARTESIAN_POINT('Ctrl Pts',(0.16549218245563,-0.0504305959589149,
0.88158066162858));
#23050=CARTESIAN_POINT('Ctrl Pts',(0.132070720552549,0.111750759440056,
0.889522829751358));
#23051=CARTESIAN_POINT('Ctrl Pts',(-0.022341089517305,0.171556938600217,
0.89746499787414));
#23052=CARTESIAN_POINT('Ctrl Pts',(-0.156286166401977,0.074199337288632,
0.905407165996919));
#23053=CARTESIAN_POINT('Ctrl Pts',(-0.147057058974526,-0.0911324797668838,
0.913349334119699));
#23054=CARTESIAN_POINT('Ctrl Pts',(-0.00310857778072832,-0.172977582960567,
0.92129150224248));
#23055=CARTESIAN_POINT('Ctrl Pts',(0.143687680016546,-0.0963574495000853,
0.929233670365259));
#23056=CARTESIAN_POINT('Ctrl Pts',(0.158851261322436,0.0685360068793772,
0.93717583848804));
#23057=CARTESIAN_POINT('Ctrl Pts',(0.0284907678468484,0.170643439985825,
0.945118006610819));
#23058=CARTESIAN_POINT('Ctrl Pts',(-0.127970195944242,0.116423951198588,
0.9530601747336));
#23059=CARTESIAN_POINT('Ctrl Pts',(-0.167197313372666,-0.0444518375735043,
0.961002342856378));
#23060=CARTESIAN_POINT('Ctrl Pts',(-0.0532545149190986,-0.164605176417482,
0.96894451097916));
#23061=CARTESIAN_POINT('Ctrl Pts',(0.10947489024455,-0.133963263130763,
0.976886679101939));
#23062=CARTESIAN_POINT('Ctrl Pts',(0.1719140491614,0.0194027617526574,0.984828847224719));
#23063=CARTESIAN_POINT('Ctrl Pts',(0.0768622776450996,0.154993863549195,
0.992771015347499));
#23064=CARTESIAN_POINT('Ctrl Pts',(-0.088603236555915,0.148594663210074,
1.00071318347028));
#23065=CARTESIAN_POINT('Ctrl Pts',(-0.172899083515371,0.00606748566075909,
1.00865535159306));
#23066=CARTESIAN_POINT('Ctrl Pts',(-0.0988016073770141,-0.142018132090297,
1.01659751971584));
#23067=CARTESIAN_POINT('Ctrl Pts',(0.0658082913934689,-0.160000550769587,
1.02453968783862));
#23068=CARTESIAN_POINT('Ctrl Pts',(0.170131034504888,-0.0314060274628177,
1.0324818559614));
#23069=CARTESIAN_POINT('Ctrl Pts',(0.118596271784576,0.125959643463681,
1.04042402408418));
#23070=CARTESIAN_POINT('Ctrl Pts',(-0.0415848597483297,0.167933340651612,
1.04836619220696));
#23071=CARTESIAN_POINT('Ctrl Pts',(-0.163669987576804,0.0560628453550813,
1.05630836032974));
#23072=CARTESIAN_POINT('Ctrl Pts',(-0.135816592328243,-0.107166975841641,
1.06425052845252));
#23073=CARTESIAN_POINT('Ctrl Pts',(0.0164587544616562,-0.172220837485682,
1.0721926965753));
#23074=CARTESIAN_POINT('Ctrl Pts',(0.153656191292587,-0.0795027190739688,
1.08013486469808));
#23075=CARTESIAN_POINT('Ctrl Pts',(0.150088771199207,0.0860480576341552,
1.08807703282086));
#23076=CARTESIAN_POINT('Ctrl Pts',(0.00902461748204118,0.172769973496559,
1.09601920094364));
#23077=CARTESIAN_POINT('Ctrl Pts',(-0.140307012982855,0.101216844302358,
1.10396136906642));
#23078=CARTESIAN_POINT('Ctrl Pts',(-0.161103005268346,-0.0630613126743013,
1.1119035371892));
#23079=CARTESIAN_POINT('Ctrl Pts',(-0.0343120939874615,-0.1695688287065,
1.11984570531198));
#23080=CARTESIAN_POINT('Ctrl Pts',(0.123912220401285,-0.120733877175888,
1.12778787343476));
#23081=CARTESIAN_POINT('Ctrl Pts',(0.168620210916381,0.0387057093103061,
1.13573004155754));
#23082=CARTESIAN_POINT('Ctrl Pts',(0.0588547652196237,0.162686889679659,
1.14367220968032));
#23083=CARTESIAN_POINT('Ctrl Pts',(-0.104827691798069,0.137630165643247,
1.1516143778031));
#23084=CARTESIAN_POINT('Ctrl Pts',(-0.172477213770776,-0.0135099294065116,
1.15955654592588));
#23085=CARTESIAN_POINT('Ctrl Pts',(-0.0821198886720452,-0.152273541192125,
1.16749871404866));
#23086=CARTESIAN_POINT('Ctrl Pts',(0.083467690946984,-0.15153894559049,
1.17544088217144));
#23087=CARTESIAN_POINT('Ctrl Pts',(0.172590290696882,-0.0119791076405788,
1.18338305029422));
#23088=CARTESIAN_POINT('Ctrl Pts',(0.103602453294194,0.13855482356859,1.191325218417));
#23089=CARTESIAN_POINT('Ctrl Pts',(-0.0602958748103966,0.162158302111078,
1.19926738653978));
#23090=CARTESIAN_POINT('Ctrl Pts',(-0.168956987158091,0.0372081167644847,
1.20720955466256));
#23091=CARTESIAN_POINT('Ctrl Pts',(-0.122836141658186,-0.121828526073448,
1.21515172278534));
#23092=CARTESIAN_POINT('Ctrl Pts',(0.0358152290369173,-0.169257723108079,
1.22309389090812));
#23093=CARTESIAN_POINT('Ctrl Pts',(0.161656170495932,-0.0616294572691503,
1.2310360590309));
#23094=CARTESIAN_POINT('Ctrl Pts',(0.13940345221127,0.102457722863032,1.23897822715368));
#23095=CARTESIAN_POINT('Ctrl Pts',(-0.0105571497596809,0.172683102970871,
1.24692039527646));
#23096=CARTESIAN_POINT('Ctrl Pts',(-0.150846317973597,0.0847130203482025,
1.25486256339924));
#23097=CARTESIAN_POINT('Ctrl Pts',(-0.152944761892581,-0.0808628918127005,
1.26280473152202));
#23098=CARTESIAN_POINT('Ctrl Pts',(-0.0149300913057054,-0.172360087712588,
1.2707468996448));
#23099=CARTESIAN_POINT('Ctrl Pts',(0.136762076743997,-0.105957736043287,
1.27868906776758));
#23100=CARTESIAN_POINT('Ctrl Pts',(0.163166132393764,0.0575127872937276,
1.28663123589036));
#23101=CARTESIAN_POINT('Ctrl Pts',(0.0400932480780463,0.168295688956082,
1.29457340401314));
#23102=CARTESIAN_POINT('Ctrl Pts',(-0.119709170414695,0.124902449862528,
1.30251557213592));
#23103=CARTESIAN_POINT('Ctrl Pts',(-0.169845690614082,-0.0329142650230248,
1.3104577402587));
#23104=CARTESIAN_POINT('Ctrl Pts',(-0.0643861093061943,-0.160578131733314,
1.31839990838148));
#23105=CARTESIAN_POINT('Ctrl Pts',(0.100057762773863,-0.141135932963798,
1.32634207650426));
#23106=CARTESIAN_POINT('Ctrl Pts',(0.172838444806952,0.00760127985757451,
1.33428424462704));
#23107=CARTESIAN_POINT('Ctrl Pts',(0.0872813550697656,0.149374939398002,
1.34222641274982));
#23108=CARTESIAN_POINT('Ctrl Pts',(-0.0782344227434143,0.154305808621531,
1.3501685808726));
#23109=CARTESIAN_POINT('Ctrl Pts',(-0.172079431848303,0.0178767046294837,
1.35811074899538));
#23110=CARTESIAN_POINT('Ctrl Pts',(-0.108282003268856,-0.134929297194493,
1.36605291711816));
#23111=CARTESIAN_POINT('Ctrl Pts',(0.0547128650701426,-0.164126201264144,
1.37399508524094));
#23112=CARTESIAN_POINT('Ctrl Pts',(0.167585127127835,-0.0429666431014547,
1.38193725336372));
#23113=CARTESIAN_POINT('Ctrl Pts',(0.126932197981417,0.117554773230619,
1.3898794214865));
#23114=CARTESIAN_POINT('Ctrl Pts',(-0.0300036684000219,0.170383942402052,
1.39782158960928));
#23115=CARTESIAN_POINT('Ctrl Pts',(-0.159453085214751,0.0671239123677834,
1.40576375773206));
#23116=CARTESIAN_POINT('Ctrl Pts',(-0.142827107870127,-0.0976285101620078,
1.41370592585484));
#23117=CARTESIAN_POINT('Ctrl Pts',(0.00464319840846943,-0.172943201171859,
1.42164809397762));
#23118=CARTESIAN_POINT('Ctrl Pts',(0.147859810582222,-0.0898241270588577,
1.4295902621004));
#23119=CARTESIAN_POINT('Ctrl Pts',(0.155621735944117,0.0755830265922534,
1.43753243022318));
#23120=CARTESIAN_POINT('Ctrl Pts',(0.0208179928734729,0.171748455656582,
1.44547459834596));
#23121=CARTESIAN_POINT('Ctrl Pts',(-0.133056846329205,0.11057447892796,
1.45341676646874));
#23122=CARTESIAN_POINT('Ctrl Pts',(-0.165038560097216,-0.0518967460486161,
1.46135893459152));
#23123=CARTESIAN_POINT('Ctrl Pts',(-0.0458268296361176,-0.166825854601292,
1.4693011027143));
#23124=CARTESIAN_POINT('Ctrl Pts',(0.115364766925686,-0.128924136976022,
1.47724327083708));
#23125=CARTESIAN_POINT('Ctrl Pts',(0.170874595884426,0.0270830477535184,
1.48518543895986));
#23126=CARTESIAN_POINT('Ctrl Pts',(0.0698377457337486,0.158283721017069,
1.49312760708264));
#23127=CARTESIAN_POINT('Ctrl Pts',(-0.0951624750893037,0.144471999488883,
1.50106977520542));
#23128=CARTESIAN_POINT('Ctrl Pts',(-0.173012914651864,-0.00167525885548286,
1.5090119433282));
#23129=CARTESIAN_POINT('Ctrl Pts',(-0.092311001583214,-0.14631755460685,
1.51695411145098));
#23130=CARTESIAN_POINT('Ctrl Pts',(0.072853104778531,-0.156861289272697,
1.52489627957376));
#23131=CARTESIAN_POINT('Ctrl Pts',(0.171475934783304,-0.0238129810547936,
1.53283844769654));
#23132=CARTESIAN_POINT('Ctrl Pts',(0.11261423476106,0.131269690464983,1.54078061581932));
#23133=CARTESIAN_POINT('Ctrl Pts',(0.00518264413773371,0.154149172621267,
1.54607539456784));
#23134=CARTESIAN_POINT('Ctrl Pts',(-0.0415060733757155,0.140340900570467,
1.5487227839421));
#23135=CARTESIAN_POINT('Ctrl Pts',(-0.146248097568756,-0.000123763188177425,
1.45893449541571));
#23136=CARTESIAN_POINT('Ctrl Pts',(-0.146367493381718,-0.0150081347743067,
1.45974264180765));
#23137=CARTESIAN_POINT('Ctrl Pts',(-0.144277648885518,-0.0298597803798721,
1.46055078819958));
#23138=CARTESIAN_POINT('Ctrl Pts',(-0.139839652725699,-0.043973059977961,
1.46135893459152));
#23139=CARTESIAN_POINT('Ctrl Pts',(-0.125301316610186,-0.0902064488995044,
1.46400632396578));
#23140=CARTESIAN_POINT('Ctrl Pts',(-0.08556407312315,-0.1285161517504,1.46665371334004));
#23141=CARTESIAN_POINT('Ctrl Pts',(-0.0388301852859989,-0.141354050238301,
1.4693011027143));
#23142=CARTESIAN_POINT('Ctrl Pts',(0.00790370255115092,-0.154191948726202,
1.47194849208856));
#23143=CARTESIAN_POINT('Ctrl Pts',(0.0616342347384179,-0.141558042851112,
1.47459588146282));
#23144=CARTESIAN_POINT('Ctrl Pts',(0.0977511389918415,-0.109239892458645,
1.47724327083708));
#23145=CARTESIAN_POINT('Ctrl Pts',(0.133868043245265,-0.0769217420661769,
1.47989066021134));
#23146=CARTESIAN_POINT('Ctrl Pts',(0.152371319564846,-0.024919347156331,
1.4825380495856));
#23147=CARTESIAN_POINT('Ctrl Pts',(0.144783482699524,0.0229486291758506,
1.48518543895986));
#23148=CARTESIAN_POINT('Ctrl Pts',(0.137195645834202,0.0708166055080336,
1.48783282833412));
#23149=CARTESIAN_POINT('Ctrl Pts',(0.103516695783975,0.114550163262552,
1.49048021770838));
#23150=CARTESIAN_POINT('Ctrl Pts',(0.0591771839550196,0.13411498855178,
1.49312760708264));
#23151=CARTESIAN_POINT('Ctrl Pts',(0.014837672126065,0.153679813841007,
1.4957749964569));
#23152=CARTESIAN_POINT('Ctrl Pts',(-0.0401624014816186,0.149075906664945,
1.49842238583116));
#23153=CARTESIAN_POINT('Ctrl Pts',(-0.0806375115458872,0.122416076686187,
1.50106977520542));
#23154=CARTESIAN_POINT('Ctrl Pts',(-0.0937869288003098,0.113754921033589,
1.50192985013695));
#23155=CARTESIAN_POINT('Ctrl Pts',(-0.105403311347291,0.102765876910903,
1.50278992506847));
#23156=CARTESIAN_POINT('Ctrl Pts',(-0.115078604842433,0.0902138214954038,
1.50365));
#23157=CARTESIAN_POINT('Ctrl Pts',(-0.0686146973663081,-0.0959584553529135,
1.07336015076065E-17));
#23158=CARTESIAN_POINT('Ctrl Pts',(-0.0712979561985307,-0.0944995001033786,
9.02613639135873E-18));
#23159=CARTESIAN_POINT('Ctrl Pts',(-0.0739152333025289,-0.0929325179580126,
1.64107321374712E-17));
#23160=CARTESIAN_POINT('Ctrl Pts',(-0.0764591723283171,-0.0912589988675934,
1.6154612370034E-17));
#23161=CARTESIAN_POINT('Ctrl Pts',(-0.0824897891353913,-0.0872917841461184,
1.52077426268717E-17));
#23162=CARTESIAN_POINT('Ctrl Pts',(-0.0881090519769445,-0.0827275518978924,
1.30971627060498E-17));
#23163=CARTESIAN_POINT('Ctrl Pts',(-0.0932912133381108,-0.0776621329443405,
1.43114686768087E-17));
#23164=CARTESIAN_POINT('Ctrl Pts',(-0.0960634919631888,-0.074952307504085,
1.49610807310118E-17));
#23165=CARTESIAN_POINT('Ctrl Pts',(-0.0987043519497191,-0.0721043812799658,
1.74993329480528E-17));
#23166=CARTESIAN_POINT('Ctrl Pts',(-0.101206237074718,-0.0691378820326018,
9.97465998686664E-18));
#23167=CARTESIAN_POINT('Ctrl Pts',(-0.105823426721714,-0.0636632543305198,
-3.91200561030858E-18));
#23168=CARTESIAN_POINT('Ctrl Pts',(-0.109972666997065,-0.0577811896139199,
2.24798207762934E-18));
#23169=CARTESIAN_POINT('Ctrl Pts',(-0.113625452403263,-0.0515741981665521,
9.54097911787244E-18));
#23170=CARTESIAN_POINT('Ctrl Pts',(-0.115386295340069,-0.0485820878086944,
1.30566037435822E-17));
#23171=CARTESIAN_POINT('Ctrl Pts',(-0.117027309103105,-0.0455212415157476,
-2.79521757168051E-18));
#23172=CARTESIAN_POINT('Ctrl Pts',(-0.118543833519887,-0.0424058589801268,
-3.46944695195361E-18));
#23173=CARTESIAN_POINT('Ctrl Pts',(-0.122700941917732,-0.0338659484069709,
-5.31764971597768E-18));
#23174=CARTESIAN_POINT('Ctrl Pts',(-0.125931492798984,-0.0249085743588085,
-1.15219401683824E-18));
#23175=CARTESIAN_POINT('Ctrl Pts',(-0.128167520083254,-0.0157105262534848,
9.54097911787244E-18));
#23176=CARTESIAN_POINT('Ctrl Pts',(-0.128992166906242,-0.0123182862745252,
1.3484621181291E-17));
#23177=CARTESIAN_POINT('Ctrl Pts',(-0.129681150280034,-0.00889298553317688,
1.10989611676181E-17));
#23178=CARTESIAN_POINT('Ctrl Pts',(-0.130229483957028,-0.00544263935519351,
9.54097911787244E-18));
#23179=CARTESIAN_POINT('Ctrl Pts',(-0.130761899349706,-0.00209245771889707,
8.02822573502553E-18));
#23180=CARTESIAN_POINT('Ctrl Pts',(-0.131160261982709,0.00127366115726457,
1.11791151702242E-17));
#23181=CARTESIAN_POINT('Ctrl Pts',(-0.131420990891747,0.00464012593483382,
8.67361737988404E-18));
#23182=CARTESIAN_POINT('Ctrl Pts',(-0.131728666658755,0.00861275649723166,
5.71697955546795E-18));
#23183=CARTESIAN_POINT('Ctrl Pts',(-0.131845259942619,0.0125891451047215,
-9.26473565962443E-18));
#23184=CARTESIAN_POINT('Ctrl Pts',(-0.131765781147177,0.0165567997877194,
-1.04083408558608E-17));
#23185=CARTESIAN_POINT('Ctrl Pts',(-0.131635692412819,0.0230509492424239,
-1.21888544026837E-17));
#23186=CARTESIAN_POINT('Ctrl Pts',(-0.13098103789945,0.0295216962360144,
-2.67049856555875E-17));
#23187=CARTESIAN_POINT('Ctrl Pts',(-0.129839098367345,0.0359278479980343,
-3.46944695195361E-17));
#23188=CARTESIAN_POINT('Ctrl Pts',(-0.129254890951344,0.0392051855997028,
-3.87818275556788E-17));
#23189=CARTESIAN_POINT('Ctrl Pts',(-0.128542951403208,0.0424656461998481,
-3.10678831811161E-17));
#23190=CARTESIAN_POINT('Ctrl Pts',(-0.1277070993652,0.0457037274559979,
-3.29597460435593E-17));
#23191=CARTESIAN_POINT('Ctrl Pts',(-0.126886363095037,0.0488832504000222,
-3.48173959609792E-17));
#23192=CARTESIAN_POINT('Ctrl Pts',(-0.125948031872817,0.0520333657183593,
-3.53366201082739E-17));
#23193=CARTESIAN_POINT('Ctrl Pts',(-0.124899042599898,0.0551436241923499,
-3.46944695195361E-17));
#23194=CARTESIAN_POINT('Ctrl Pts',(-0.122234979928128,0.0630425834229368,
-3.30636335736642E-17));
#23195=CARTESIAN_POINT('Ctrl Pts',(-0.118856305871375,0.070695441500891,
-2.1366080483524E-17));
#23196=CARTESIAN_POINT('Ctrl Pts',(-0.114834854776346,0.078019637496205,
-1.73472347597681E-17));
#23197=CARTESIAN_POINT('Ctrl Pts',(-0.11215901866562,0.0828930893082948,
-1.46731322388254E-17));
#23198=CARTESIAN_POINT('Ctrl Pts',(-0.109198005187061,0.0876211033078822,
8.28606628989234E-18));
#23199=CARTESIAN_POINT('Ctrl Pts',(-0.105966883726074,0.0921780034666525,
8.67361737988404E-18));
#23200=CARTESIAN_POINT('Ctrl Pts',(-0.104137243112614,0.094758373688769,
8.89307035390601E-18));
#23201=CARTESIAN_POINT('Ctrl Pts',(-0.102221042121924,0.0972831505018574,
-2.31209379389524E-17));
#23202=CARTESIAN_POINT('Ctrl Pts',(-0.100229777791505,0.0997373632832089,
-2.08166817117217E-17));
#23203=CARTESIAN_POINT('Ctrl Pts',(-0.0937202782075859,0.107760254486057,
-1.32840027382311E-17));
#23204=CARTESIAN_POINT('Ctrl Pts',(-0.0863914655699752,0.115060936709644,
5.4842312373535E-18));
#23205=CARTESIAN_POINT('Ctrl Pts',(-0.0783508402622743,0.121487309774744,
1.38777878078145E-17));
#23206=CARTESIAN_POINT('Ctrl Pts',(-0.073610711791116,0.125275800441382,
1.8825977152717E-17));
#23207=CARTESIAN_POINT('Ctrl Pts',(-0.068622257850438,0.128760167547443,
-9.09579695168528E-18));
#23208=CARTESIAN_POINT('Ctrl Pts',(-0.0634007094575209,0.131904027763685,
-6.93889390390723E-18));
#23209=CARTESIAN_POINT('Origin',(0.,0.,0.));
#23210=CARTESIAN_POINT('Origin',(-0.0721687836487033,-0.125,-0.3));
#23211=CARTESIAN_POINT('',(-0.0721687836487033,-0.125,-0.3));
#23212=CARTESIAN_POINT('',(0.0721687836487032,-0.125,-0.3));
#23213=CARTESIAN_POINT('',(-0.0360843918243517,-0.125,-0.3));
#23214=CARTESIAN_POINT('',(-0.0721687836487033,-0.125,-0.15));
#23215=CARTESIAN_POINT('',(-0.0721687836487033,-0.125,-0.3));
#23216=CARTESIAN_POINT('',(0.0721687836487032,-0.125,-0.15));
#23217=CARTESIAN_POINT('',(-0.0721687836487033,-0.125,-0.15));
#23218=CARTESIAN_POINT('',(0.0721687836487032,-0.125,-0.3));
#23219=CARTESIAN_POINT('Origin',(-0.144337567297406,1.76762539787485E-17,
-0.3));
#23220=CARTESIAN_POINT('',(-0.144337567297406,1.76762539787485E-17,-0.3));
#23221=CARTESIAN_POINT('',(-0.126295371385231,-0.03125,-0.3));
#23222=CARTESIAN_POINT('',(-0.144337567297406,2.77555756156289E-17,-0.15));
#23223=CARTESIAN_POINT('',(-0.144337567297406,1.76762539787485E-17,-0.3));
#23224=CARTESIAN_POINT('',(-0.144337567297406,1.76762539787485E-17,-0.15));
#23225=CARTESIAN_POINT('Origin',(-0.0721687836487032,0.125,-0.3));
#23226=CARTESIAN_POINT('',(-0.0721687836487032,0.125,-0.3));
#23227=CARTESIAN_POINT('',(-0.090210979560879,0.09375,-0.3));
#23228=CARTESIAN_POINT('',(-0.0721687836487032,0.125,-0.15));
#23229=CARTESIAN_POINT('',(-0.0721687836487032,0.125,-0.3));
#23230=CARTESIAN_POINT('',(-0.0721687836487032,0.125,-0.15));
#23231=CARTESIAN_POINT('Origin',(0.0721687836487032,0.125,-0.3));
#23232=CARTESIAN_POINT('',(0.0721687836487032,0.125,-0.3));
#23233=CARTESIAN_POINT('',(0.0360843918243516,0.125,-0.3));
#23234=CARTESIAN_POINT('',(0.0721687836487032,0.125,-0.15));
#23235=CARTESIAN_POINT('',(0.0721687836487032,0.125,-0.3));
#23236=CARTESIAN_POINT('',(0.0721687836487032,0.125,-0.15));
#23237=CARTESIAN_POINT('Origin',(0.144337567297406,0.,-0.3));
#23238=CARTESIAN_POINT('',(0.144337567297406,0.,-0.3));
#23239=CARTESIAN_POINT('',(0.126295371385231,0.03125,-0.3));
#23240=CARTESIAN_POINT('',(0.144337567297406,0.,-0.15));
#23241=CARTESIAN_POINT('',(0.144337567297406,0.,-0.3));
#23242=CARTESIAN_POINT('',(0.144337567297406,0.,-0.15));
#23243=CARTESIAN_POINT('Origin',(0.0721687836487032,-0.125,-0.3));
#23244=CARTESIAN_POINT('',(0.0902109795608791,-0.09375,-0.3));
#23245=CARTESIAN_POINT('',(0.0721687836487032,-0.125,-0.15));
#23246=CARTESIAN_POINT('Origin',(0.,0.,-0.15));
#23247=CARTESIAN_POINT('Origin',(0.,0.,0.));
#23248=CARTESIAN_POINT('',(-0.275,-3.36777869765522E-17,0.));
#23249=CARTESIAN_POINT('Origin',(0.,0.,0.));
#23250=CARTESIAN_POINT('Origin',(0.,0.,-0.3));
#23251=CARTESIAN_POINT('',(-0.275,-3.36777869765522E-17,-0.3));
#23252=CARTESIAN_POINT('',(-0.275,-3.36777869765522E-17,-0.3));
#23253=CARTESIAN_POINT('Origin',(0.,0.,-0.3));
#23254=CARTESIAN_POINT('Origin',(0.,0.,-0.3));
#23255=CARTESIAN_POINT('Origin',(0.,0.,1.6));
#24792=UNCERTAINTY_MEASURE_WITH_UNIT(LENGTH_MEASURE(0.001),#24810,
'DISTANCE_ACCURACY_VALUE',
'Maximum model space distance between geometric entities at asserted c
onnectivities');
#24796=UNCERTAINTY_MEASURE_WITH_UNIT(LENGTH_MEASURE(0.001),#24810,
'DISTANCE_ACCURACY_VALUE',
'Maximum model space distance between geometric entities at asserted c
onnectivities');
#24805=(
GEOMETRIC_REPRESENTATION_CONTEXT(3)
GLOBAL_UNCERTAINTY_ASSIGNED_CONTEXT((#24792))
GLOBAL_UNIT_ASSIGNED_CONTEXT((#24810,#24812,#24813))
REPRESENTATION_CONTEXT('','3D')
);
#24809=(
GEOMETRIC_REPRESENTATION_CONTEXT(3)
GLOBAL_UNCERTAINTY_ASSIGNED_CONTEXT((#24796))
GLOBAL_UNIT_ASSIGNED_CONTEXT((#24810,#24812,#24813))
REPRESENTATION_CONTEXT('','3D')
);
#24810=(
LENGTH_UNIT()
NAMED_UNIT(*)
SI_UNIT(.CENTI.,.METRE.)
);
#24812=(
NAMED_UNIT(*)
PLANE_ANGLE_UNIT()
SI_UNIT($,.RADIAN.)
);
#24813=(
NAMED_UNIT(*)
SI_UNIT($,.STERADIAN.)
SOLID_ANGLE_UNIT()
);
#24822=SHAPE_DEFINITION_REPRESENTATION(#24834,#24862);
#24834=PRODUCT_DEFINITION_SHAPE('',$,#24875);
#24862=SHAPE_REPRESENTATION('',(#10487),#24805);
#24866=PRODUCT_DEFINITION_CONTEXT('part definition',#24904,'design');
#24875=PRODUCT_DEFINITION('2026-11-10-05-11-11-302',
'Socket head cap screw M3x16',#24887,#24866);
#24887=PRODUCT_DEFINITION_FORMATION('',$,#24914);
#24904=APPLICATION_CONTEXT(
'Core Data for Automotive Mechanical Design Process');
#24905=PRODUCT_CONTEXT('part definition',#24904,'mechanical');
#24914=PRODUCT('2026-11-10-05-11-11-302','Socket head cap screw M3x16',
$,(#24905));
#24921=PRESENTATION_STYLE_ASSIGNMENT((#24929));
#24929=SURFACE_STYLE_USAGE(.BOTH.,#24937);
#24937=SURFACE_SIDE_STYLE('',(#24945));
#24945=SURFACE_STYLE_FILL_AREA(#24953);
#24953=FILL_AREA_STYLE('Dark gray',(#24961));
#24961=FILL_AREA_STYLE_COLOUR('Dark gray',#24969);
#24969=COLOUR_RGB('Dark gray',0.250980392156863,0.282352941176471,0.32156862745098);
ENDSEC;
END-ISO-10303-21;
